ISO-10303-21;
HEADER;
FILE_DESCRIPTION (('STEP AP214'),
    '1' );
FILE_NAME ('spur gear_iso_ISO - Spur gear 2M 50T 20PA 8FW ---S50A75H50L22.0R1.step',
    '2026-09-28T15:49:00',
    ( '' ),
    ( '' ),
    'SwSTEP 2.0',
    'SolidWorks 2026',
    '' );
FILE_SCHEMA (( 'AUTOMOTIVE_DESIGN' ));
ENDSEC;

DATA;
#3=EDGE_CURVE ( 'NONE', #21603, #30554, #20379, .T. ) ;
#4=EDGE_LOOP ( 'NONE', ( #3245, #31755, #34673, #24973 ) ) ;
#6=EDGE_CURVE ( 'NONE', #33603, #20080, #10924, .T. ) ;
#8=CYLINDRICAL_SURFACE ( 'NONE', #33227, 47.49900000000001654 ) ;
#9=VERTEX_POINT ( 'NONE', #21941 ) ;
#14=ORIENTED_EDGE ( 'NONE', *, *, #31358, .T. ) ;
#17=DIRECTION ( 'NONE',  ( -1.000000000000000000, -0.000000000000000000, -0.000000000000000000 ) ) ;
#21=EDGE_CURVE ( 'NONE', #11865, #28075, #4908, .T. ) ;
#23=CARTESIAN_POINT ( 'NONE',  ( 7.999999999999992895, 0.000000000000000000, 0.000000000000000000 ) ) ;
#24=CARTESIAN_POINT ( 'NONE',  ( 7.999999999999992895, 13.56094713063570723, 50.20060470671747055 ) ) ;
#29=EDGE_CURVE ( 'NONE', #15669, #7819, #25865, .T. ) ;
#30=VERTEX_POINT ( 'NONE', #8607 ) ;
#33=AXIS2_PLACEMENT_3D ( 'NONE', #19655, #6177, #11053 ) ;
#48=ADVANCED_FACE ( 'NONE', ( #22956 ), #19423, .T. ) ;
#50=LINE ( 'NONE', #33346, #23380 ) ;
#57=ORIENTED_EDGE ( 'NONE', *, *, #32180, .F. ) ;
#60=DIRECTION ( 'NONE',  ( 0.000000000000000000, -0.3681245526846852467, 0.9297764858882484607 ) ) ;
#62=CARTESIAN_POINT ( 'NONE',  ( 7.999999999999992895, 46.21320724403649649, 10.97699764141971102 ) ) ;
#69=CIRCLE ( 'NONE', #24242, 52.00000000000000711 ) ;
#74=EDGE_CURVE ( 'NONE', #4180, #540, #6597, .T. ) ;
#75=DIRECTION ( 'NONE',  ( -1.000000000000000000, 0.000000000000000000, -0.000000000000000000 ) ) ;
#76=ORIENTED_EDGE ( 'NONE', *, *, #2779, .T. ) ;
#83=ORIENTED_EDGE ( 'NONE', *, *, #30527, .F. ) ;
#84=LINE ( 'NONE', #13940, #22802 ) ;
#86=CARTESIAN_POINT ( 'NONE',  ( 0.000000000000000000, 43.83938735307269496, 18.28286404005814703 ) ) ;
#88=CYLINDRICAL_SURFACE ( 'NONE', #8916, 47.49900000000001654 ) ;
#93=DIRECTION ( 'NONE',  ( -1.000000000000000000, 0.000000000000000000, -0.000000000000000000 ) ) ;
#96=ORIENTED_EDGE ( 'NONE', *, *, #21612, .T. ) ;
#101=ORIENTED_EDGE ( 'NONE', *, *, #74, .T. ) ;
#107=EDGE_CURVE ( 'NONE', #5795, #7932, #19266, .T. ) ;
#118=CARTESIAN_POINT ( 'NONE',  ( 7.999999999999992895, -46.90537658765327933, -2.727856614654800005 ) ) ;
#128=VERTEX_POINT ( 'NONE', #22295 ) ;
#136=AXIS2_PLACEMENT_3D ( 'NONE', #5268, #29577, #7420 ) ;
#141=ORIENTED_EDGE ( 'NONE', *, *, #2856, .F. ) ;
#144=DIRECTION ( 'NONE',  ( -1.000000000000000000, 0.000000000000000000, -0.000000000000000000 ) ) ;
#145=DIRECTION ( 'NONE',  ( -1.000000000000000000, 0.000000000000000000, 0.000000000000000000 ) ) ;
#164=CARTESIAN_POINT ( 'NONE',  ( 0.000000000000000000, 37.91532898920963390, -28.61088654061597225 ) ) ;
#166=VECTOR ( 'NONE', #13952, 1000.000000000000000 ) ;
#169=VERTEX_POINT ( 'NONE', #28551 ) ;
#171=DIRECTION ( 'NONE',  ( 1.000000000000000000, 0.000000000000000000, 0.000000000000000000 ) ) ;
#172=CARTESIAN_POINT ( 'NONE',  ( 7.999999999999992895, 0.000000000000000000, 0.000000000000000000 ) ) ;
#181=CARTESIAN_POINT ( 'NONE',  ( 7.999999999999992895, -37.91532898920942074, 28.61088654061626357 ) ) ;
#189=VECTOR ( 'NONE', #29534, 1000.000000000000000 ) ;
#191=DIRECTION ( 'NONE',  ( 0.000000000000000000, 0.000000000000000000, 1.000000000000000000 ) ) ;
#203=AXIS2_PLACEMENT_3D ( 'NONE', #2270, #7808, #27270 ) ;
#204=DIRECTION ( 'NONE',  ( -1.000000000000000000, -0.000000000000000000, 0.000000000000000000 ) ) ;
#212=AXIS2_PLACEMENT_3D ( 'NONE', #10093, #32066, #18373 ) ;
#218=ORIENTED_EDGE ( 'NONE', *, *, #1180, .F. ) ;
#225=LINE ( 'NONE', #30656, #27926 ) ;
#226=EDGE_LOOP ( 'NONE', ( #27642, #13433, #11030, #13764 ) ) ;
#236=AXIS2_PLACEMENT_3D ( 'NONE', #6665, #9551, #20518 ) ;
#237=FACE_OUTER_BOUND ( 'NONE', #27820, .T. ) ;
#264=EDGE_CURVE ( 'NONE', #30567, #34766, #2139, .T. ) ;
#275=EDGE_CURVE ( 'NONE', #2191, #19467, #3280, .T. ) ;
#286=DIRECTION ( 'NONE',  ( -1.000000000000000000, 0.000000000000000000, 0.000000000000000000 ) ) ;
#288=DIRECTION ( 'NONE',  ( -1.000000000000000000, 0.000000000000000000, 0.000000000000000000 ) ) ;
#290=CYLINDRICAL_SURFACE ( 'NONE', #33735, 20.00000000000000355 ) ;
#293=CIRCLE ( 'NONE', #26762, 20.00000000000001066 ) ;
#295=ORIENTED_EDGE ( 'NONE', *, *, #4026, .T. ) ;
#297=FACE_OUTER_BOUND ( 'NONE', #4749, .T. ) ;
#303=EDGE_LOOP ( 'NONE', ( #1691, #1216, #1468, #3078 ) ) ;
#317=ORIENTED_EDGE ( 'NONE', *, *, #1121, .T. ) ;
#320=CARTESIAN_POINT ( 'NONE',  ( 7.999999999999992895, 0.000000000000000000, 0.000000000000000000 ) ) ;
#321=ORIENTED_EDGE ( 'NONE', *, *, #9480, .F. ) ;
#323=AXIS2_PLACEMENT_3D ( 'NONE', #35472, #10977, #16174 ) ;
#329=CARTESIAN_POINT ( 'NONE',  ( 0.000000000000000000, -45.78515115856053797, 12.64416602183649019 ) ) ;
#338=AXIS2_PLACEMENT_3D ( 'NONE', #9593, #20561, #17688 ) ;
#348=EDGE_LOOP ( 'NONE', ( #11431, #30900, #20303, #6750 ) ) ;
#349=AXIS2_PLACEMENT_3D ( 'NONE', #33743, #25292, #25111 ) ;
#352=VERTEX_POINT ( 'NONE', #8172 ) ;
#353=ORIENTED_EDGE ( 'NONE', *, *, #11463, .F. ) ;
#355=CARTESIAN_POINT ( 'NONE',  ( 7.999999999999992895, 0.000000000000000000, 0.000000000000000000 ) ) ;
#357=ORIENTED_EDGE ( 'NONE', *, *, #10887, .T. ) ;
#360=ORIENTED_EDGE ( 'NONE', *, *, #19402, .F. ) ;
#369=DIRECTION ( 'NONE',  ( 1.000000000000000000, 0.000000000000000000, 0.000000000000000000 ) ) ;
#377=CARTESIAN_POINT ( 'NONE',  ( 0.000000000000000000, 44.75336757549799671, -14.30704879393557327 ) ) ;
#380=ORIENTED_EDGE ( 'NONE', *, *, #21612, .F. ) ;
#386=CARTESIAN_POINT ( 'NONE',  ( 7.999999999999992895, 46.90537658765329354, 2.727856614654466938 ) ) ;
#388=CARTESIAN_POINT ( 'NONE',  ( 0.000000000000000000, 51.19683565102445755, 9.104066087303644750 ) ) ;
#389=AXIS2_PLACEMENT_3D ( 'NONE', #7723, #24133, #18535 ) ;
#390=VECTOR ( 'NONE', #25326, 1000.000000000000000 ) ;
#392=CIRCLE ( 'NONE', #1591, 47.49900000000000944 ) ;
#395=ORIENTED_EDGE ( 'NONE', *, *, #3137, .T. ) ;
#396=ORIENTED_EDGE ( 'NONE', *, *, #22449, .F. ) ;
#403=VERTEX_POINT ( 'NONE', #30151 ) ;
#404=EDGE_LOOP ( 'NONE', ( #13036, #19341, #25152, #34846 ) ) ;
#416=AXIS2_PLACEMENT_3D ( 'NONE', #846, #31809, #12558 ) ;
#417=ADVANCED_FACE ( 'NONE', ( #22037 ), #5488, .T. ) ;
#423=VERTEX_POINT ( 'NONE', #35569 ) ;
#424=DIRECTION ( 'NONE',  ( 0.000000000000000000, 0.000000000000000000, 1.000000000000000000 ) ) ;
#425=CYLINDRICAL_SURFACE ( 'NONE', #5340, 47.49900000000001654 ) ;
#432=DIRECTION ( 'NONE',  ( 0.000000000000000000, 0.000000000000000000, 1.000000000000000000 ) ) ;
#433=CARTESIAN_POINT ( 'NONE',  ( 7.999999999999992895, 45.78515115856061612, -12.64416602183615623 ) ) ;
#437=DIRECTION ( 'NONE',  ( 0.000000000000000000, 0.1253332335643046747, -0.9921147013144777649 ) ) ;
#453=VERTEX_POINT ( 'NONE', #32313 ) ;
#454=CIRCLE ( 'NONE', #19981, 20.00000000000000355 ) ;
#471=CIRCLE ( 'NONE', #25782, 20.00000000000000711 ) ;
#477=ORIENTED_EDGE ( 'NONE', *, *, #31892, .F. ) ;
#479=ADVANCED_FACE ( 'NONE', ( #18984 ), #14625, .T. ) ;
#482=CARTESIAN_POINT ( 'NONE',  ( 0.000000000000000000, 51.85248208264525260, -3.914090171285633524 ) ) ;
#488=DIRECTION ( 'NONE',  ( 0.000000000000000000, 0.5877852522924742473, -0.8090169943749466741 ) ) ;
#494=CARTESIAN_POINT ( 'NONE',  ( 0.000000000000000000, -34.03046037009232094, -33.13733193845841640 ) ) ;
#503=CARTESIAN_POINT ( 'NONE',  ( 0.000000000000000000, 17.08890430202750110, 43.76671000081951490 ) ) ;
#506=ADVANCED_FACE ( 'NONE', ( #28329 ), #31024, .T. ) ;
#508=DIRECTION ( 'NONE',  ( -1.000000000000000000, 0.000000000000000000, -0.000000000000000000 ) ) ;
#512=CARTESIAN_POINT ( 'NONE',  ( 7.999999999999992895, 0.000000000000000000, 0.000000000000000000 ) ) ;
#513=DIRECTION ( 'NONE',  ( -1.000000000000000000, -0.000000000000000000, -0.000000000000000000 ) ) ;
#524=EDGE_CURVE ( 'NONE', #10046, #1935, #25095, .T. ) ;
#531=DIRECTION ( 'NONE',  ( -1.000000000000000000, 0.000000000000000000, 0.000000000000000000 ) ) ;
#535=ORIENTED_EDGE ( 'NONE', *, *, #3545, .F. ) ;
#540=VERTEX_POINT ( 'NONE', #11585 ) ;
#556=ORIENTED_EDGE ( 'NONE', *, *, #35529, .F. ) ;
#557=ORIENTED_EDGE ( 'NONE', *, *, #20368, .F. ) ;
#558=LINE ( 'NONE', #915, #5728 ) ;
#560=ORIENTED_EDGE ( 'NONE', *, *, #26222, .T. ) ;
#562=EDGE_LOOP ( 'NONE', ( #8046, #15728, #33138, #17649 ) ) ;
#570=VECTOR ( 'NONE', #19867, 1000.000000000000000 ) ;
#574=VERTEX_POINT ( 'NONE', #20021 ) ;
#576=VECTOR ( 'NONE', #819, 1000.000000000000000 ) ;
#578=AXIS2_PLACEMENT_3D ( 'NONE', #13486, #24469, #16158 ) ;
#579=CARTESIAN_POINT ( 'NONE',  ( 7.999999999999992895, -24.47917365149979219, 45.87777302070927732 ) ) ;
#585=ORIENTED_EDGE ( 'NONE', *, *, #4307, .T. ) ;
#587=EDGE_CURVE ( 'NONE', #5670, #2768, #8782, .T. ) ;
#591=LINE ( 'NONE', #31017, #5597 ) ;
#595=VECTOR ( 'NONE', #30757, 1000.000000000000000 ) ;
#603=DIRECTION ( 'NONE',  ( -1.000000000000000000, 0.000000000000000000, 0.000000000000000000 ) ) ;
#604=ORIENTED_EDGE ( 'NONE', *, *, #33983, .T. ) ;
#605=LINE ( 'NONE', #3678, #32361 ) ;
#608=DIRECTION ( 'NONE',  ( 0.000000000000000000, 0.9980267284282712259, 0.06279051952931682945 ) ) ;
#610=CARTESIAN_POINT ( 'NONE',  ( -9.999999999999994671, 0.000000000000000000, 0.000000000000000000 ) ) ;
#615=ORIENTED_EDGE ( 'NONE', *, *, #4691, .F. ) ;
#618=ORIENTED_EDGE ( 'NONE', *, *, #23308, .T. ) ;
#621=CARTESIAN_POINT ( 'NONE',  ( 7.999999999999992895, 0.000000000000000000, 0.000000000000000000 ) ) ;
#630=DIRECTION ( 'NONE',  ( -1.000000000000000000, -0.000000000000000000, 0.000000000000000000 ) ) ;
#634=DIRECTION ( 'NONE',  ( -1.000000000000000000, 0.000000000000000000, 0.000000000000000000 ) ) ;
#635=AXIS2_PLACEMENT_3D ( 'NONE', #18306, #29485, #1579 ) ;
#645=ORIENTED_EDGE ( 'NONE', *, *, #12370, .F. ) ;
#648=CARTESIAN_POINT ( 'NONE',  ( 7.999999999999992895, 47.00885577955413908, 6.806061952192451692 ) ) ;
#649=CARTESIAN_POINT ( 'NONE',  ( 7.999999999999992895, 19.44205635905603202, -43.33776004284589334 ) ) ;
#654=CARTESIAN_POINT ( 'NONE',  ( 0.000000000000000000, 35.20873326984128227, -31.88259874183993503 ) ) ;
#655=ORIENTED_EDGE ( 'NONE', *, *, #31762, .F. ) ;
#658=CARTESIAN_POINT ( 'NONE',  ( 4.000000000000003553, 44.25018368420744252, 27.31155879685197263 ) ) ;
#668=CARTESIAN_POINT ( 'NONE',  ( 7.999999999999992895, -47.22458491092824318, 5.098390039074071289 ) ) ;
#682=DIRECTION ( 'NONE',  ( 0.000000000000000000, 0.9048270524660205760, -0.4257792915650702170 ) ) ;
#685=DIRECTION ( 'NONE',  ( -1.000000000000000000, 0.000000000000000000, -0.000000000000000000 ) ) ;
#687=CARTESIAN_POINT ( 'NONE',  ( 7.999999999999992895, 44.75336757549799671, -14.30704879393557327 ) ) ;
#688=VERTEX_POINT ( 'NONE', #7244 ) ;
#692=ORIENTED_EDGE ( 'NONE', *, *, #31285, .T. ) ;
#693=ORIENTED_EDGE ( 'NONE', *, *, #12556, .F. ) ;
#698=EDGE_CURVE ( 'NONE', #15493, #29381, #34092, .T. ) ;
#703=ORIENTED_EDGE ( 'NONE', *, *, #21313, .T. ) ;
#707=EDGE_LOOP ( 'NONE', ( #35537, #16646, #35410, #34981 ) ) ;
#712=FACE_OUTER_BOUND ( 'NONE', #1339, .T. ) ;
#718=CIRCLE ( 'NONE', #22558, 52.00000000000000711 ) ;
#728=DIRECTION ( 'NONE',  ( -1.000000000000000000, 0.000000000000000000, -0.000000000000000000 ) ) ;
#731=CARTESIAN_POINT ( 'NONE',  ( 7.999999999999992895, -7.162210897275381072, -51.50439529848838305 ) ) ;
#732=DIRECTION ( 'NONE',  ( 0.000000000000000000, 0.000000000000000000, 1.000000000000000000 ) ) ;
#734=AXIS2_PLACEMENT_3D ( 'NONE', #10668, #13371, #21624 ) ;
#736=ORIENTED_EDGE ( 'NONE', *, *, #10860, .F. ) ;
#744=ORIENTED_EDGE ( 'NONE', *, *, #6570, .T. ) ;
#749=CIRCLE ( 'NONE', #31207, 52.00000000000000711 ) ;
#773=AXIS2_PLACEMENT_3D ( 'NONE', #25054, #11547, #30805 ) ;
#774=CIRCLE ( 'NONE', #13989, 47.49900000000001654 ) ;
#779=VERTEX_POINT ( 'NONE', #6892 ) ;
#783=CARTESIAN_POINT ( 'NONE',  ( 7.999999999999992895, 15.49408907645234734, -44.90087086784577508 ) ) ;
#786=DIRECTION ( 'NONE',  ( -1.000000000000000000, -0.000000000000000000, 0.000000000000000000 ) ) ;
#791=CARTESIAN_POINT ( 'NONE',  ( 7.999999999999992895, 39.78933988720149273, -24.98727647984960853 ) ) ;
#795=ORIENTED_EDGE ( 'NONE', *, *, #19790, .F. ) ;
#800=AXIS2_PLACEMENT_3D ( 'NONE', #30330, #75, #27458 ) ;
#804=FACE_OUTER_BOUND ( 'NONE', #7598, .T. ) ;
#806=AXIS2_PLACEMENT_3D ( 'NONE', #19835, #22373, #33370 ) ;
#814=DIRECTION ( 'NONE',  ( 0.000000000000000000, 0.1253332335642974305, 0.9921147013144787641 ) ) ;
#815=DIRECTION ( 'NONE',  ( 0.000000000000000000, 0.000000000000000000, 1.000000000000000000 ) ) ;
#819=DIRECTION ( 'NONE',  ( -1.000000000000000000, 0.000000000000000000, -0.000000000000000000 ) ) ;
#822=DIRECTION ( 'NONE',  ( -1.000000000000000000, 0.000000000000000000, 0.000000000000000000 ) ) ;
#828=LINE ( 'NONE', #11810, #9606 ) ;
#833=ORIENTED_EDGE ( 'NONE', *, *, #10772, .F. ) ;
#836=EDGE_CURVE ( 'NONE', #11310, #17425, #3855, .T. ) ;
#838=CARTESIAN_POINT ( 'NONE',  ( 0.000000000000000000, -39.64889472655756464, 33.64468972902493960 ) ) ;
#846=CARTESIAN_POINT ( 'NONE',  ( -9.999999999999994671, 0.000000000000000000, 0.000000000000000000 ) ) ;
#849=CYLINDRICAL_SURFACE ( 'NONE', #28263, 47.49900000000001654 ) ;
#863=CYLINDRICAL_SURFACE ( 'NONE', #14722, 47.49900000000001654 ) ;
#868=ORIENTED_EDGE ( 'NONE', *, *, #16358, .T. ) ;
#870=AXIS2_PLACEMENT_3D ( 'NONE', #6568, #19233, #11989 ) ;
#877=EDGE_CURVE ( 'NONE', #33166, #32215, #26711, .T. ) ;
#881=AXIS2_PLACEMENT_3D ( 'NONE', #18246, #26551, #34156 ) ;
#883=EDGE_LOOP ( 'NONE', ( #34471, #34935, #28562, #25963 ) ) ;
#886=EDGE_CURVE ( 'NONE', #6583, #5115, #8131, .T. ) ;
#888=ADVANCED_FACE ( 'NONE', ( #7597 ), #29763, .T. ) ;
#892=VERTEX_POINT ( 'NONE', #10490 ) ;
#895=ORIENTED_EDGE ( 'NONE', *, *, #19002, .T. ) ;
#900=DIRECTION ( 'NONE',  ( 0.000000000000000000, 0.000000000000000000, 1.000000000000000000 ) ) ;
#902=LINE ( 'NONE', #34037, #32658 ) ;
#907=DIRECTION ( 'NONE',  ( -1.000000000000000000, -0.000000000000000000, 0.000000000000000000 ) ) ;
#915=CARTESIAN_POINT ( 'NONE',  ( 4.000000000000003553, -12.30077720129132679, 50.52416135122078344 ) ) ;
#917=AXIS2_PLACEMENT_3D ( 'NONE', #22747, #16640, #22392 ) ;
#921=ORIENTED_EDGE ( 'NONE', *, *, #33278, .T. ) ;
#927=ORIENTED_EDGE ( 'NONE', *, *, #14396, .F. ) ;
#929=CARTESIAN_POINT ( 'NONE',  ( 0.000000000000000000, 22.43957647427161461, 41.27978878573636479 ) ) ;
#933=VERTEX_POINT ( 'NONE', #16399 ) ;
#936=AXIS2_PLACEMENT_3D ( 'NONE', #35608, #27322, #5706 ) ;
#941=ORIENTED_EDGE ( 'NONE', *, *, #10320, .T. ) ;
#944=ORIENTED_EDGE ( 'NONE', *, *, #22014, .F. ) ;
#945=ORIENTED_EDGE ( 'NONE', *, *, #7975, .T. ) ;
#948=DIRECTION ( 'NONE',  ( -1.000000000000000000, 0.000000000000000000, 0.000000000000000000 ) ) ;
#951=DIRECTION ( 'NONE',  ( 0.000000000000000000, 0.3681245526846718685, 0.9297764858882537897 ) ) ;
#958=DIRECTION ( 'NONE',  ( 0.000000000000000000, 0.000000000000000000, 1.000000000000000000 ) ) ;
#962=CARTESIAN_POINT ( 'NONE',  ( 0.000000000000000000, -42.60732521687585006, 19.80331771201643321 ) ) ;
#963=DIRECTION ( 'NONE',  ( 0.000000000000000000, 0.000000000000000000, 1.000000000000000000 ) ) ;
#965=AXIS2_PLACEMENT_3D ( 'NONE', #19885, #17736, #3717 ) ;
#966=VERTEX_POINT ( 'NONE', #18759 ) ;
#967=AXIS2_PLACEMENT_3D ( 'NONE', #19477, #2946, #5809 ) ;
#973=EDGE_CURVE ( 'NONE', #27298, #22879, #2405, .T. ) ;
#978=CYLINDRICAL_SURFACE ( 'NONE', #23374, 20.00000000000000355 ) ;
#987=EDGE_LOOP ( 'NONE', ( #17416, #22843, #3443, #6878 ) ) ;
#989=ORIENTED_EDGE ( 'NONE', *, *, #3063, .T. ) ;
#992=CIRCLE ( 'NONE', #28003, 47.49900000000001654 ) ;
#994=CIRCLE ( 'NONE', #2177, 52.00000000000000711 ) ;
#1008=ORIENTED_EDGE ( 'NONE', *, *, #33723, .T. ) ;
#1014=AXIS2_PLACEMENT_3D ( 'NONE', #5144, #32851, #10892 ) ;
#1015=DIRECTION ( 'NONE',  ( 1.000000000000000000, 0.000000000000000000, -0.000000000000000000 ) ) ;
#1016=CYLINDRICAL_SURFACE ( 'NONE', #2626, 52.00000000000000711 ) ;
#1022=CIRCLE ( 'NONE', #2766, 47.49900000000001654 ) ;
#1032=ORIENTED_EDGE ( 'NONE', *, *, #29947, .T. ) ;
#1047=VECTOR ( 'NONE', #10594, 1000.000000000000000 ) ;
#1049=DIRECTION ( 'NONE',  ( 0.000000000000000000, 0.000000000000000000, 1.000000000000000000 ) ) ;
#1051=ADVANCED_FACE ( 'NONE', ( #25419 ), #33335, .T. ) ;
#1061=EDGE_LOOP ( 'NONE', ( #19343, #9916, #7797, #11714 ) ) ;
#1071=CARTESIAN_POINT ( 'NONE',  ( -9.999999999999994671, 0.000000000000000000, 52.00000000000000711 ) ) ;
#1073=VECTOR ( 'NONE', #29292, 1000.000000000000000 ) ;
#1076=VECTOR ( 'NONE', #16065, 1000.000000000000000 ) ;
#1078=ORIENTED_EDGE ( 'NONE', *, *, #3827, .T. ) ;
#1081=EDGE_LOOP ( 'NONE', ( #34389, #6733, #17492, #18601 ) ) ;
#1086=DIRECTION ( 'NONE',  ( 0.000000000000000000, -0.4817536741017037771, -0.8763066800438699122 ) ) ;
#1097=ORIENTED_EDGE ( 'NONE', *, *, #34186, .F. ) ;
#1098=CIRCLE ( 'NONE', #1672, 20.00000000000000711 ) ;
#1111=DIRECTION ( 'NONE',  ( -1.000000000000000000, 0.000000000000000000, 0.000000000000000000 ) ) ;
#1112=CARTESIAN_POINT ( 'NONE',  ( 7.999999999999992895, 50.95304419620840264, -10.38206564895607897 ) ) ;
#1121=EDGE_CURVE ( 'NONE', #31360, #19035, #11897, .T. ) ;
#1123=DIRECTION ( 'NONE',  ( -1.000000000000000000, 0.000000000000000000, 0.000000000000000000 ) ) ;
#1125=ORIENTED_EDGE ( 'NONE', *, *, #11845, .F. ) ;
#1130=ORIENTED_EDGE ( 'NONE', *, *, #6598, .T. ) ;
#1141=FACE_OUTER_BOUND ( 'NONE', #15819, .T. ) ;
#1143=EDGE_CURVE ( 'NONE', #23788, #31360, #16286, .T. ) ;
#1148=ORIENTED_EDGE ( 'NONE', *, *, #29574, .T. ) ;
#1150=CARTESIAN_POINT ( 'NONE',  ( 0.000000000000000000, -20.99948489194452250, 42.60488980472776177 ) ) ;
#1155=FACE_OUTER_BOUND ( 'NONE', #2027, .T. ) ;
#1166=ORIENTED_EDGE ( 'NONE', *, *, #2056, .T. ) ;
#1167=VERTEX_POINT ( 'NONE', #33502 ) ;
#1175=DIRECTION ( 'NONE',  ( 0.000000000000000000, 0.000000000000000000, 1.000000000000000000 ) ) ;
#1180=EDGE_CURVE ( 'NONE', #19478, #15493, #33568, .T. ) ;
#1188=CARTESIAN_POINT ( 'NONE',  ( 7.999999999999992895, -44.25018368420762016, 27.31155879685168131 ) ) ;
#1189=DIRECTION ( 'NONE',  ( 0.000000000000000000, -0.1253332335642905193, -0.9921147013144796523 ) ) ;
#1191=CARTESIAN_POINT ( 'NONE',  ( 4.000000000000003553, -31.08872492059928305, -41.68322423723133596 ) ) ;
#1201=DIRECTION ( 'NONE',  ( -1.000000000000000000, 0.000000000000000000, -0.000000000000000000 ) ) ;
#1210=EDGE_CURVE ( 'NONE', #15079, #24598, #29193, .T. ) ;
#1216=ORIENTED_EDGE ( 'NONE', *, *, #6898, .F. ) ;
#1220=ORIENTED_EDGE ( 'NONE', *, *, #17331, .T. ) ;
#1233=DIRECTION ( 'NONE',  ( -1.000000000000000000, 0.000000000000000000, -0.000000000000000000 ) ) ;
#1234=DIRECTION ( 'NONE',  ( 0.000000000000000000, 0.000000000000000000, 1.000000000000000000 ) ) ;
#1237=ORIENTED_EDGE ( 'NONE', *, *, #26784, .F. ) ;
#1239=DIRECTION ( 'NONE',  ( 0.000000000000000000, 0.000000000000000000, -1.000000000000000000 ) ) ;
#1242=ORIENTED_EDGE ( 'NONE', *, *, #4478, .F. ) ;
#1244=ORIENTED_EDGE ( 'NONE', *, *, #30141, .T. ) ;
#1261=CARTESIAN_POINT ( 'NONE',  ( 7.999999999999992895, -36.05989434073634925, 30.12041790338604130 ) ) ;
#1277=ORIENTED_EDGE ( 'NONE', *, *, #33014, .F. ) ;
#1285=EDGE_CURVE ( 'NONE', #9210, #9731, #26681, .T. ) ;
#1289=EDGE_CURVE ( 'NONE', #9085, #7270, #12869, .T. ) ;
#1294=ORIENTED_EDGE ( 'NONE', *, *, #20447, .T. ) ;
#1301=VERTEX_POINT ( 'NONE', #12081 ) ;
#1304=DIRECTION ( 'NONE',  ( 0.000000000000000000, 0.000000000000000000, -1.000000000000000000 ) ) ;
#1313=DIRECTION ( 'NONE',  ( 0.000000000000000000, 0.000000000000000000, 1.000000000000000000 ) ) ;
#1319=VECTOR ( 'NONE', #603, 1000.000000000000000 ) ;
#1320=CIRCLE ( 'NONE', #19123, 52.00000000000000711 ) ;
#1331=VERTEX_POINT ( 'NONE', #34423 ) ;
#1333=EDGE_CURVE ( 'NONE', #31962, #25998, #21476, .T. ) ;
#1336=ORIENTED_EDGE ( 'NONE', *, *, #33171, .F. ) ;
#1339=EDGE_LOOP ( 'NONE', ( #24643, #28837, #2913, #12705 ) ) ;
#1341=AXIS2_PLACEMENT_3D ( 'NONE', #13158, #21408, #35126 ) ;
#1347=VECTOR ( 'NONE', #5447, 1000.000000000000000 ) ;
#1349=DIRECTION ( 'NONE',  ( 0.000000000000000000, 0.000000000000000000, 1.000000000000000000 ) ) ;
#1360=EDGE_CURVE ( 'NONE', #6851, #27996, #26102, .T. ) ;
#1364=CARTESIAN_POINT ( 'NONE',  ( 7.999999999999992895, 0.000000000000000000, 0.000000000000000000 ) ) ;
#1366=FACE_OUTER_BOUND ( 'NONE', #1458, .T. ) ;
#1374=VERTEX_POINT ( 'NONE', #1112 ) ;
#1378=EDGE_CURVE ( 'NONE', #15078, #7666, #28381, .T. ) ;
#1384=DIRECTION ( 'NONE',  ( -1.000000000000000000, -0.000000000000000000, -0.000000000000000000 ) ) ;
#1387=CARTESIAN_POINT ( 'NONE',  ( 7.999999999999992895, 0.000000000000000000, 0.000000000000000000 ) ) ;
#1388=ORIENTED_EDGE ( 'NONE', *, *, #27301, .T. ) ;
#1405=EDGE_CURVE ( 'NONE', #11997, #7078, #5393, .T. ) ;
#1414=CARTESIAN_POINT ( 'NONE',  ( 0.000000000000000000, -6.109652351742118626, 46.58570277113506819 ) ) ;
#1418=CARTESIAN_POINT ( 'NONE',  ( 0.000000000000000000, -19.44205635905572649, 43.33776004284603545 ) ) ;
#1421=EDGE_CURVE ( 'NONE', #33849, #12864, #8271, .T. ) ;
#1423=EDGE_CURVE ( 'NONE', #19035, #2094, #30704, .T. ) ;
#1430=VERTEX_POINT ( 'NONE', #2549 ) ;
#1431=ORIENTED_EDGE ( 'NONE', *, *, #8430, .T. ) ;
#1441=DIRECTION ( 'NONE',  ( 0.000000000000000000, 0.2486898871648482723, 0.9685831611286327414 ) ) ;
#1446=ORIENTED_EDGE ( 'NONE', *, *, #15244, .T. ) ;
#1447=DIRECTION ( 'NONE',  ( 1.000000000000000000, -0.000000000000000000, -0.000000000000000000 ) ) ;
#1458=EDGE_LOOP ( 'NONE', ( #11792, #3585, #10476, #29290 ) ) ;
#1463=ORIENTED_EDGE ( 'NONE', *, *, #1964, .T. ) ;
#1466=CARTESIAN_POINT ( 'NONE',  ( 0.000000000000000000, 44.25018368420781911, -27.31155879685134735 ) ) ;
#1468=ORIENTED_EDGE ( 'NONE', *, *, #7214, .F. ) ;
#1471=CARTESIAN_POINT ( 'NONE',  ( 7.999999999999992895, -42.41764978026593269, -20.20639853260333751 ) ) ;
#1473=ORIENTED_EDGE ( 'NONE', *, *, #27539, .T. ) ;
#1489=DIRECTION ( 'NONE',  ( -1.000000000000000000, 0.000000000000000000, 0.000000000000000000 ) ) ;
#1497=DIRECTION ( 'NONE',  ( 0.000000000000000000, 0.000000000000000000, 1.000000000000000000 ) ) ;
#1498=CIRCLE ( 'NONE', #11263, 20.00000000000000355 ) ;
#1506=AXIS2_PLACEMENT_3D ( 'NONE', #11333, #10980, #8612 ) ;
#1509=CARTESIAN_POINT ( 'NONE',  ( 7.999999999999992895, 8.053585752062575764, -46.81126742072014224 ) ) ;
#1512=ORIENTED_EDGE ( 'NONE', *, *, #33057, .T. ) ;
#1515=CIRCLE ( 'NONE', #9556, 47.49900000000001654 ) ;
#1517=EDGE_LOOP ( 'NONE', ( #11963, #9808, #14744, #20075 ) ) ;
#1524=VECTOR ( 'NONE', #11116, 1000.000000000000000 ) ;
#1537=FACE_OUTER_BOUND ( 'NONE', #4, .T. ) ;
#1543=CARTESIAN_POINT ( 'NONE',  ( -9.999999999999994671, 0.000000000000000000, 0.000000000000000000 ) ) ;
#1560=EDGE_LOOP ( 'NONE', ( #24461, #30077, #34040, #21604 ) ) ;
#1563=AXIS2_PLACEMENT_3D ( 'NONE', #7966, #2244, #21462 ) ;
#1566=DIRECTION ( 'NONE',  ( 0.000000000000000000, 0.000000000000000000, -1.000000000000000000 ) ) ;
#1568=CIRCLE ( 'NONE', #21677, 20.00000000000000711 ) ;
#1575=ORIENTED_EDGE ( 'NONE', *, *, #17609, .T. ) ;
#1576=DIRECTION ( 'NONE',  ( -1.000000000000000000, -0.000000000000000000, -0.000000000000000000 ) ) ;
#1579=DIRECTION ( 'NONE',  ( 0.000000000000000000, 0.9822872507286879440, 0.1873813145857286533 ) ) ;
#1591=AXIS2_PLACEMENT_3D ( 'NONE', #9571, #1658, #14789 ) ;
#1593=CARTESIAN_POINT ( 'NONE',  ( -9.999999999999994671, 0.000000000000000000, 0.000000000000000000 ) ) ;
#1599=DIRECTION ( 'NONE',  ( 0.000000000000000000, -0.4817536741017222623, 0.8763066800438598092 ) ) ;
#1601=EDGE_CURVE ( 'NONE', #2400, #19047, #7682, .T. ) ;
#1612=AXIS2_PLACEMENT_3D ( 'NONE', #34734, #34923, #10247 ) ;
#1619=AXIS2_PLACEMENT_3D ( 'NONE', #24813, #19725, #5552 ) ;
#1626=DIRECTION ( 'NONE',  ( -1.000000000000000000, 0.000000000000000000, -0.000000000000000000 ) ) ;
#1634=LINE ( 'NONE', #31862, #22234 ) ;
#1637=DIRECTION ( 'NONE',  ( 0.000000000000000000, 0.000000000000000000, 1.000000000000000000 ) ) ;
#1640=VERTEX_POINT ( 'NONE', #17075 ) ;
#1643=AXIS2_PLACEMENT_3D ( 'NONE', #35597, #17003, #14133 ) ;
#1651=ORIENTED_EDGE ( 'NONE', *, *, #19402, .T. ) ;
#1658=DIRECTION ( 'NONE',  ( -1.000000000000000000, -0.000000000000000000, 0.000000000000000000 ) ) ;
#1660=CARTESIAN_POINT ( 'NONE',  ( 7.999999999999992895, -42.41764978026593269, -20.20639853260333751 ) ) ;
#1661=ORIENTED_EDGE ( 'NONE', *, *, #9630, .T. ) ;
#1662=ORIENTED_EDGE ( 'NONE', *, *, #15007, .F. ) ;
#1672=AXIS2_PLACEMENT_3D ( 'NONE', #9437, #12867, #15717 ) ;
#1678=LINE ( 'NONE', #29755, #10646 ) ;
#1681=DIRECTION ( 'NONE',  ( 0.000000000000000000, 0.000000000000000000, 1.000000000000000000 ) ) ;
#1683=ORIENTED_EDGE ( 'NONE', *, *, #29106, .F. ) ;
#1691=ORIENTED_EDGE ( 'NONE', *, *, #21387, .T. ) ;
#1693=FACE_OUTER_BOUND ( 'NONE', #25240, .T. ) ;
#1695=DIRECTION ( 'NONE',  ( -1.000000000000000000, 0.000000000000000000, 0.000000000000000000 ) ) ;
#1699=VECTOR ( 'NONE', #25053, 1000.000000000000000 ) ;
#1700=ORIENTED_EDGE ( 'NONE', *, *, #28806, .F. ) ;
#1703=EDGE_CURVE ( 'NONE', #33387, #8613, #31283, .T. ) ;
#1710=FACE_OUTER_BOUND ( 'NONE', #26903, .T. ) ;
#1725=CARTESIAN_POINT ( 'NONE',  ( 7.999999999999992895, 0.000000000000000000, 0.000000000000000000 ) ) ;
#1731=ORIENTED_EDGE ( 'NONE', *, *, #25116, .T. ) ;
#1740=ORIENTED_EDGE ( 'NONE', *, *, #5999, .T. ) ;
#1742=VERTEX_POINT ( 'NONE', #19437 ) ;
#1746=FACE_OUTER_BOUND ( 'NONE', #7968, .T. ) ;
#1750=ORIENTED_EDGE ( 'NONE', *, *, #12552, .T. ) ;
#1759=CIRCLE ( 'NONE', #33, 47.49900000000001654 ) ;
#1764=CARTESIAN_POINT ( 'NONE',  ( 7.999999999999992895, 19.44205635905542451, 43.33776004284616334 ) ) ;
#1768=CARTESIAN_POINT ( 'NONE',  ( 7.999999999999992895, 24.47917365149947244, 45.87777302070943364 ) ) ;
#1775=AXIS2_PLACEMENT_3D ( 'NONE', #9392, #14792, #34435 ) ;
#1776=LINE ( 'NONE', #17956, #13518 ) ;
#1786=ORIENTED_EDGE ( 'NONE', *, *, #16107, .T. ) ;
#1788=LINE ( 'NONE', #26456, #1047 ) ;
#1791=DIRECTION ( 'NONE',  ( 0.000000000000000000, 0.000000000000000000, 1.000000000000000000 ) ) ;
#1801=CIRCLE ( 'NONE', #20164, 20.00000000000000355 ) ;
#1805=EDGE_CURVE ( 'NONE', #11039, #33784, #34741, .T. ) ;
#1812=CARTESIAN_POINT ( 'NONE',  ( 4.000000000000003553, -49.65209126885753221, -15.44894276735603356 ) ) ;
#1814=DIRECTION ( 'NONE',  ( 0.000000000000000000, 0.000000000000000000, 1.000000000000000000 ) ) ;
#1824=EDGE_CURVE ( 'NONE', #4708, #15928, #3696, .T. ) ;
#1829=DIRECTION ( 'NONE',  ( 0.000000000000000000, 0.000000000000000000, -1.000000000000000000 ) ) ;
#1831=CARTESIAN_POINT ( 'NONE',  ( 0.000000000000000000, 0.000000000000000000, 0.000000000000000000 ) ) ;
#1837=DIRECTION ( 'NONE',  ( 0.000000000000000000, 0.9048270524660205760, -0.4257792915650703836 ) ) ;
#1839=VERTEX_POINT ( 'NONE', #29151 ) ;
#1845=FACE_OUTER_BOUND ( 'NONE', #31583, .T. ) ;
#1846=ORIENTED_EDGE ( 'NONE', *, *, #19121, .F. ) ;
#1853=ADVANCED_FACE ( 'NONE', ( #12398 ), #34017, .T. ) ;
#1855=DIRECTION ( 'NONE',  ( -1.000000000000000000, -0.000000000000000000, -0.000000000000000000 ) ) ;
#1867=EDGE_CURVE ( 'NONE', #13043, #6684, #17784, .T. ) ;
#1868=VERTEX_POINT ( 'NONE', #25917 ) ;
#1873=DIRECTION ( 'NONE',  ( -1.000000000000000000, 0.000000000000000000, -0.000000000000000000 ) ) ;
#1874=DIRECTION ( 'NONE',  ( -1.000000000000000000, 0.000000000000000000, -0.000000000000000000 ) ) ;
#1880=CARTESIAN_POINT ( 'NONE',  ( 4.000000000000003553, -49.65209126885775248, 15.44894276735532479 ) ) ;
#1885=CIRCLE ( 'NONE', #23711, 47.49900000000003075 ) ;
#1887=EDGE_CURVE ( 'NONE', #6697, #28711, #25741, .T. ) ;
#1891=ORIENTED_EDGE ( 'NONE', *, *, #27121, .F. ) ;
#1893=CARTESIAN_POINT ( 'NONE',  ( 4.000000000000003553, 49.65209126885784485, -15.44894276735497840 ) ) ;
#1895=CIRCLE ( 'NONE', #19137, 52.00000000000000711 ) ;
#1911=CARTESIAN_POINT ( 'NONE',  ( 7.999999999999992895, 0.000000000000000000, 0.000000000000000000 ) ) ;
#1913=DIRECTION ( 'NONE',  ( 0.000000000000000000, 0.000000000000000000, 1.000000000000000000 ) ) ;
#1915=ORIENTED_EDGE ( 'NONE', *, *, #20368, .T. ) ;
#1921=ORIENTED_EDGE ( 'NONE', *, *, #32147, .T. ) ;
#1926=VERTEX_POINT ( 'NONE', #2503 ) ;
#1928=ORIENTED_EDGE ( 'NONE', *, *, #1210, .T. ) ;
#1931=AXIS2_PLACEMENT_3D ( 'NONE', #3409, #3050, #22460 ) ;
#1932=CIRCLE ( 'NONE', #6508, 20.00000000000000355 ) ;
#1935=VERTEX_POINT ( 'NONE', #26804 ) ;
#1938=ORIENTED_EDGE ( 'NONE', *, *, #26880, .F. ) ;
#1941=CARTESIAN_POINT ( 'NONE',  ( 0.000000000000000000, 47.00885577955422434, -6.806061952191799769 ) ) ;
#1952=CARTESIAN_POINT ( 'NONE',  ( 7.999999999999992895, -38.92705108641712286, -27.21837053747841395 ) ) ;
#1956=CARTESIAN_POINT ( 'NONE',  ( 0.000000000000000000, 19.44205635905542451, 43.33776004284616334 ) ) ;
#1958=ORIENTED_EDGE ( 'NONE', *, *, #17210, .T. ) ;
#1959=ORIENTED_EDGE ( 'NONE', *, *, #3260, .F. ) ;
#1964=EDGE_CURVE ( 'NONE', #30554, #5386, #23236, .T. ) ;
#1965=VERTEX_POINT ( 'NONE', #4843 ) ;
#1966=EDGE_LOOP ( 'NONE', ( #21280, #17394, #22966, #10202 ) ) ;
#1971=LINE ( 'NONE', #32208, #9850 ) ;
#1978=DIRECTION ( 'NONE',  ( -1.000000000000000000, -0.000000000000000000, -0.000000000000000000 ) ) ;
#1990=DIRECTION ( 'NONE',  ( 0.000000000000000000, 0.000000000000000000, 1.000000000000000000 ) ) ;
#1995=ADVANCED_FACE ( 'NONE', ( #15784 ), #2332, .T. ) ;
#2002=CARTESIAN_POINT ( 'NONE',  ( 7.999999999999992895, -17.08890430202781374, 43.76671000081938701 ) ) ;
#2006=CIRCLE ( 'NONE', #8296, 52.00000000000000711 ) ;
#2007=VECTOR ( 'NONE', #8781, 1000.000000000000000 ) ;
#2009=ADVANCED_FACE ( 'NONE', ( #10048 ), #13131, .T. ) ;
#2017=EDGE_LOOP ( 'NONE', ( #17165, #833, #1097, #12056 ) ) ;
#2022=VERTEX_POINT ( 'NONE', #24110 ) ;
#2027=EDGE_LOOP ( 'NONE', ( #13304, #13650, #27522, #7305 ) ) ;
#2033=EDGE_CURVE ( 'NONE', #8928, #4539, #21500, .T. ) ;
#2035=CARTESIAN_POINT ( 'NONE',  ( 0.000000000000000000, 3.840921266749832252, 47.34345070675172451 ) ) ;
#2039=DIRECTION ( 'NONE',  ( 0.000000000000000000, -6.938893903907226800E-15, 1.000000000000000000 ) ) ;
#2042=EDGE_CURVE ( 'NONE', #7369, #15707, #5996, .T. ) ;
#2043=ADVANCED_FACE ( 'NONE', ( #26631 ), #2680, .T. ) ;
#2044=VERTEX_POINT ( 'NONE', #34916 ) ;
#2046=CARTESIAN_POINT ( 'NONE',  ( 7.999999999999992895, 47.22458491092828581, -5.098390039073752433 ) ) ;
#2048=CARTESIAN_POINT ( 'NONE',  ( 7.999999999999992895, -47.49120266317495975, -0.8606222198180163430 ) ) ;
#2049=CIRCLE ( 'NONE', #23886, 20.00000000000000000 ) ;
#2056=EDGE_CURVE ( 'NONE', #20209, #34767, #10030, .T. ) ;
#2067=CYLINDRICAL_SURFACE ( 'NONE', #11799, 20.00000000000000355 ) ;
#2074=AXIS2_PLACEMENT_3D ( 'NONE', #14194, #22117, #32936 ) ;
#2090=EDGE_CURVE ( 'NONE', #3377, #6697, #2006, .T. ) ;
#2091=CARTESIAN_POINT ( 'NONE',  ( 0.000000000000000000, 0.000000000000000000, 0.000000000000000000 ) ) ;
#2093=DIRECTION ( 'NONE',  ( -1.000000000000000000, -0.000000000000000000, 0.000000000000000000 ) ) ;
#2094=VERTEX_POINT ( 'NONE', #6067 ) ;
#2095=CIRCLE ( 'NONE', #3323, 47.49900000000000944 ) ;
#2105=AXIS2_PLACEMENT_3D ( 'NONE', #31118, #28073, #6620 ) ;
#2117=VECTOR ( 'NONE', #31383, 1000.000000000000000 ) ;
#2120=EDGE_CURVE ( 'NONE', #21198, #7610, #10947, .T. ) ;
#2122=EDGE_LOOP ( 'NONE', ( #10353, #19149, #3304, #34630 ) ) ;
#2123=EDGE_LOOP ( 'NONE', ( #19667, #24283, #27688, #14747 ) ) ;
#2132=AXIS2_PLACEMENT_3D ( 'NONE', #26977, #16129, #35605 ) ;
#2134=DIRECTION ( 'NONE',  ( -1.000000000000000000, -0.000000000000000000, -0.000000000000000000 ) ) ;
#2139=CIRCLE ( 'NONE', #25120, 47.49900000000001654 ) ;
#2142=DIRECTION ( 'NONE',  ( -1.000000000000000000, -0.000000000000000000, -0.000000000000000000 ) ) ;
#2146=FACE_OUTER_BOUND ( 'NONE', #10993, .T. ) ;
#2147=ORIENTED_EDGE ( 'NONE', *, *, #19604, .F. ) ;
#2153=ORIENTED_EDGE ( 'NONE', *, *, #1887, .T. ) ;
#2156=CARTESIAN_POINT ( 'NONE',  ( 0.000000000000000000, 46.11014828289842882, -9.022736828080857308 ) ) ;
#2157=CARTESIAN_POINT ( 'NONE',  ( 0.000000000000000000, -11.90021268425521939, -45.45261810511225065 ) ) ;
#2159=AXIS2_PLACEMENT_3D ( 'NONE', #24105, #29857, #15780 ) ;
#2161=VECTOR ( 'NONE', #5248, 1000.000000000000000 ) ;
#2162=AXIS2_PLACEMENT_3D ( 'NONE', #34855, #34495, #26203 ) ;
#2163=CARTESIAN_POINT ( 'NONE',  ( 7.999999999999992895, 8.053585752061906078, 46.81126742072027014 ) ) ;
#2166=DIRECTION ( 'NONE',  ( -1.000000000000000000, 0.000000000000000000, 0.000000000000000000 ) ) ;
#2172=AXIS2_PLACEMENT_3D ( 'NONE', #9053, #6001, #11576 ) ;
#2173=LINE ( 'NONE', #21746, #32980 ) ;
#2175=VERTEX_POINT ( 'NONE', #654 ) ;
#2177=AXIS2_PLACEMENT_3D ( 'NONE', #3570, #14517, #25531 ) ;
#2180=CIRCLE ( 'NONE', #30327, 47.49900000000000944 ) ;
#2182=DIRECTION ( 'NONE',  ( -1.000000000000000000, 0.000000000000000000, 0.000000000000000000 ) ) ;
#2191=VERTEX_POINT ( 'NONE', #33599 ) ;
#2199=AXIS2_PLACEMENT_3D ( 'NONE', #33545, #14447, #424 ) ;
#2202=AXIS2_PLACEMENT_3D ( 'NONE', #2838, #30368, #33062 ) ;
#2207=AXIS2_PLACEMENT_3D ( 'NONE', #18684, #26994, #13309 ) ;
#2208=DIRECTION ( 'NONE',  ( -1.000000000000000000, 0.000000000000000000, -0.000000000000000000 ) ) ;
#2209=DIRECTION ( 'NONE',  ( -1.000000000000000000, 0.000000000000000000, 0.000000000000000000 ) ) ;
#2212=DIRECTION ( 'NONE',  ( -1.000000000000000000, -0.000000000000000000, -0.000000000000000000 ) ) ;
#2218=ADVANCED_FACE ( 'NONE', ( #30909 ), #6245, .T. ) ;
#2221=ORIENTED_EDGE ( 'NONE', *, *, #22660, .F. ) ;
#2224=CARTESIAN_POINT ( 'NONE',  ( -9.999999999999994671, 0.000000000000000000, 0.000000000000000000 ) ) ;
#2225=FACE_OUTER_BOUND ( 'NONE', #18607, .T. ) ;
#2228=EDGE_CURVE ( 'NONE', #14555, #32804, #26047, .T. ) ;
#2237=CARTESIAN_POINT ( 'NONE',  ( 7.999999999999992895, -0.2227391519113268437, -46.98410307550732057 ) ) ;
#2238=ORIENTED_EDGE ( 'NONE', *, *, #6902, .T. ) ;
#2244=DIRECTION ( 'NONE',  ( -1.000000000000000000, 0.000000000000000000, 0.000000000000000000 ) ) ;
#2259=EDGE_CURVE ( 'NONE', #6879, #19623, #19786, .T. ) ;
#2270=CARTESIAN_POINT ( 'NONE',  ( 7.999999999999992895, 36.34385289850631295, -29.77717097092039111 ) ) ;
#2278=ORIENTED_EDGE ( 'NONE', *, *, #26040, .F. ) ;
#2282=DIRECTION ( 'NONE',  ( -1.000000000000000000, 0.000000000000000000, 0.000000000000000000 ) ) ;
#2298=ORIENTED_EDGE ( 'NONE', *, *, #1210, .F. ) ;
#2304=VERTEX_POINT ( 'NONE', #7127 ) ;
#2308=AXIS2_PLACEMENT_3D ( 'NONE', #11711, #24881, #6143 ) ;
#2319=CARTESIAN_POINT ( 'NONE',  ( 7.999999999999992895, 17.08890430202814059, -43.76671000081924490 ) ) ;
#2327=ADVANCED_FACE ( 'NONE', ( #28384 ), #31441, .T. ) ;
#2328=ORIENTED_EDGE ( 'NONE', *, *, #10515, .T. ) ;
#2329=CIRCLE ( 'NONE', #5778, 20.00000000000000711 ) ;
#2332=CYLINDRICAL_SURFACE ( 'NONE', #35340, 52.00000000000000711 ) ;
#2334=ORIENTED_EDGE ( 'NONE', *, *, #3653, .T. ) ;
#2337=VECTOR ( 'NONE', #32741, 1000.000000000000000 ) ;
#2341=CARTESIAN_POINT ( 'NONE',  ( 7.999999999999992895, 0.000000000000000000, 0.000000000000000000 ) ) ;
#2343=ORIENTED_EDGE ( 'NONE', *, *, #14120, .F. ) ;
#2349=DIRECTION ( 'NONE',  ( 0.000000000000000000, 0.9822872507286891652, -0.1873813145857216034 ) ) ;
#2352=FACE_OUTER_BOUND ( 'NONE', #34563, .T. ) ;
#2362=FACE_OUTER_BOUND ( 'NONE', #12722, .T. ) ;
#2363=EDGE_LOOP ( 'NONE', ( #14878, #11766, #29319, #29549 ) ) ;
#2367=DIRECTION ( 'NONE',  ( -1.000000000000000000, 0.000000000000000000, 0.000000000000000000 ) ) ;
#2370=EDGE_CURVE ( 'NONE', #688, #26487, #25513, .T. ) ;
#2373=AXIS2_PLACEMENT_3D ( 'NONE', #30750, #22812, #9139 ) ;
#2376=CARTESIAN_POINT ( 'NONE',  ( 0.000000000000000000, 44.47301969247445186, 16.68249143361927267 ) ) ;
#2377=CARTESIAN_POINT ( 'NONE',  ( 7.999999999999992895, -40.47821179127737423, 32.64221760512746329 ) ) ;
#2379=ORIENTED_EDGE ( 'NONE', *, *, #3575, .F. ) ;
#2384=CIRCLE ( 'NONE', #29383, 47.49900000000002365 ) ;
#2386=EDGE_LOOP ( 'NONE', ( #30983, #31580, #18187, #1336 ) ) ;
#2387=ORIENTED_EDGE ( 'NONE', *, *, #33522, .F. ) ;
#2400=VERTEX_POINT ( 'NONE', #31264 ) ;
#2401=VECTOR ( 'NONE', #34422, 1000.000000000000000 ) ;
#2405=LINE ( 'NONE', #13372, #28354 ) ;
#2417=ORIENTED_EDGE ( 'NONE', *, *, #6, .F. ) ;
#2418=VERTEX_POINT ( 'NONE', #34686 ) ;
#2420=ADVANCED_FACE ( 'NONE', ( #12719 ), #15748, .T. ) ;
#2422=ORIENTED_EDGE ( 'NONE', *, *, #31724, .F. ) ;
#2427=AXIS2_PLACEMENT_3D ( 'NONE', #25707, #6783, #31624 ) ;
#2428=DIRECTION ( 'NONE',  ( 0.000000000000000000, -0.7705132427757949154, 0.6374239897486828621 ) ) ;
#2436=AXIS2_PLACEMENT_3D ( 'NONE', #26748, #31599, #6753 ) ;
#2437=CARTESIAN_POINT ( 'NONE',  ( 0.000000000000000000, 0.000000000000000000, 0.000000000000000000 ) ) ;
#2438=ORIENTED_EDGE ( 'NONE', *, *, #30780, .T. ) ;
#2441=CARTESIAN_POINT ( 'NONE',  ( 0.000000000000000000, 24.72041153920734047, 40.55929306992698002 ) ) ;
#2451=EDGE_CURVE ( 'NONE', #9311, #26508, #15764, .T. ) ;
#2458=FACE_OUTER_BOUND ( 'NONE', #27702, .T. ) ;
#2459=DIRECTION ( 'NONE',  ( -1.000000000000000000, -0.000000000000000000, 0.000000000000000000 ) ) ;
#2460=EDGE_LOOP ( 'NONE', ( #26962, #477, #20585, #28253 ) ) ;
#2469=DIRECTION ( 'NONE',  ( -1.000000000000000000, 0.000000000000000000, -0.000000000000000000 ) ) ;
#2487=CIRCLE ( 'NONE', #15659, 20.00000000000000355 ) ;
#2488=CARTESIAN_POINT ( 'NONE',  ( 7.999999999999992895, -24.72041153920704915, -40.55929306992714345 ) ) ;
#2490=CYLINDRICAL_SURFACE ( 'NONE', #936, 11.00000000000000000 ) ;
#2500=AXIS2_PLACEMENT_3D ( 'NONE', #4387, #17693, #18044 ) ;
#2503=CARTESIAN_POINT ( 'NONE',  ( 0.000000000000000000, -30.93515269692138503, 36.04401931830242489 ) ) ;
#2511=CARTESIAN_POINT ( 'NONE',  ( 7.999999999999992895, -45.78515115856034612, -12.64416602183715455 ) ) ;
#2512=ORIENTED_EDGE ( 'NONE', *, *, #15046, .T. ) ;
#2514=CIRCLE ( 'NONE', #23173, 20.00000000000000711 ) ;
#2516=CARTESIAN_POINT ( 'NONE',  ( 7.999999999999992895, 34.03046037009305280, -33.13733193845769165 ) ) ;
#2518=ORIENTED_EDGE ( 'NONE', *, *, #16282, .T. ) ;
#2526=AXIS2_PLACEMENT_3D ( 'NONE', #11105, #13623, #8039 ) ;
#2549=CARTESIAN_POINT ( 'NONE',  ( 7.999999999999992895, 36.06787431788733045, -37.45808914225451502 ) ) ;
#2553=AXIS2_PLACEMENT_3D ( 'NONE', #1831, #9562, #20530 ) ;
#2557=VERTEX_POINT ( 'NONE', #8359 ) ;
#2561=ORIENTED_EDGE ( 'NONE', *, *, #28176, .F. ) ;
#2567=ADVANCED_FACE ( 'NONE', ( #19515 ), #22569, .T. ) ;
#2570=DIRECTION ( 'NONE',  ( 1.000000000000000000, -0.000000000000000000, 0.000000000000000000 ) ) ;
#2575=CARTESIAN_POINT ( 'NONE',  ( 7.999999999999992895, 50.95304419620825342, 10.38206564895680017 ) ) ;
#2577=CIRCLE ( 'NONE', #22079, 52.00000000000000711 ) ;
#2583=EDGE_LOOP ( 'NONE', ( #34138, #24817, #3479, #17301 ) ) ;
#2598=ORIENTED_EDGE ( 'NONE', *, *, #28445, .F. ) ;
#2605=CARTESIAN_POINT ( 'NONE',  ( 0.000000000000000000, -49.65209126885775248, 15.44894276735533900 ) ) ;
#2618=DIRECTION ( 'NONE',  ( 1.000000000000000000, -0.000000000000000000, -0.000000000000000000 ) ) ;
#2621=DIRECTION ( 'NONE',  ( -1.000000000000000000, 0.000000000000000000, 0.000000000000000000 ) ) ;
#2622=ORIENTED_EDGE ( 'NONE', *, *, #16268, .T. ) ;
#2625=VECTOR ( 'NONE', #16350, 1000.000000000000000 ) ;
#2626=AXIS2_PLACEMENT_3D ( 'NONE', #1543, #3714, #11994 ) ;
#2630=CARTESIAN_POINT ( 'NONE',  ( 0.000000000000000000, -46.90537658765333617, 2.727856614654147638 ) ) ;
#2631=AXIS2_PLACEMENT_3D ( 'NONE', #9421, #6368, #23097 ) ;
#2635=CARTESIAN_POINT ( 'NONE',  ( 0.000000000000000000, -35.11945359308137427, 38.34871548466002622 ) ) ;
#2642=CIRCLE ( 'NONE', #10670, 52.00000000000000711 ) ;
#2643=ORIENTED_EDGE ( 'NONE', *, *, #33970, .T. ) ;
#2647=EDGE_LOOP ( 'NONE', ( #29100, #1130, #4213, #18407 ) ) ;
#2651=CARTESIAN_POINT ( 'NONE',  ( 7.999999999999992895, 46.87740477351712798, 3.172455868806031809 ) ) ;
#2653=EDGE_CURVE ( 'NONE', #17256, #16010, #11249, .T. ) ;
#2654=FACE_OUTER_BOUND ( 'NONE', #14905, .T. ) ;
#2675=VERTEX_POINT ( 'NONE', #27479 ) ;
#2676=VERTEX_POINT ( 'NONE', #2825 ) ;
#2679=AXIS2_PLACEMENT_3D ( 'NONE', #9068, #15159, #17327 ) ;
#2680=CYLINDRICAL_SURFACE ( 'NONE', #5442, 20.00000000000000711 ) ;
#2682=ORIENTED_EDGE ( 'NONE', *, *, #27285, .T. ) ;
#2684=EDGE_CURVE ( 'NONE', #19439, #23884, #32970, .T. ) ;
#2685=VECTOR ( 'NONE', #21530, 1000.000000000000000 ) ;
#2688=CYLINDRICAL_SURFACE ( 'NONE', #1619, 52.00000000000000711 ) ;
#2690=LINE ( 'NONE', #11643, #24823 ) ;
#2694=EDGE_CURVE ( 'NONE', #3168, #31652, #1932, .T. ) ;
#2697=EDGE_CURVE ( 'NONE', #8613, #11997, #33386, .T. ) ;
#2698=CARTESIAN_POINT ( 'NONE',  ( 7.999999999999992895, 0.000000000000000000, 0.000000000000000000 ) ) ;
#2714=DIRECTION ( 'NONE',  ( 0.000000000000000000, 0.000000000000000000, 1.000000000000000000 ) ) ;
#2715=CIRCLE ( 'NONE', #14726, 52.00000000000000711 ) ;
#2716=LINE ( 'NONE', #27886, #30807 ) ;
#2717=CARTESIAN_POINT ( 'NONE',  ( 7.999999999999992895, 47.00885577955422434, -6.806061952191799769 ) ) ;
#2719=CYLINDRICAL_SURFACE ( 'NONE', #32546, 20.00000000000000355 ) ;
#2727=DIRECTION ( 'NONE',  ( -1.000000000000000000, 0.000000000000000000, -0.000000000000000000 ) ) ;
#2731=EDGE_CURVE ( 'NONE', #5795, #2094, #27824, .T. ) ;
#2737=EDGE_CURVE ( 'NONE', #19471, #14555, #13967, .T. ) ;
#2743=CARTESIAN_POINT ( 'NONE',  ( 0.000000000000000000, -46.11014828289837197, -9.022736828081189486 ) ) ;
#2755=DIRECTION ( 'NONE',  ( -1.000000000000000000, 0.000000000000000000, -0.000000000000000000 ) ) ;
#2760=AXIS2_PLACEMENT_3D ( 'NONE', #29979, #21488, #19151 ) ;
#2761=CARTESIAN_POINT ( 'NONE',  ( 7.999999999999992895, 0.000000000000000000, 0.000000000000000000 ) ) ;
#2766=AXIS2_PLACEMENT_3D ( 'NONE', #23713, #32516, #7330 ) ;
#2768=VERTEX_POINT ( 'NONE', #20038 ) ;
#2769=AXIS2_PLACEMENT_3D ( 'NONE', #15840, #18731, #4557 ) ;
#2771=ORIENTED_EDGE ( 'NONE', *, *, #16151, .T. ) ;
#2775=AXIS2_PLACEMENT_3D ( 'NONE', #27205, #24322, #16184 ) ;
#2777=EDGE_CURVE ( 'NONE', #34614, #5335, #31042, .T. ) ;
#2779=EDGE_CURVE ( 'NONE', #9066, #22316, #7634, .T. ) ;
#2804=DIRECTION ( 'NONE',  ( 0.000000000000000000, -0.8443279255020087470, -0.5358267949790064266 ) ) ;
#2806=ORIENTED_EDGE ( 'NONE', *, *, #2856, .T. ) ;
#2824=CYLINDRICAL_SURFACE ( 'NONE', #17671, 20.00000000000000355 ) ;
#2825=CARTESIAN_POINT ( 'NONE',  ( 7.999999999999992895, 30.93515269692163372, -36.04401931830219752 ) ) ;
#2833=DIRECTION ( 'NONE',  ( -1.000000000000000000, 0.000000000000000000, -0.000000000000000000 ) ) ;
#2837=CARTESIAN_POINT ( 'NONE',  ( 7.999999999999992895, 0.000000000000000000, 0.000000000000000000 ) ) ;
#2838=CARTESIAN_POINT ( 'NONE',  ( 0.000000000000000000, 0.000000000000000000, 0.000000000000000000 ) ) ;
#2843=DIRECTION ( 'NONE',  ( 1.000000000000000000, 0.000000000000000000, 0.000000000000000000 ) ) ;
#2855=ORIENTED_EDGE ( 'NONE', *, *, #6898, .T. ) ;
#2856=EDGE_CURVE ( 'NONE', #1839, #25395, #10526, .T. ) ;
#2861=AXIS2_PLACEMENT_3D ( 'NONE', #7141, #18116, #29121 ) ;
#2863=VECTOR ( 'NONE', #27050, 1000.000000000000000 ) ;
#2864=CARTESIAN_POINT ( 'NONE',  ( 7.999999999999992895, -42.03146605346803000, 22.12489237027305577 ) ) ;
#2883=CARTESIAN_POINT ( 'NONE',  ( -9.999999999999994671, 0.000000000000000000, 0.000000000000000000 ) ) ;
#2887=EDGE_LOOP ( 'NONE', ( #26162, #35518, #4200, #22277 ) ) ;
#2888=DIRECTION ( 'NONE',  ( 0.000000000000000000, 0.000000000000000000, 1.000000000000000000 ) ) ;
#2890=AXIS2_PLACEMENT_3D ( 'NONE', #21151, #32145, #26941 ) ;
#2897=EDGE_CURVE ( 'NONE', #25998, #4505, #24923, .T. ) ;
#2898=DIRECTION ( 'NONE',  ( 0.000000000000000000, 0.000000000000000000, 1.000000000000000000 ) ) ;
#2904=DIRECTION ( 'NONE',  ( 0.000000000000000000, 0.000000000000000000, 1.000000000000000000 ) ) ;
#2905=DIRECTION ( 'NONE',  ( -1.000000000000000000, 0.000000000000000000, 0.000000000000000000 ) ) ;
#2906=EDGE_LOOP ( 'NONE', ( #24197, #13132, #7241, #3218 ) ) ;
#2910=EDGE_CURVE ( 'NONE', #7078, #26596, #21460, .T. ) ;
#2913=ORIENTED_EDGE ( 'NONE', *, *, #26815, .F. ) ;
#2916=DIRECTION ( 'NONE',  ( -1.000000000000000000, 0.000000000000000000, 0.000000000000000000 ) ) ;
#2923=LINE ( 'NONE', #16913, #6457 ) ;
#2929=ORIENTED_EDGE ( 'NONE', *, *, #9500, .T. ) ;
#2931=ORIENTED_EDGE ( 'NONE', *, *, #35217, .F. ) ;
#2939=VERTEX_POINT ( 'NONE', #29418 ) ;
#2945=AXIS2_PLACEMENT_3D ( 'NONE', #1471, #25798, #28671 ) ;
#2946=DIRECTION ( 'NONE',  ( -1.000000000000000000, 0.000000000000000000, 0.000000000000000000 ) ) ;
#2972=EDGE_CURVE ( 'NONE', #32704, #32451, #15526, .T. ) ;
#2983=LINE ( 'NONE', #32683, #25157 ) ;
#2987=FACE_OUTER_BOUND ( 'NONE', #6987, .T. ) ;
#2990=DIRECTION ( 'NONE',  ( 0.000000000000000000, 0.000000000000000000, 1.000000000000000000 ) ) ;
#2991=DIRECTION ( 'NONE',  ( -1.000000000000000000, 0.000000000000000000, 0.000000000000000000 ) ) ;
#3000=CARTESIAN_POINT ( 'NONE',  ( 4.000000000000003553, -0.6505223195679143977, -51.99593080916758936 ) ) ;
#3005=LINE ( 'NONE', #19693, #30450 ) ;
#3006=DIRECTION ( 'NONE',  ( 0.000000000000000000, 0.000000000000000000, 1.000000000000000000 ) ) ;
#3008=DIRECTION ( 'NONE',  ( -1.000000000000000000, -0.000000000000000000, 0.000000000000000000 ) ) ;
#3024=DIRECTION ( 'NONE',  ( 0.000000000000000000, 0.000000000000000000, -1.000000000000000000 ) ) ;
#3037=VERTEX_POINT ( 'NONE', #17856 ) ;
#3038=ORIENTED_EDGE ( 'NONE', *, *, #18067, .F. ) ;
#3040=LINE ( 'NONE', #668, #33918 ) ;
#3041=ORIENTED_EDGE ( 'NONE', *, *, #27315, .F. ) ;
#3050=DIRECTION ( 'NONE',  ( -1.000000000000000000, -0.000000000000000000, 0.000000000000000000 ) ) ;
#3052=CARTESIAN_POINT ( 'NONE',  ( 0.000000000000000000, -44.25018368420762016, 27.31155879685168131 ) ) ;
#3063=EDGE_CURVE ( 'NONE', #28711, #5428, #718, .T. ) ;
#3064=AXIS2_PLACEMENT_3D ( 'NONE', #22052, #14116, #16986 ) ;
#3072=ORIENTED_EDGE ( 'NONE', *, *, #16909, .F. ) ;
#3075=DIRECTION ( 'NONE',  ( -1.000000000000000000, -0.000000000000000000, -0.000000000000000000 ) ) ;
#3078=ORIENTED_EDGE ( 'NONE', *, *, #22725, .T. ) ;
#3082=LINE ( 'NONE', #11689, #19011 ) ;
#3083=ORIENTED_EDGE ( 'NONE', *, *, #14355, .T. ) ;
#3087=CARTESIAN_POINT ( 'NONE',  ( 7.999999999999992895, 5.667686777401707232, 46.64153600743606631 ) ) ;
#3088=ORIENTED_EDGE ( 'NONE', *, *, #10237, .F. ) ;
#3096=CARTESIAN_POINT ( 'NONE',  ( 0.000000000000000000, -36.34385289850609979, 29.77717097092063980 ) ) ;
#3104=EDGE_CURVE ( 'NONE', #28091, #14794, #34078, .T. ) ;
#3105=CARTESIAN_POINT ( 'NONE',  ( 50.00005079999998969, 10.58300524425836109, -3.000000000000002665 ) ) ;
#3116=CARTESIAN_POINT ( 'NONE',  ( 0.000000000000000000, -19.44205635905512608, -43.33776004284631256 ) ) ;
#3119=VERTEX_POINT ( 'NONE', #6703 ) ;
#3124=CARTESIAN_POINT ( 'NONE',  ( 0.000000000000000000, 35.11945359308111847, 38.34871548466026070 ) ) ;
#3135=ADVANCED_FACE ( 'NONE', ( #28683 ), #4570, .T. ) ;
#3137=EDGE_CURVE ( 'NONE', #34977, #23819, #3596, .T. ) ;
#3141=DIRECTION ( 'NONE',  ( -1.000000000000000000, 0.000000000000000000, 0.000000000000000000 ) ) ;
#3143=DIRECTION ( 'NONE',  ( -1.000000000000000000, -0.000000000000000000, -0.000000000000000000 ) ) ;
#3146=EDGE_CURVE ( 'NONE', #23782, #28075, #12829, .T. ) ;
#3148=ORIENTED_EDGE ( 'NONE', *, *, #13055, .F. ) ;
#3155=ORIENTED_EDGE ( 'NONE', *, *, #32670, .T. ) ;
#3160=CARTESIAN_POINT ( 'NONE',  ( 7.999999999999992895, -8.053585752062238257, 46.81126742072021329 ) ) ;
#3167=EDGE_LOOP ( 'NONE', ( #19715, #27036, #1388, #15787 ) ) ;
#3168=VERTEX_POINT ( 'NONE', #31558 ) ;
#3178=EDGE_CURVE ( 'NONE', #11728, #31611, #15857, .T. ) ;
#3191=DIRECTION ( 'NONE',  ( 0.000000000000000000, 0.000000000000000000, -1.000000000000000000 ) ) ;
#3192=VERTEX_POINT ( 'NONE', #2035 ) ;
#3199=ORIENTED_EDGE ( 'NONE', *, *, #28205, .T. ) ;
#3205=ADVANCED_FACE ( 'NONE', ( #21269 ), #5436, .T. ) ;
#3206=ADVANCED_FACE ( 'NONE', ( #10659 ), #18926, .T. ) ;
#3211=AXIS2_PLACEMENT_3D ( 'NONE', #31257, #6579, #17553 ) ;
#3214=ORIENTED_EDGE ( 'NONE', *, *, #10364, .T. ) ;
#3215=AXIS2_PLACEMENT_3D ( 'NONE', #31002, #5818, #33526 ) ;
#3217=CARTESIAN_POINT ( 'NONE',  ( 7.999999999999992895, 44.75336757549778355, 14.30704879393622520 ) ) ;
#3218=ORIENTED_EDGE ( 'NONE', *, *, #22731, .T. ) ;
#3220=AXIS2_PLACEMENT_3D ( 'NONE', #10228, #29315, #21192 ) ;
#3225=DIRECTION ( 'NONE',  ( 0.000000000000000000, 0.000000000000000000, 1.000000000000000000 ) ) ;
#3228=DIRECTION ( 'NONE',  ( -1.000000000000000000, -0.000000000000000000, -0.000000000000000000 ) ) ;
#3233=ORIENTED_EDGE ( 'NONE', *, *, #18323, .T. ) ;
#3234=DIRECTION ( 'NONE',  ( -1.000000000000000000, 0.000000000000000000, 0.000000000000000000 ) ) ;
#3235=ORIENTED_EDGE ( 'NONE', *, *, #28132, .T. ) ;
#3238=VECTOR ( 'NONE', #21287, 1000.000000000000000 ) ;
#3244=DIRECTION ( 'NONE',  ( -1.000000000000000000, -0.000000000000000000, -0.000000000000000000 ) ) ;
#3245=ORIENTED_EDGE ( 'NONE', *, *, #28445, .T. ) ;
#3249=ADVANCED_FACE ( 'NONE', ( #2225 ), #13537, .T. ) ;
#3252=ORIENTED_EDGE ( 'NONE', *, *, #32189, .T. ) ;
#3255=CIRCLE ( 'NONE', #25691, 20.00000000000001066 ) ;
#3256=ORIENTED_EDGE ( 'NONE', *, *, #18348, .F. ) ;
#3257=ORIENTED_EDGE ( 'NONE', *, *, #26825, .F. ) ;
#3260=EDGE_CURVE ( 'NONE', #32804, #20080, #14481, .T. ) ;
#3278=DIRECTION ( 'NONE',  ( 0.000000000000000000, 0.000000000000000000, 1.000000000000000000 ) ) ;
#3280=CIRCLE ( 'NONE', #23387, 47.49900000000001654 ) ;
#3284=ORIENTED_EDGE ( 'NONE', *, *, #22447, .T. ) ;
#3294=EDGE_CURVE ( 'NONE', #20209, #3876, #9339, .T. ) ;
#3304=ORIENTED_EDGE ( 'NONE', *, *, #18350, .F. ) ;
#3307=CARTESIAN_POINT ( 'NONE',  ( 0.000000000000000000, 0.000000000000000000, 0.000000000000000000 ) ) ;
#3321=CIRCLE ( 'NONE', #29206, 20.00000000000000711 ) ;
#3323=AXIS2_PLACEMENT_3D ( 'NONE', #8576, #33082, #6238 ) ;
#3336=FACE_OUTER_BOUND ( 'NONE', #30465, .T. ) ;
#3341=EDGE_CURVE ( 'NONE', #12939, #35590, #8755, .T. ) ;
#3345=ADVANCED_FACE ( 'NONE', ( #34795 ), #7764, .T. ) ;
#3352=ORIENTED_EDGE ( 'NONE', *, *, #26701, .T. ) ;
#3353=AXIS2_PLACEMENT_3D ( 'NONE', #24854, #11170, #14214 ) ;
#3361=CARTESIAN_POINT ( 'NONE',  ( 7.999999999999992895, 44.61570720899074161, 14.73072383765644489 ) ) ;
#3362=CARTESIAN_POINT ( 'NONE',  ( 0.000000000000000000, 0.000000000000000000, 0.000000000000000000 ) ) ;
#3372=DIRECTION ( 'NONE',  ( 0.000000000000000000, 0.000000000000000000, 1.000000000000000000 ) ) ;
#3374=EDGE_CURVE ( 'NONE', #23819, #19728, #2923, .T. ) ;
#3376=DIRECTION ( 'NONE',  ( -1.000000000000000000, -0.000000000000000000, -0.000000000000000000 ) ) ;
#3377=VERTEX_POINT ( 'NONE', #33151 ) ;
#3384=VERTEX_POINT ( 'NONE', #24 ) ;
#3390=ORIENTED_EDGE ( 'NONE', *, *, #9869, .F. ) ;
#3391=EDGE_CURVE ( 'NONE', #9669, #4180, #13942, .T. ) ;
#3395=EDGE_CURVE ( 'NONE', #28380, #3813, #30458, .T. ) ;
#3409=CARTESIAN_POINT ( 'NONE',  ( 7.999999999999992895, 0.000000000000000000, 0.000000000000000000 ) ) ;
#3420=VECTOR ( 'NONE', #8550, 1000.000000000000000 ) ;
#3422=CARTESIAN_POINT ( 'NONE',  ( 7.999999999999992895, -19.44205635905572649, 43.33776004284603545 ) ) ;
#3425=AXIS2_PLACEMENT_3D ( 'NONE', #34075, #25976, #23806 ) ;
#3434=ORIENTED_EDGE ( 'NONE', *, *, #31199, .T. ) ;
#3435=FACE_OUTER_BOUND ( 'NONE', #10788, .T. ) ;
#3439=ORIENTED_EDGE ( 'NONE', *, *, #24763, .F. ) ;
#3442=DIRECTION ( 'NONE',  ( 0.000000000000000000, -0.9048270524660145808, -0.4257792915650830956 ) ) ;
#3443=ORIENTED_EDGE ( 'NONE', *, *, #9526, .T. ) ;
#3453=CARTESIAN_POINT ( 'NONE',  ( 0.000000000000000000, -46.21320724403641833, -10.97699764142004497 ) ) ;
#3457=ORIENTED_EDGE ( 'NONE', *, *, #27350, .F. ) ;
#3469=AXIS2_PLACEMENT_3D ( 'NONE', #2651, #24608, #10024 ) ;
#3472=ORIENTED_EDGE ( 'NONE', *, *, #8151, .T. ) ;
#3473=ORIENTED_EDGE ( 'NONE', *, *, #18559, .T. ) ;
#3479=ORIENTED_EDGE ( 'NONE', *, *, #27615, .F. ) ;
#3493=CIRCLE ( 'NONE', #6353, 20.00000000000000355 ) ;
#3495=EDGE_CURVE ( 'NONE', #23884, #3935, #16828, .T. ) ;
#3496=EDGE_CURVE ( 'NONE', #16062, #16883, #15098, .T. ) ;
#3497=CIRCLE ( 'NONE', #26476, 20.00000000000000711 ) ;
#3498=CARTESIAN_POINT ( 'NONE',  ( 0.000000000000000000, 0.000000000000000000, 0.000000000000000000 ) ) ;
#3505=CARTESIAN_POINT ( 'NONE',  ( 7.999999999999992895, 34.03046037009256963, 33.13733193845818903 ) ) ;
#3509=ORIENTED_EDGE ( 'NONE', *, *, #30780, .F. ) ;
#3518=ORIENTED_EDGE ( 'NONE', *, *, #24631, .F. ) ;
#3531=LINE ( 'NONE', #16833, #27771 ) ;
#3533=EDGE_CURVE ( 'NONE', #4435, #4367, #11536, .T. ) ;
#3537=FACE_OUTER_BOUND ( 'NONE', #11543, .T. ) ;
#3541=DIRECTION ( 'NONE',  ( 0.000000000000000000, 0.000000000000000000, 1.000000000000000000 ) ) ;
#3543=DIRECTION ( 'NONE',  ( 0.000000000000000000, 0.000000000000000000, -1.000000000000000000 ) ) ;
#3545=EDGE_CURVE ( 'NONE', #29395, #5751, #22003, .T. ) ;
#3546=AXIS2_PLACEMENT_3D ( 'NONE', #17473, #14776, #14245 ) ;
#3548=CARTESIAN_POINT ( 'NONE',  ( 7.999999999999992895, -46.21320724403657465, 10.97699764141937884 ) ) ;
#3551=ORIENTED_EDGE ( 'NONE', *, *, #3545, .T. ) ;
#3554=DIRECTION ( 'NONE',  ( 0.000000000000000000, 0.000000000000000000, 1.000000000000000000 ) ) ;
#3557=ORIENTED_EDGE ( 'NONE', *, *, #19002, .F. ) ;
#3561=EDGE_CURVE ( 'NONE', #11684, #32704, #13965, .T. ) ;
#3567=AXIS2_PLACEMENT_3D ( 'NONE', #4199, #29393, #4737 ) ;
#3568=ORIENTED_EDGE ( 'NONE', *, *, #27997, .T. ) ;
#3570=CARTESIAN_POINT ( 'NONE',  ( 0.000000000000000000, 0.000000000000000000, 0.000000000000000000 ) ) ;
#3575=EDGE_CURVE ( 'NONE', #26508, #27200, #28452, .T. ) ;
#3576=CYLINDRICAL_SURFACE ( 'NONE', #24372, 52.00000000000000711 ) ;
#3577=CARTESIAN_POINT ( 'NONE',  ( 0.000000000000000000, 19.74581912682909390, -48.10512059033372623 ) ) ;
#3578=EDGE_CURVE ( 'NONE', #22879, #18391, #1320, .T. ) ;
#3581=CARTESIAN_POINT ( 'NONE',  ( 0.000000000000000000, 2.123073309835184830, 47.45152853935336168 ) ) ;
#3585=ORIENTED_EDGE ( 'NONE', *, *, #10165, .F. ) ;
#3588=AXIS2_PLACEMENT_3D ( 'NONE', #7853, #3008, #24428 ) ;
#3593=ORIENTED_EDGE ( 'NONE', *, *, #21723, .T. ) ;
#3596=CIRCLE ( 'NONE', #11073, 47.49900000000001654 ) ;
#3601=CARTESIAN_POINT ( 'NONE',  ( 0.000000000000000000, -45.78515115856034612, -12.64416602183715455 ) ) ;
#3603=ORIENTED_EDGE ( 'NONE', *, *, #24762, .T. ) ;
#3607=CARTESIAN_POINT ( 'NONE',  ( 0.000000000000000000, 39.64889472655781333, -33.64468972902464827 ) ) ;
#3608=ORIENTED_EDGE ( 'NONE', *, *, #35235, .T. ) ;
#3613=ADVANCED_FACE ( 'NONE', ( #9361 ), #28986, .T. ) ;
#3614=CARTESIAN_POINT ( 'NONE',  ( 7.999999999999992895, 43.55304910509406824, 28.41006711800001128 ) ) ;
#3630=VERTEX_POINT ( 'NONE', #4334 ) ;
#3632=EDGE_LOOP ( 'NONE', ( #32776, #34412, #11398, #18008 ) ) ;
#3634=CARTESIAN_POINT ( 'NONE',  ( 7.999999999999992895, -9.744342220503712682, 46.48873837489796301 ) ) ;
#3635=ORIENTED_EDGE ( 'NONE', *, *, #26640, .F. ) ;
#3653=EDGE_CURVE ( 'NONE', #9489, #6860, #8784, .T. ) ;
#3663=AXIS2_PLACEMENT_3D ( 'NONE', #8420, #144, #20088 ) ;
#3666=CARTESIAN_POINT ( 'NONE',  ( 0.000000000000000000, 39.55064067543098361, -25.36340625197317067 ) ) ;
#3671=DIRECTION ( 'NONE',  ( 0.000000000000000000, 0.000000000000000000, 1.000000000000000000 ) ) ;
#3672=AXIS2_PLACEMENT_3D ( 'NONE', #8094, #27206, #7922 ) ;
#3673=CIRCLE ( 'NONE', #19720, 20.00000000000000355 ) ;
#3678=CARTESIAN_POINT ( 'NONE',  ( 4.000000000000003553, -5.871425383721907920, 51.66745943012281117 ) ) ;
#3681=DIRECTION ( 'NONE',  ( -1.000000000000000000, 0.000000000000000000, 0.000000000000000000 ) ) ;
#3688=DIRECTION ( 'NONE',  ( -1.000000000000000000, -0.000000000000000000, 0.000000000000000000 ) ) ;
#3689=ORIENTED_EDGE ( 'NONE', *, *, #33057, .F. ) ;
#3690=ORIENTED_EDGE ( 'NONE', *, *, #4198, .T. ) ;
#3695=DIRECTION ( 'NONE',  ( 1.000000000000000000, 0.000000000000000000, -0.000000000000000000 ) ) ;
#3696=CIRCLE ( 'NONE', #29001, 20.00000000000000711 ) ;
#3706=DIRECTION ( 'NONE',  ( 0.000000000000000000, 0.000000000000000000, 1.000000000000000000 ) ) ;
#3714=DIRECTION ( 'NONE',  ( -1.000000000000000000, -0.000000000000000000, -0.000000000000000000 ) ) ;
#3717=DIRECTION ( 'NONE',  ( 0.000000000000000000, 0.000000000000000000, 1.000000000000000000 ) ) ;
#3718=FACE_OUTER_BOUND ( 'NONE', #10049, .T. ) ;
#3721=CARTESIAN_POINT ( 'NONE',  ( 7.999999999999992895, 32.32520163883582853, 34.09746168776048592 ) ) ;
#3723=AXIS2_PLACEMENT_3D ( 'NONE', #20648, #31650, #28079 ) ;
#3737=ORIENTED_EDGE ( 'NONE', *, *, #27615, .T. ) ;
#3738=EDGE_LOOP ( 'NONE', ( #28761, #23199, #32340, #21052 ) ) ;
#3752=CARTESIAN_POINT ( 'NONE',  ( 7.999999999999992895, -12.30077720129132679, 50.52416135122078344 ) ) ;
#3757=AXIS2_PLACEMENT_3D ( 'NONE', #8825, #204, #16919 ) ;
#3764=DIRECTION ( 'NONE',  ( 1.000000000000000000, -0.000000000000000000, 0.000000000000000000 ) ) ;
#3765=EDGE_CURVE ( 'NONE', #13043, #27252, #27782, .T. ) ;
#3768=ORIENTED_EDGE ( 'NONE', *, *, #23274, .F. ) ;
#3774=ORIENTED_EDGE ( 'NONE', *, *, #4198, .F. ) ;
#3775=ORIENTED_EDGE ( 'NONE', *, *, #23135, .F. ) ;
#3780=EDGE_LOOP ( 'NONE', ( #15499, #57, #17915, #25124 ) ) ;
#3781=EDGE_CURVE ( 'NONE', #32945, #28711, #749, .T. ) ;
#3785=AXIS2_PLACEMENT_3D ( 'NONE', #19970, #14762, #31156 ) ;
#3786=ORIENTED_EDGE ( 'NONE', *, *, #2897, .T. ) ;
#3795=CIRCLE ( 'NONE', #27367, 11.00000000000000000 ) ;
#3799=DIRECTION ( 'NONE',  ( -1.000000000000000000, 0.000000000000000000, 0.000000000000000000 ) ) ;
#3800=AXIS2_PLACEMENT_3D ( 'NONE', #19314, #11409, #11751 ) ;
#3803=ORIENTED_EDGE ( 'NONE', *, *, #4651, .T. ) ;
#3810=DIRECTION ( 'NONE',  ( -1.000000000000000000, -0.000000000000000000, 0.000000000000000000 ) ) ;
#3811=AXIS2_PLACEMENT_3D ( 'NONE', #13598, #24592, #35584 ) ;
#3813=VERTEX_POINT ( 'NONE', #29882 ) ;
#3827=EDGE_CURVE ( 'NONE', #32451, #22834, #32371, .T. ) ;
#3830=AXIS2_PLACEMENT_3D ( 'NONE', #7768, #13015, #35515 ) ;
#3831=CIRCLE ( 'NONE', #29114, 20.00000000000001066 ) ;
#3833=DIRECTION ( 'NONE',  ( -1.000000000000000000, 0.000000000000000000, -0.000000000000000000 ) ) ;
#3838=ORIENTED_EDGE ( 'NONE', *, *, #25536, .T. ) ;
#3839=ORIENTED_EDGE ( 'NONE', *, *, #5999, .F. ) ;
#3842=CIRCLE ( 'NONE', #18751, 20.00000000000000711 ) ;
#3849=UNCERTAINTY_MEASURE_WITH_UNIT (LENGTH_MEASURE( 1.000000000000000082E-05 ), #12860, 'distance_accuracy_value', 'NONE');
#3854=DIRECTION ( 'NONE',  ( 0.000000000000000000, 0.9980267284282717810, -0.06279051952930990443 ) ) ;
#3855=LINE ( 'NONE', #26160, #10555 ) ;
#3858=ORIENTED_EDGE ( 'NONE', *, *, #26022, .F. ) ;
#3865=CIRCLE ( 'NONE', #4425, 20.00000000000000355 ) ;
#3876=VERTEX_POINT ( 'NONE', #21755 ) ;
#3878=ORIENTED_EDGE ( 'NONE', *, *, #2056, .F. ) ;
#3883=CARTESIAN_POINT ( 'NONE',  ( 0.000000000000000000, 0.000000000000000000, 0.000000000000000000 ) ) ;
#3884=AXIS2_PLACEMENT_3D ( 'NONE', #35496, #35323, #34973 ) ;
#3903=EDGE_CURVE ( 'NONE', #30827, #35186, #19059, .T. ) ;
#3907=ORIENTED_EDGE ( 'NONE', *, *, #29480, .F. ) ;
#3914=ORIENTED_EDGE ( 'NONE', *, *, #24499, .T. ) ;
#3918=CARTESIAN_POINT ( 'NONE',  ( 7.999999999999992895, 11.46872990052381880, 45.56340405422447049 ) ) ;
#3919=ORIENTED_EDGE ( 'NONE', *, *, #2451, .T. ) ;
#3924=CARTESIAN_POINT ( 'NONE',  ( 7.999999999999992895, 51.93417535146742381, 2.615612846549361770 ) ) ;
#3925=CARTESIAN_POINT ( 'NONE',  ( 0.000000000000000000, 0.000000000000000000, 0.000000000000000000 ) ) ;
#3926=DIRECTION ( 'NONE',  ( 0.000000000000000000, 0.5877852522924742473, -0.8090169943749466741 ) ) ;
#3930=ORIENTED_EDGE ( 'NONE', *, *, #18025, .T. ) ;
#3935=VERTEX_POINT ( 'NONE', #10073 ) ;
#3940=AXIS2_PLACEMENT_3D ( 'NONE', #13568, #29787, #60 ) ;
#3946=DIRECTION ( 'NONE',  ( -1.000000000000000000, 0.000000000000000000, 0.000000000000000000 ) ) ;
#3948=AXIS2_PLACEMENT_3D ( 'NONE', #11696, #33656, #8990 ) ;
#3954=EDGE_CURVE ( 'NONE', #33383, #23477, #23189, .T. ) ;
#3955=DIRECTION ( 'NONE',  ( 0.000000000000000000, -0.1253332335643113082, 0.9921147013144768767 ) ) ;
#3961=ORIENTED_EDGE ( 'NONE', *, *, #1805, .T. ) ;
#3967=ORIENTED_EDGE ( 'NONE', *, *, #7911, .F. ) ;
#3970=LINE ( 'NONE', #17432, #19410 ) ;
#3983=DIRECTION ( 'NONE',  ( -1.000000000000000000, 0.000000000000000000, 0.000000000000000000 ) ) ;
#3986=AXIS2_PLACEMENT_3D ( 'NONE', #14226, #27918, #9179 ) ;
#4000=ORIENTED_EDGE ( 'NONE', *, *, #7661, .T. ) ;
#4009=EDGE_CURVE ( 'NONE', #2675, #28676, #774, .T. ) ;
#4013=ORIENTED_EDGE ( 'NONE', *, *, #27941, .F. ) ;
#4023=ORIENTED_EDGE ( 'NONE', *, *, #27764, .F. ) ;
#4024=ORIENTED_EDGE ( 'NONE', *, *, #74, .F. ) ;
#4026=EDGE_CURVE ( 'NONE', #29368, #30768, #4813, .T. ) ;
#4029=DIRECTION ( 'NONE',  ( 0.000000000000000000, 0.000000000000000000, 1.000000000000000000 ) ) ;
#4041=AXIS2_PLACEMENT_3D ( 'NONE', #12019, #1576, #6789 ) ;
#4048=AXIS2_PLACEMENT_3D ( 'NONE', #13665, #5221, #32392 ) ;
#4051=EDGE_CURVE ( 'NONE', #33849, #2400, #5948, .T. ) ;
#4057=ORIENTED_EDGE ( 'NONE', *, *, #3575, .T. ) ;
#4059=VERTEX_POINT ( 'NONE', #33622 ) ;
#4060=( LENGTH_UNIT ( ) NAMED_UNIT ( * ) SI_UNIT ( .MILLI., .METRE. ) );
#4061=VERTEX_POINT ( 'NONE', #8955 ) ;
#4068=AXIS2_PLACEMENT_3D ( 'NONE', #11325, #33289, #8606 ) ;
#4071=EDGE_CURVE ( 'NONE', #11477, #29543, #3673, .T. ) ;
#4074=DIRECTION ( 'NONE',  ( 1.000000000000000000, -0.000000000000000000, -0.000000000000000000 ) ) ;
#4084=EDGE_CURVE ( 'NONE', #29056, #20040, #34118, .T. ) ;
#4091=VERTEX_POINT ( 'NONE', #26072 ) ;
#4094=LINE ( 'NONE', #22599, #19795 ) ;
#4098=CARTESIAN_POINT ( 'NONE',  ( 4.000000000000003553, -40.47821179127691238, -32.64221760512803172 ) ) ;
#4101=VERTEX_POINT ( 'NONE', #3577 ) ;
#4102=AXIS2_PLACEMENT_3D ( 'NONE', #29592, #17872, #13027 ) ;
#4109=VERTEX_POINT ( 'NONE', #31470 ) ;
#4114=VERTEX_POINT ( 'NONE', #34175 ) ;
#4125=DIRECTION ( 'NONE',  ( -1.000000000000000000, 0.000000000000000000, 0.000000000000000000 ) ) ;
#4127=DIRECTION ( 'NONE',  ( 0.000000000000000000, 0.000000000000000000, 1.000000000000000000 ) ) ;
#4132=PLANE ( 'NONE',  #16368 ) ;
#4134=ORIENTED_EDGE ( 'NONE', *, *, #30362, .T. ) ;
#4138=VERTEX_POINT ( 'NONE', #17231 ) ;
#4139=ORIENTED_EDGE ( 'NONE', *, *, #11974, .F. ) ;
#4141=DIRECTION ( 'NONE',  ( -1.000000000000000000, -0.000000000000000000, 0.000000000000000000 ) ) ;
#4143=VECTOR ( 'NONE', #7228, 1000.000000000000000 ) ;
#4144=CIRCLE ( 'NONE', #34024, 20.00000000000001066 ) ;
#4148=EDGE_LOOP ( 'NONE', ( #3038, #28387, #26592, #11205 ) ) ;
#4152=CARTESIAN_POINT ( 'NONE',  ( 7.999999999999992895, 0.000000000000000000, 0.000000000000000000 ) ) ;
#4159=DIRECTION ( 'NONE',  ( -1.000000000000000000, 0.000000000000000000, 0.000000000000000000 ) ) ;
#4162=DIRECTION ( 'NONE',  ( 1.000000000000000000, 0.000000000000000000, -0.000000000000000000 ) ) ;
#4170=EDGE_LOOP ( 'NONE', ( #11152, #15433, #25560, #1166 ) ) ;
#4172=AXIS2_PLACEMENT_3D ( 'NONE', #35236, #18650, #16115 ) ;
#4173=CARTESIAN_POINT ( 'NONE',  ( 7.999999999999992895, 0.000000000000000000, 0.000000000000000000 ) ) ;
#4180=VERTEX_POINT ( 'NONE', #26245 ) ;
#4186=ORIENTED_EDGE ( 'NONE', *, *, #27677, .T. ) ;
#4197=AXIS2_PLACEMENT_3D ( 'NONE', #4744, #4912, #13362 ) ;
#4198=EDGE_CURVE ( 'NONE', #1742, #29371, #15235, .T. ) ;
#4199=CARTESIAN_POINT ( 'NONE',  ( 0.000000000000000000, -39.55064067543046491, -25.36340625197400200 ) ) ;
#4200=ORIENTED_EDGE ( 'NONE', *, *, #30836, .T. ) ;
#4211=AXIS2_PLACEMENT_3D ( 'NONE', #20845, #28800, #12952 ) ;
#4213=ORIENTED_EDGE ( 'NONE', *, *, #26015, .F. ) ;
#4219=AXIS2_PLACEMENT_3D ( 'NONE', #29701, #27009, #15634 ) ;
#4225=EDGE_CURVE ( 'NONE', #11477, #19439, #7096, .T. ) ;
#4226=ORIENTED_EDGE ( 'NONE', *, *, #7057, .F. ) ;
#4227=DIRECTION ( 'NONE',  ( -1.000000000000000000, -0.000000000000000000, 0.000000000000000000 ) ) ;
#4237=ADVANCED_FACE ( 'NONE', ( #22415 ), #27501, .T. ) ;
#4244=AXIS2_PLACEMENT_3D ( 'NONE', #17585, #20457, #6796 ) ;
#4246=EDGE_CURVE ( 'NONE', #20080, #7610, #9387, .T. ) ;
#4250=VERTEX_POINT ( 'NONE', #25140 ) ;
#4256=VECTOR ( 'NONE', #16966, 1000.000000000000000 ) ;
#4257=CARTESIAN_POINT ( 'NONE',  ( 7.999999999999992895, 30.03615769709793426, -42.44795908868959344 ) ) ;
#4261=ORIENTED_EDGE ( 'NONE', *, *, #7748, .T. ) ;
#4266=ORIENTED_EDGE ( 'NONE', *, *, #13822, .F. ) ;
#4270=CIRCLE ( 'NONE', #19766, 52.00000000000000711 ) ;
#4273=ORIENTED_EDGE ( 'NONE', *, *, #14515, .F. ) ;
#4277=ORIENTED_EDGE ( 'NONE', *, *, #33464, .T. ) ;
#4278=DIRECTION ( 'NONE',  ( 0.000000000000000000, 0.7705132427757861446, 0.6374239897486934092 ) ) ;
#4279=DIRECTION ( 'NONE',  ( -1.000000000000000000, -0.000000000000000000, -0.000000000000000000 ) ) ;
#4282=CARTESIAN_POINT ( 'NONE',  ( 0.000000000000000000, -43.55304910509426009, 28.41006711799970574 ) ) ;
#4286=FACE_OUTER_BOUND ( 'NONE', #6788, .T. ) ;
#4298=LINE ( 'NONE', #1764, #28211 ) ;
#4299=CARTESIAN_POINT ( 'NONE',  ( 7.999999999999992895, -13.56094713063606072, 50.20060470671736397 ) ) ;
#4300=FACE_OUTER_BOUND ( 'NONE', #28429, .T. ) ;
#4307=EDGE_CURVE ( 'NONE', #403, #27203, #31234, .T. ) ;
#4314=ORIENTED_EDGE ( 'NONE', *, *, #836, .F. ) ;
#4321=VECTOR ( 'NONE', #17740, 1000.000000000000000 ) ;
#4328=VERTEX_POINT ( 'NONE', #33408 ) ;
#4330=VECTOR ( 'NONE', #33498, 1000.000000000000000 ) ;
#4334=CARTESIAN_POINT ( 'NONE',  ( 7.999999999999992895, 14.30000000000000071, -3.000000000000002665 ) ) ;
#4338=LINE ( 'NONE', #20860, #21638 ) ;
#4361=EDGE_LOOP ( 'NONE', ( #2387, #8402, #29708, #703 ) ) ;
#4365=DIRECTION ( 'NONE',  ( 0.000000000000000000, -6.938893903907226011E-15, 1.000000000000000000 ) ) ;
#4367=VERTEX_POINT ( 'NONE', #16660 ) ;
#4375=CYLINDRICAL_SURFACE ( 'NONE', #15466, 47.49900000000001654 ) ;
#4376=CIRCLE ( 'NONE', #3800, 52.00000000000000711 ) ;
#4377=AXIS2_PLACEMENT_3D ( 'NONE', #21496, #27112, #35390 ) ;
#4387=CARTESIAN_POINT ( 'NONE',  ( 7.999999999999992895, -22.43957647427188817, 41.27978878573619426 ) ) ;
#4394=ADVANCED_FACE ( 'NONE', ( #34306 ), #14849, .T. ) ;
#4398=AXIS2_PLACEMENT_3D ( 'NONE', #32622, #21272, #34800 ) ;
#4402=CARTESIAN_POINT ( 'NONE',  ( 0.000000000000000000, 0.000000000000000000, 0.000000000000000000 ) ) ;
#4410=( NAMED_UNIT ( * ) PLANE_ANGLE_UNIT ( ) SI_UNIT ( $, .RADIAN. ) );
#4417=CARTESIAN_POINT ( 'NONE',  ( 0.000000000000000000, 24.47917365149946534, 45.87777302070943364 ) ) ;
#4425=AXIS2_PLACEMENT_3D ( 'NONE', #22957, #33955, #814 ) ;
#4427=ORIENTED_EDGE ( 'NONE', *, *, #32912, .T. ) ;
#4435=VERTEX_POINT ( 'NONE', #26025 ) ;
#4436=LINE ( 'NONE', #15194, #23992 ) ;
#4443=EDGE_CURVE ( 'NONE', #13336, #3876, #31242, .T. ) ;
#4445=DIRECTION ( 'NONE',  ( 0.000000000000000000, 0.9980267284282717810, -0.06279051952930989056 ) ) ;
#4455=ORIENTED_EDGE ( 'NONE', *, *, #26584, .F. ) ;
#4459=EDGE_LOOP ( 'NONE', ( #1431, #12773, #21732, #14037 ) ) ;
#4461=LINE ( 'NONE', #31619, #1073 ) ;
#4462=CARTESIAN_POINT ( 'NONE',  ( 7.999999999999992895, 41.20225022064671805, -23.63323037071357646 ) ) ;
#4464=VECTOR ( 'NONE', #21064, 1000.000000000000000 ) ;
#4474=FACE_OUTER_BOUND ( 'NONE', #13684, .T. ) ;
#4478=EDGE_CURVE ( 'NONE', #21589, #22983, #28898, .T. ) ;
#4488=DIRECTION ( 'NONE',  ( -1.000000000000000000, 0.000000000000000000, 0.000000000000000000 ) ) ;
#4490=LINE ( 'NONE', #26618, #18172 ) ;
#4495=ADVANCED_FACE ( 'NONE', ( #22770 ), #33771, .T. ) ;
#4500=ORIENTED_EDGE ( 'NONE', *, *, #35245, .F. ) ;
#4505=VERTEX_POINT ( 'NONE', #9099 ) ;
#4509=CYLINDRICAL_SURFACE ( 'NONE', #26341, 20.00000000000000355 ) ;
#4512=AXIS2_PLACEMENT_3D ( 'NONE', #6289, #4141, #26095 ) ;
#4523=EDGE_CURVE ( 'NONE', #33987, #15078, #15021, .T. ) ;
#4533=CYLINDRICAL_SURFACE ( 'NONE', #25429, 47.49900000000001654 ) ;
#4536=DIRECTION ( 'NONE',  ( 0.000000000000000000, 0.000000000000000000, 1.000000000000000000 ) ) ;
#4539=VERTEX_POINT ( 'NONE', #32307 ) ;
#4542=AXIS2_PLACEMENT_3D ( 'NONE', #24522, #16204, #26878 ) ;
#4555=ORIENTED_EDGE ( 'NONE', *, *, #29947, .F. ) ;
#4557=DIRECTION ( 'NONE',  ( 0.000000000000000000, 0.5877852522924742473, -0.8090169943749466741 ) ) ;
#4564=CYLINDRICAL_SURFACE ( 'NONE', #31139, 47.49900000000001654 ) ;
#4570=CYLINDRICAL_SURFACE ( 'NONE', #32914, 52.00000000000000711 ) ;
#4576=CARTESIAN_POINT ( 'NONE',  ( 0.000000000000000000, -50.95304419620832448, 10.38206564895643957 ) ) ;
#4607=CARTESIAN_POINT ( 'NONE',  ( 4.000000000000003553, 49.25004636492388954, 16.68630974939777545 ) ) ;
#4609=CARTESIAN_POINT ( 'NONE',  ( 7.999999999999992895, 0.000000000000000000, 0.000000000000000000 ) ) ;
#4610=VERTEX_POINT ( 'NONE', #7810 ) ;
#4612=CIRCLE ( 'NONE', #17808, 52.00000000000000711 ) ;
#4613=PRODUCT_DEFINITION_FORMATION_WITH_SPECIFIED_SOURCE ( 'ANY', '', #8910, .NOT_KNOWN. ) ;
#4618=CARTESIAN_POINT ( 'NONE',  ( 7.999999999999992895, -30.93515269692138503, 36.04401931830242489 ) ) ;
#4622=FACE_OUTER_BOUND ( 'NONE', #29568, .T. ) ;
#4644=FACE_OUTER_BOUND ( 'NONE', #7398, .T. ) ;
#4651=EDGE_CURVE ( 'NONE', #1430, #25395, #20770, .T. ) ;
#4654=CYLINDRICAL_SURFACE ( 'NONE', #28619, 20.00000000000000711 ) ;
#4662=ADVANCED_FACE ( 'NONE', ( #21138 ), #12698, .T. ) ;
#4664=DIRECTION ( 'NONE',  ( 0.000000000000000000, 0.5877852522924686962, 0.8090169943749506709 ) ) ;
#4667=CARTESIAN_POINT ( 'NONE',  ( 7.999999999999992895, 0.000000000000000000, 0.000000000000000000 ) ) ;
#4668=EDGE_LOOP ( 'NONE', ( #21258, #7130, #25073, #22230 ) ) ;
#4671=VECTOR ( 'NONE', #3833, 1000.000000000000000 ) ;
#4672=DIRECTION ( 'NONE',  ( 0.000000000000000000, 0.000000000000000000, 1.000000000000000000 ) ) ;
#4677=DIRECTION ( 'NONE',  ( 0.000000000000000000, 0.000000000000000000, 1.000000000000000000 ) ) ;
#4682=DIRECTION ( 'NONE',  ( 0.000000000000000000, 0.000000000000000000, 1.000000000000000000 ) ) ;
#4685=CARTESIAN_POINT ( 'NONE',  ( 7.999999999999992895, -27.43636312076347394, 38.14186064215141414 ) ) ;
#4686=ORIENTED_EDGE ( 'NONE', *, *, #31450, .T. ) ;
#4687=ORIENTED_EDGE ( 'NONE', *, *, #9702, .F. ) ;
#4689=ADVANCED_FACE ( 'NONE', ( #34665 ), #15546, .T. ) ;
#4691=EDGE_CURVE ( 'NONE', #9, #23286, #20311, .T. ) ;
#4705=ADVANCED_FACE ( 'NONE', ( #21853 ), #8338, .T. ) ;
#4708=VERTEX_POINT ( 'NONE', #13579 ) ;
#4709=DIRECTION ( 'NONE',  ( -1.000000000000000000, 0.000000000000000000, 0.000000000000000000 ) ) ;
#4711=ORIENTED_EDGE ( 'NONE', *, *, #22449, .T. ) ;
#4716=ORIENTED_EDGE ( 'NONE', *, *, #13607, .T. ) ;
#4720=ORIENTED_EDGE ( 'NONE', *, *, #6449, .T. ) ;
#4724=EDGE_CURVE ( 'NONE', #9813, #32383, #35320, .T. ) ;
#4725=DIRECTION ( 'NONE',  ( 0.000000000000000000, 0.000000000000000000, 1.000000000000000000 ) ) ;
#4728=EDGE_CURVE ( 'NONE', #31732, #32324, #24572, .T. ) ;
#4731=LINE ( 'NONE', #5081, #19576 ) ;
#4732=ORIENTED_EDGE ( 'NONE', *, *, #32747, .T. ) ;
#4737=DIRECTION ( 'NONE',  ( 0.000000000000000000, 0.000000000000000000, -1.000000000000000000 ) ) ;
#4743=DIRECTION ( 'NONE',  ( 0.000000000000000000, 0.000000000000000000, 1.000000000000000000 ) ) ;
#4744=CARTESIAN_POINT ( 'NONE',  ( 0.000000000000000000, 0.000000000000000000, 0.000000000000000000 ) ) ;
#4747=CYLINDRICAL_SURFACE ( 'NONE', #34880, 47.49900000000001654 ) ;
#4749=EDGE_LOOP ( 'NONE', ( #29469, #8930, #24312, #15619 ) ) ;
#4754=CYLINDRICAL_SURFACE ( 'NONE', #29111, 20.00000000000000355 ) ;
#4758=DIRECTION ( 'NONE',  ( -1.000000000000000000, 0.000000000000000000, 0.000000000000000000 ) ) ;
#4761=EDGE_CURVE ( 'NONE', #6860, #26487, #4270, .T. ) ;
#4765=EDGE_LOOP ( 'NONE', ( #20616, #8302, #6492, #18096 ) ) ;
#4775=LINE ( 'NONE', #29611, #21416 ) ;
#4778=DIRECTION ( 'NONE',  ( -1.000000000000000000, 0.000000000000000000, 0.000000000000000000 ) ) ;
#4781=CYLINDRICAL_SURFACE ( 'NONE', #203, 20.00000000000000711 ) ;
#4783=VECTOR ( 'NONE', #6481, 1000.000000000000000 ) ;
#4791=ORIENTED_EDGE ( 'NONE', *, *, #33012, .F. ) ;
#4793=DIRECTION ( 'NONE',  ( 0.000000000000000000, -0.3681245526846853022, 0.9297764858882484607 ) ) ;
#4798=DIRECTION ( 'NONE',  ( 0.000000000000000000, 0.000000000000000000, -1.000000000000000000 ) ) ;
#4801=ORIENTED_EDGE ( 'NONE', *, *, #275, .F. ) ;
#4810=ORIENTED_EDGE ( 'NONE', *, *, #16382, .F. ) ;
#4813=CIRCLE ( 'NONE', #27243, 52.00000000000000711 ) ;
#4819=CARTESIAN_POINT ( 'NONE',  ( 4.000000000000003553, 39.64889472655781333, -33.64468972902464827 ) ) ;
#4824=LINE ( 'NONE', #23902, #6376 ) ;
#4830=CARTESIAN_POINT ( 'NONE',  ( 0.000000000000000000, 0.000000000000000000, 0.000000000000000000 ) ) ;
#4831=CARTESIAN_POINT ( 'NONE',  ( 7.999999999999992895, 5.667686777401707232, 46.64153600743606631 ) ) ;
#4832=VECTOR ( 'NONE', #31692, 1000.000000000000000 ) ;
#4834=LINE ( 'NONE', #32009, #33893 ) ;
#4840=VERTEX_POINT ( 'NONE', #8167 ) ;
#4843=CARTESIAN_POINT ( 'NONE',  ( 0.000000000000000000, 5.871425383721554425, 51.66745943012285380 ) ) ;
#4848=DIRECTION ( 'NONE',  ( -1.000000000000000000, -0.000000000000000000, -0.000000000000000000 ) ) ;
#4855=ORIENTED_EDGE ( 'NONE', *, *, #9500, .F. ) ;
#4874=FACE_OUTER_BOUND ( 'NONE', #4361, .T. ) ;
#4880=DIRECTION ( 'NONE',  ( 1.000000000000000000, -0.000000000000000000, -0.000000000000000000 ) ) ;
#4886=DIRECTION ( 'NONE',  ( -1.000000000000000000, 0.000000000000000000, 0.000000000000000000 ) ) ;
#4887=ADVANCED_FACE ( 'NONE', ( #12431 ), #9728, .T. ) ;
#4891=AXIS2_PLACEMENT_3D ( 'NONE', #30428, #19587, #8090 ) ;
#4893=DIRECTION ( 'NONE',  ( 0.000000000000000000, -0.4817536741017035551, -0.8763066800438700232 ) ) ;
#4896=DIRECTION ( 'NONE',  ( 0.000000000000000000, 0.000000000000000000, -1.000000000000000000 ) ) ;
#4899=ADVANCED_FACE ( 'NONE', ( #25945 ), #15288, .T. ) ;
#4903=ORIENTED_EDGE ( 'NONE', *, *, #2228, .F. ) ;
#4908=CIRCLE ( 'NONE', #870, 47.49900000000000944 ) ;
#4912=DIRECTION ( 'NONE',  ( -1.000000000000000000, -0.000000000000000000, 0.000000000000000000 ) ) ;
#4917=CYLINDRICAL_SURFACE ( 'NONE', #3830, 52.00000000000000711 ) ;
#4919=EDGE_CURVE ( 'NONE', #9813, #26454, #24409, .T. ) ;
#4921=EDGE_CURVE ( 'NONE', #35237, #29395, #12321, .T. ) ;
#4927=DIRECTION ( 'NONE',  ( -1.000000000000000000, 0.000000000000000000, -0.000000000000000000 ) ) ;
#4933=CARTESIAN_POINT ( 'NONE',  ( 0.000000000000000000, 0.2227391519116599106, 46.98410307550729215 ) ) ;
#4946=CARTESIAN_POINT ( 'NONE',  ( 0.000000000000000000, -39.64889472655708857, -33.64468972902551513 ) ) ;
#4956=DIRECTION ( 'NONE',  ( -1.000000000000000000, 0.000000000000000000, 0.000000000000000000 ) ) ;
#4957=EDGE_LOOP ( 'NONE', ( #35361, #31161, #15292, #4277 ) ) ;
#4965=DIRECTION ( 'NONE',  ( -1.000000000000000000, -0.000000000000000000, -0.000000000000000000 ) ) ;
#4967=DIRECTION ( 'NONE',  ( -1.000000000000000000, 0.000000000000000000, 0.000000000000000000 ) ) ;
#4969=CIRCLE ( 'NONE', #3811, 52.00000000000000711 ) ;
#4973=VECTOR ( 'NONE', #9505, 1000.000000000000000 ) ;
#4976=DIRECTION ( 'NONE',  ( -1.000000000000000000, -0.000000000000000000, -0.000000000000000000 ) ) ;
#4978=VERTEX_POINT ( 'NONE', #31337 ) ;
#4981=ORIENTED_EDGE ( 'NONE', *, *, #13607, .F. ) ;
#4982=ORIENTED_EDGE ( 'NONE', *, *, #18025, .F. ) ;
#4984=CIRCLE ( 'NONE', #8967, 20.00000000000000711 ) ;
#4988=ORIENTED_EDGE ( 'NONE', *, *, #7057, .T. ) ;
#4989=AXIS2_PLACEMENT_3D ( 'NONE', #610, #19337, #11244 ) ;
#4990=CARTESIAN_POINT ( 'NONE',  ( 7.999999999999992895, -51.85248208264516023, -3.914090171286743747 ) ) ;
#4991=LINE ( 'NONE', #4819, #34483 ) ;
#4997=EDGE_CURVE ( 'NONE', #15078, #352, #9436, .T. ) ;
#5005=DIRECTION ( 'NONE',  ( 0.000000000000000000, 0.000000000000000000, 1.000000000000000000 ) ) ;
#5009=CYLINDRICAL_SURFACE ( 'NONE', #5208, 47.49900000000001654 ) ;
#5014=CYLINDRICAL_SURFACE ( 'NONE', #7766, 52.00000000000000711 ) ;
#5019=CIRCLE ( 'NONE', #967, 47.49900000000001654 ) ;
#5023=CIRCLE ( 'NONE', #22240, 47.49900000000001654 ) ;
#5036=DIRECTION ( 'NONE',  ( 0.000000000000000000, 0.000000000000000000, 1.000000000000000000 ) ) ;
#5040=AXIS2_PLACEMENT_3D ( 'NONE', #7405, #16016, #4893 ) ;
#5042=CIRCLE ( 'NONE', #7343, 52.00000000000000711 ) ;
#5052=CYLINDRICAL_SURFACE ( 'NONE', #6116, 52.00000000000000711 ) ;
#5056=DIRECTION ( 'NONE',  ( 0.000000000000000000, -0.2486898871648416942, -0.9685831611286345177 ) ) ;
#5057=DIRECTION ( 'NONE',  ( 0.000000000000000000, 0.000000000000000000, 1.000000000000000000 ) ) ;
#5061=ADVANCED_FACE ( 'NONE', ( #10622 ), #9182, .T. ) ;
#5070=EDGE_LOOP ( 'NONE', ( #12284, #35440, #2417, #18326 ) ) ;
#5072=AXIS2_PLACEMENT_3D ( 'NONE', #13308, #4848, #4682 ) ;
#5081=CARTESIAN_POINT ( 'NONE',  ( 7.999999999999992895, 24.72041153920734047, 40.55929306992698002 ) ) ;
#5082=ORIENTED_EDGE ( 'NONE', *, *, #9526, .F. ) ;
#5094=EDGE_CURVE ( 'NONE', #18961, #3813, #2577, .T. ) ;
#5098=CARTESIAN_POINT ( 'NONE',  ( 7.999999999999992895, 0.6505223195683029758, 51.99593080916758936 ) ) ;
#5102=ORIENTED_EDGE ( 'NONE', *, *, #30443, .F. ) ;
#5104=DIRECTION ( 'NONE',  ( 0.000000000000000000, 0.000000000000000000, -1.000000000000000000 ) ) ;
#5107=DIRECTION ( 'NONE',  ( 0.000000000000000000, 0.000000000000000000, 1.000000000000000000 ) ) ;
#5115=VERTEX_POINT ( 'NONE', #10274 ) ;
#5119=ORIENTED_EDGE ( 'NONE', *, *, #4225, .F. ) ;
#5121=CIRCLE ( 'NONE', #5675, 47.49900000000001654 ) ;
#5128=DIRECTION ( 'NONE',  ( 0.000000000000000000, 0.000000000000000000, 1.000000000000000000 ) ) ;
#5129=PRODUCT_DEFINITION ( 'UNKNOWN', '', #4613, #9044 ) ;
#5135=EDGE_CURVE ( 'NONE', #31456, #19390, #25564, .T. ) ;
#5142=VECTOR ( 'NONE', #3695, 1000.000000000000000 ) ;
#5144=CARTESIAN_POINT ( 'NONE',  ( 7.999999999999992895, 17.50309955389611716, 43.60271849949368317 ) ) ;
#5149=ORIENTED_EDGE ( 'NONE', *, *, #7263, .T. ) ;
#5156=DIRECTION ( 'NONE',  ( -1.000000000000000000, 0.000000000000000000, 0.000000000000000000 ) ) ;
#5157=ORIENTED_EDGE ( 'NONE', *, *, #18480, .T. ) ;
#5165=EDGE_CURVE ( 'NONE', #27200, #11310, #35341, .T. ) ;
#5170=EDGE_CURVE ( 'NONE', #4180, #7835, #27366, .T. ) ;
#5171=ADVANCED_FACE ( 'NONE', ( #2362 ), #13681, .T. ) ;
#5176=DIRECTION ( 'NONE',  ( -1.000000000000000000, 0.000000000000000000, 0.000000000000000000 ) ) ;
#5181=DIRECTION ( 'NONE',  ( -1.000000000000000000, 0.000000000000000000, 0.000000000000000000 ) ) ;
#5185=CARTESIAN_POINT ( 'NONE',  ( 7.999999999999992895, 27.79676263918186052, 37.88001506494778425 ) ) ;
#5188=DIRECTION ( 'NONE',  ( 0.000000000000000000, 0.000000000000000000, -1.000000000000000000 ) ) ;
#5197=CYLINDRICAL_SURFACE ( 'NONE', #31343, 20.00000000000000355 ) ;
#5199=CYLINDRICAL_SURFACE ( 'NONE', #22826, 20.00000000000000355 ) ;
#5201=CIRCLE ( 'NONE', #4068, 47.49900000000000944 ) ;
#5208=AXIS2_PLACEMENT_3D ( 'NONE', #7684, #26980, #7865 ) ;
#5211=EDGE_CURVE ( 'NONE', #25508, #21169, #27719, .T. ) ;
#5212=DIRECTION ( 'NONE',  ( -1.000000000000000000, 0.000000000000000000, 0.000000000000000000 ) ) ;
#5221=DIRECTION ( 'NONE',  ( 1.000000000000000000, 0.000000000000000000, 0.000000000000000000 ) ) ;
#5222=ORIENTED_EDGE ( 'NONE', *, *, #877, .F. ) ;
#5228=DIRECTION ( 'NONE',  ( 0.000000000000000000, 0.000000000000000000, 1.000000000000000000 ) ) ;
#5230=DIRECTION ( 'NONE',  ( -1.000000000000000000, -0.000000000000000000, -0.000000000000000000 ) ) ;
#5232=CARTESIAN_POINT ( 'NONE',  ( 7.999999999999992895, -17.08890430202781374, 43.76671000081938701 ) ) ;
#5233=ORIENTED_EDGE ( 'NONE', *, *, #32854, .T. ) ;
#5234=CARTESIAN_POINT ( 'NONE',  ( 0.000000000000000000, 5.667686777401707232, 46.64153600743606631 ) ) ;
#5240=CARTESIAN_POINT ( 'NONE',  ( 7.999999999999992895, 25.61928775981107265, -45.25098998563451147 ) ) ;
#5248=DIRECTION ( 'NONE',  ( -1.000000000000000000, 0.000000000000000000, -0.000000000000000000 ) ) ;
#5253=CARTESIAN_POINT ( 'NONE',  ( -9.999999999999994671, 0.000000000000000000, 0.000000000000000000 ) ) ;
#5268=CARTESIAN_POINT ( 'NONE',  ( 0.000000000000000000, 0.000000000000000000, 0.000000000000000000 ) ) ;
#5305=EDGE_CURVE ( 'NONE', #29834, #8656, #6574, .T. ) ;
#5306=DIRECTION ( 'NONE',  ( -1.000000000000000000, -0.000000000000000000, 0.000000000000000000 ) ) ;
#5313=CIRCLE ( 'NONE', #27159, 52.00000000000000711 ) ;
#5317=LINE ( 'NONE', #7998, #24027 ) ;
#5319=EDGE_CURVE ( 'NONE', #2939, #31530, #15765, .T. ) ;
#5320=CARTESIAN_POINT ( 'NONE',  ( -9.999999999999994671, 0.000000000000000000, 0.000000000000000000 ) ) ;
#5326=VECTOR ( 'NONE', #31056, 1000.000000000000000 ) ;
#5328=DIRECTION ( 'NONE',  ( 0.000000000000000000, -0.3681245526846853022, 0.9297764858882484607 ) ) ;
#5335=VERTEX_POINT ( 'NONE', #14531 ) ;
#5340=AXIS2_PLACEMENT_3D ( 'NONE', #31201, #22203, #963 ) ;
#5343=CARTESIAN_POINT ( 'NONE',  ( 7.999999999999992895, 49.65209126885785906, -15.44894276735497840 ) ) ;
#5345=CARTESIAN_POINT ( 'NONE',  ( 7.999999999999992895, 31.08872492060014991, -41.68322423723069647 ) ) ;
#5347=ORIENTED_EDGE ( 'NONE', *, *, #16789, .T. ) ;
#5352=DIRECTION ( 'NONE',  ( -0.000000000000000000, 1.000000000000000000, 0.000000000000000000 ) ) ;
#5354=DIRECTION ( 'NONE',  ( 0.000000000000000000, -0.9980267284282708928, -0.06279051952932436509 ) ) ;
#5360=AXIS2_PLACEMENT_3D ( 'NONE', #35171, #27416, #29762 ) ;
#5370=CARTESIAN_POINT ( 'NONE',  ( 7.999999999999992895, -47.00885577955417460, 6.806061952192132836 ) ) ;
#5377=ORIENTED_EDGE ( 'NONE', *, *, #3561, .F. ) ;
#5382=CARTESIAN_POINT ( 'NONE',  ( 7.999999999999992895, 42.60732521687599217, -19.80331771201615609 ) ) ;
#5386=VERTEX_POINT ( 'NONE', #23186 ) ;
#5387=ORIENTED_EDGE ( 'NONE', *, *, #20047, .F. ) ;
#5391=CARTESIAN_POINT ( 'NONE',  ( 50.00005079999998969, 14.30000000000000071, 3.000000000000002665 ) ) ;
#5393=CIRCLE ( 'NONE', #9408, 20.00000000000000355 ) ;
#5404=CARTESIAN_POINT ( 'NONE',  ( 0.000000000000000000, 0.000000000000000000, 0.000000000000000000 ) ) ;
#5405=CARTESIAN_POINT ( 'NONE',  ( 7.999999999999992895, -11.46872990052412611, 45.56340405422440654 ) ) ;
#5426=DIRECTION ( 'NONE',  ( 0.000000000000000000, 0.6845471059286900584, -0.7289686274214103312 ) ) ;
#5428=VERTEX_POINT ( 'NONE', #23542 ) ;
#5436=CYLINDRICAL_SURFACE ( 'NONE', #15643, 20.00000000000000711 ) ;
#5441=LINE ( 'NONE', #19785, #4330 ) ;
#5442=AXIS2_PLACEMENT_3D ( 'NONE', #12937, #21734, #13303 ) ;
#5447=DIRECTION ( 'NONE',  ( 1.000000000000000000, -0.000000000000000000, 0.000000000000000000 ) ) ;
#5453=LINE ( 'NONE', #11033, #13842 ) ;
#5455=ADVANCED_FACE ( 'NONE', ( #4300 ), #31119, .T. ) ;
#5457=DIRECTION ( 'NONE',  ( -1.000000000000000000, -0.000000000000000000, 0.000000000000000000 ) ) ;
#5486=DIRECTION ( 'NONE',  ( 0.000000000000000000, -0.7705132427757815927, -0.6374239897486989603 ) ) ;
#5488=CYLINDRICAL_SURFACE ( 'NONE', #8204, 20.00000000000000711 ) ;
#5495=DIRECTION ( 'NONE',  ( -1.000000000000000000, -0.000000000000000000, -0.000000000000000000 ) ) ;
#5502=ORIENTED_EDGE ( 'NONE', *, *, #11527, .F. ) ;
#5503=CYLINDRICAL_SURFACE ( 'NONE', #34862, 11.00000000000000000 ) ;
#5504=CYLINDRICAL_SURFACE ( 'NONE', #26325, 20.00000000000000711 ) ;
#5506=ORIENTED_EDGE ( 'NONE', *, *, #5170, .T. ) ;
#5511=ORIENTED_EDGE ( 'NONE', *, *, #25488, .T. ) ;
#5516=AXIS2_PLACEMENT_3D ( 'NONE', #18629, #13418, #18085 ) ;
#5518=DIRECTION ( 'NONE',  ( 1.000000000000000000, 0.000000000000000000, 0.000000000000000000 ) ) ;
#5534=( NAMED_UNIT ( * ) SI_UNIT ( $, .STERADIAN. ) SOLID_ANGLE_UNIT ( ) );
#5535=ORIENTED_EDGE ( 'NONE', *, *, #2090, .T. ) ;
#5541=ADVANCED_FACE ( 'NONE', ( #35255 ), #13457, .T. ) ;
#5548=AXIS2_PLACEMENT_3D ( 'NONE', #24170, #10124, #2039 ) ;
#5552=DIRECTION ( 'NONE',  ( 0.000000000000000000, 0.000000000000000000, 1.000000000000000000 ) ) ;
#5556=AXIS2_PLACEMENT_3D ( 'NONE', #27320, #22077, #24438 ) ;
#5557=ORIENTED_EDGE ( 'NONE', *, *, #13905, .T. ) ;
#5561=DIRECTION ( 'NONE',  ( -1.000000000000000000, -0.000000000000000000, 0.000000000000000000 ) ) ;
#5564=CYLINDRICAL_SURFACE ( 'NONE', #21260, 52.00000000000000711 ) ;
#5569=ADVANCED_FACE ( 'NONE', ( #18852 ), #32528, .T. ) ;
#5575=AXIS2_PLACEMENT_3D ( 'NONE', #31781, #2282, #23869 ) ;
#5576=DIRECTION ( 'NONE',  ( -1.000000000000000000, 0.000000000000000000, 0.000000000000000000 ) ) ;
#5579=LINE ( 'NONE', #10804, #27383 ) ;
#5581=EDGE_LOOP ( 'NONE', ( #5157, #29192, #3774, #25220 ) ) ;
#5583=ORIENTED_EDGE ( 'NONE', *, *, #15851, .F. ) ;
#5586=FACE_OUTER_BOUND ( 'NONE', #2906, .T. ) ;
#5588=VECTOR ( 'NONE', #31602, 1000.000000000000000 ) ;
#5591=CARTESIAN_POINT ( 'NONE',  ( 7.999999999999992895, 39.64889472655731595, 33.64468972902522381 ) ) ;
#5597=VECTOR ( 'NONE', #25086, 1000.000000000000000 ) ;
#5601=FACE_OUTER_BOUND ( 'NONE', #30432, .T. ) ;
#5602=AXIS2_PLACEMENT_3D ( 'NONE', #10715, #27646, #14106 ) ;
#5609=EDGE_CURVE ( 'NONE', #11196, #14042, #7738, .T. ) ;
#5611=CYLINDRICAL_SURFACE ( 'NONE', #32296, 52.00000000000000711 ) ;
#5617=CARTESIAN_POINT ( 'NONE',  ( 0.000000000000000000, 0.000000000000000000, 0.000000000000000000 ) ) ;
#5627=ORIENTED_EDGE ( 'NONE', *, *, #30440, .T. ) ;
#5640=DIRECTION ( 'NONE',  ( -1.000000000000000000, 0.000000000000000000, 0.000000000000000000 ) ) ;
#5643=ORIENTED_EDGE ( 'NONE', *, *, #2090, .F. ) ;
#5646=AXIS2_PLACEMENT_3D ( 'NONE', #19663, #6188, #12120 ) ;
#5648=ORIENTED_EDGE ( 'NONE', *, *, #24708, .T. ) ;
#5655=AXIS2_PLACEMENT_3D ( 'NONE', #32548, #15790, #20835 ) ;
#5656=AXIS2_PLACEMENT_3D ( 'NONE', #3307, #33530, #8323 ) ;
#5659=DIRECTION ( 'NONE',  ( 0.000000000000000000, -0.9510565162951500895, -0.3090169943749581094 ) ) ;
#5663=CARTESIAN_POINT ( 'NONE',  ( 7.999999999999992895, 45.78515115856044559, 12.64416602183680816 ) ) ;
#5670=VERTEX_POINT ( 'NONE', #1768 ) ;
#5675=AXIS2_PLACEMENT_3D ( 'NONE', #24127, #2182, #35118 ) ;
#5679=ORIENTED_EDGE ( 'NONE', *, *, #5977, .T. ) ;
#5683=DIRECTION ( 'NONE',  ( 0.000000000000000000, 0.000000000000000000, 1.000000000000000000 ) ) ;
#5684=CARTESIAN_POINT ( 'NONE',  ( 0.000000000000000000, 36.05989434073656241, -30.12041790338579261 ) ) ;
#5689=EDGE_LOOP ( 'NONE', ( #27939, #30777, #560, #31615 ) ) ;
#5691=EDGE_CURVE ( 'NONE', #2768, #16982, #16386, .T. ) ;
#5706=DIRECTION ( 'NONE',  ( 0.000000000000000000, 0.000000000000000000, 1.000000000000000000 ) ) ;
#5707=DIRECTION ( 'NONE',  ( -1.000000000000000000, -0.000000000000000000, -0.000000000000000000 ) ) ;
#5718=CARTESIAN_POINT ( 'NONE',  ( 7.999999999999992895, 0.000000000000000000, 0.000000000000000000 ) ) ;
#5721=VERTEX_POINT ( 'NONE', #6053 ) ;
#5728=VECTOR ( 'NONE', #31645, 1000.000000000000000 ) ;
#5735=DIRECTION ( 'NONE',  ( -1.000000000000000000, -0.000000000000000000, -0.000000000000000000 ) ) ;
#5742=DIRECTION ( 'NONE',  ( -1.000000000000000000, 0.000000000000000000, -0.000000000000000000 ) ) ;
#5747=DIRECTION ( 'NONE',  ( -1.000000000000000000, -0.000000000000000000, 0.000000000000000000 ) ) ;
#5749=DIRECTION ( 'NONE',  ( -1.000000000000000000, 0.000000000000000000, 0.000000000000000000 ) ) ;
#5751=VERTEX_POINT ( 'NONE', #5875 ) ;
#5756=AXIS2_PLACEMENT_3D ( 'NONE', #15801, #27178, #16334 ) ;
#5760=ORIENTED_EDGE ( 'NONE', *, *, #32795, .T. ) ;
#5767=CARTESIAN_POINT ( 'NONE',  ( 7.999999999999992895, 0.000000000000000000, 0.000000000000000000 ) ) ;
#5775=DIRECTION ( 'NONE',  ( 0.000000000000000000, 0.000000000000000000, 1.000000000000000000 ) ) ;
#5776=ORIENTED_EDGE ( 'NONE', *, *, #33278, .F. ) ;
#5777=ORIENTED_EDGE ( 'NONE', *, *, #9123, .F. ) ;
#5778=AXIS2_PLACEMENT_3D ( 'NONE', #20107, #1233, #682 ) ;
#5786=CARTESIAN_POINT ( 'NONE',  ( 4.000000000000003553, -5.871425383721172508, -51.66745943012291065 ) ) ;
#5795=VERTEX_POINT ( 'NONE', #30719 ) ;
#5798=DIRECTION ( 'NONE',  ( -1.000000000000000000, 0.000000000000000000, 0.000000000000000000 ) ) ;
#5801=CARTESIAN_POINT ( 'NONE',  ( 0.000000000000000000, -37.91532898920900863, -28.61088654061680359 ) ) ;
#5809=DIRECTION ( 'NONE',  ( 0.000000000000000000, -0.4817536741017223734, 0.8763066800438596982 ) ) ;
#5813=ORIENTED_EDGE ( 'NONE', *, *, #6, .T. ) ;
#5818=DIRECTION ( 'NONE',  ( -1.000000000000000000, 0.000000000000000000, 0.000000000000000000 ) ) ;
#5823=CARTESIAN_POINT ( 'NONE',  ( 7.999999999999992895, 32.00046193115148441, 34.40241257139697950 ) ) ;
#5833=LINE ( 'NONE', #5663, #4256 ) ;
#5834=EDGE_LOOP ( 'NONE', ( #83, #8174, #18060, #17881, #19428, #3557, #27030, #14661, #15332, #645, #11844, #25433, #9520, #3768, #25926, #25396, #29295, #26380, #10502, #12097, #7784, #6404, #17993, #9191, #25074, #25842, #18293, #3839, #17278, #218, #19085, #29667, #24452, #9122, #8662, #25459, #17922, #14908, #10889, #14003, #4855, #5377, #13891, #20708, #17972, #15436, #28649, #5102, #24534, #28308, #23877, #3509, #33834, #8304, #32870, #9883, #13435, #29636, #33881, #23171, #6596, #18198, #4266, #9223, #1277, #17526, #9620, #21158, #29937, #3041, #32080, #8834, #34454, #6032, #5082, #24858, #33609, #34458, #22683, #24574, #17508, #12351, #29908, #4455, #13267, #5387, #944, #27115, #24629, #18273, #19815, #19210, #19384, #35113, #29394, #8368, #3256, #18542, #26415, #18897, #12912, #33159, #35057, #535, #29721, #6506, #30243, #20575, #28627, #18994, #23251, #27304, #6548, #25382, #35615, #5969, #16238, #22183, #21341, #13955, #34702, #31664, #26310, #32032, #12551, #24720, #28746, #18712, #17593, #28646, #17707, #380, #26358, #7658, #13516, #22229, #15831, #6313, #29000, #29420, #29998, #9742, #24143, #10685, #24331, #4024, #11201, #795, #12623, #19013, #29103, #16227, #11567, #16176, #1125, #14541, #27531, #18560, #10906, #23330, #30593, #5941, #25210, #15527, #31492, #2221, #29914, #3257, #13743, #6108, #27158, #22754, #27550, #14903, #28633, #7165, #22276, #24549, #24157, #22357, #28628, #15370, #3439, #32695, #10803, #16311, #24636, #11350, #27689, #2278, #12387, #3088, #12002, #25888, #12584, #22539, #25201, #17725, #21880, #28815, #26299, #12682, #5643 ) ) ;
#5839=VERTEX_POINT ( 'NONE', #12337 ) ;
#5843=CYLINDRICAL_SURFACE ( 'NONE', #21097, 52.00000000000000711 ) ;
#5848=CARTESIAN_POINT ( 'NONE',  ( 0.000000000000000000, 0.000000000000000000, 0.000000000000000000 ) ) ;
#5858=EDGE_LOOP ( 'NONE', ( #30808, #17885, #18933, #1750 ) ) ;
#5860=DIRECTION ( 'NONE',  ( 0.000000000000000000, 0.9980267284282717810, -0.06279051952930997382 ) ) ;
#5865=DIRECTION ( 'NONE',  ( 0.000000000000000000, -0.1253332335642904638, -0.9921147013144796523 ) ) ;
#5874=DIRECTION ( 'NONE',  ( 0.000000000000000000, -0.7705132427757817037, -0.6374239897486988493 ) ) ;
#5875=CARTESIAN_POINT ( 'NONE',  ( 7.999999999999992895, 3.840921266750509488, -47.34345070675166767 ) ) ;
#5877=DIRECTION ( 'NONE',  ( 0.000000000000000000, -0.3681245526846653737, -0.9297764858882564543 ) ) ;
#5879=ORIENTED_EDGE ( 'NONE', *, *, #18479, .T. ) ;
#5883=DIRECTION ( 'NONE',  ( -1.000000000000000000, 0.000000000000000000, 0.000000000000000000 ) ) ;
#5887=DIRECTION ( 'NONE',  ( -1.000000000000000000, 0.000000000000000000, 0.000000000000000000 ) ) ;
#5901=FACE_OUTER_BOUND ( 'NONE', #2583, .T. ) ;
#5908=AXIS2_PLACEMENT_3D ( 'NONE', #14310, #25313, #34304 ) ;
#5922=ADVANCED_FACE ( 'NONE', ( #14489 ), #15029, .T. ) ;
#5923=CARTESIAN_POINT ( 'NONE',  ( 0.000000000000000000, 6.109652351741788223, 46.58570277113510372 ) ) ;
#5932=EDGE_CURVE ( 'NONE', #4250, #28091, #26174, .T. ) ;
#5937=DIRECTION ( 'NONE',  ( 0.000000000000000000, 0.000000000000000000, -1.000000000000000000 ) ) ;
#5941=ORIENTED_EDGE ( 'NONE', *, *, #4051, .F. ) ;
#5942=CARTESIAN_POINT ( 'NONE',  ( 7.999999999999992895, 0.000000000000000000, 0.000000000000000000 ) ) ;
#5948=CIRCLE ( 'NONE', #12845, 20.00000000000000711 ) ;
#5961=CYLINDRICAL_SURFACE ( 'NONE', #3757, 20.00000000000000355 ) ;
#5966=ADVANCED_FACE ( 'NONE', ( #17370 ), #1016, .T. ) ;
#5969=ORIENTED_EDGE ( 'NONE', *, *, #8709, .F. ) ;
#5977=EDGE_CURVE ( 'NONE', #25395, #13426, #33642, .T. ) ;
#5986=LINE ( 'NONE', #27948, #19926 ) ;
#5990=ORIENTED_EDGE ( 'NONE', *, *, #1378, .F. ) ;
#5992=DIRECTION ( 'NONE',  ( -1.000000000000000000, 0.000000000000000000, 0.000000000000000000 ) ) ;
#5994=CYLINDRICAL_SURFACE ( 'NONE', #14904, 47.49900000000001654 ) ;
#5996=CIRCLE ( 'NONE', #22653, 20.00000000000000711 ) ;
#5999=EDGE_CURVE ( 'NONE', #29381, #19471, #27339, .T. ) ;
#6001=DIRECTION ( 'NONE',  ( -1.000000000000000000, 0.000000000000000000, 0.000000000000000000 ) ) ;
#6005=DIRECTION ( 'NONE',  ( -1.000000000000000000, -0.000000000000000000, 0.000000000000000000 ) ) ;
#6007=EDGE_CURVE ( 'NONE', #15607, #19637, #20404, .T. ) ;
#6009=DIRECTION ( 'NONE',  ( 0.000000000000000000, 0.000000000000000000, 1.000000000000000000 ) ) ;
#6019=CARTESIAN_POINT ( 'NONE',  ( 7.999999999999992895, 14.30000000000000071, 3.000000000000002665 ) ) ;
#6021=EDGE_CURVE ( 'NONE', #34112, #7789, #23304, .T. ) ;
#6032=ORIENTED_EDGE ( 'NONE', *, *, #3653, .F. ) ;
#6041=DIRECTION ( 'NONE',  ( 0.000000000000000000, 0.000000000000000000, 1.000000000000000000 ) ) ;
#6053=CARTESIAN_POINT ( 'NONE',  ( 0.000000000000000000, -46.21320724403657465, 10.97699764141937884 ) ) ;
#6066=DIRECTION ( 'NONE',  ( -1.000000000000000000, 0.000000000000000000, -0.000000000000000000 ) ) ;
#6067=CARTESIAN_POINT ( 'NONE',  ( 0.000000000000000000, -8.053585752062238257, 46.81126742072021329 ) ) ;
#6091=DIRECTION ( 'NONE',  ( 0.000000000000000000, 0.000000000000000000, 1.000000000000000000 ) ) ;
#6093=CARTESIAN_POINT ( 'NONE',  ( 7.999999999999992895, 32.00046193115196758, -34.40241257139653186 ) ) ;
#6095=AXIS2_PLACEMENT_3D ( 'NONE', #10319, #10493, #15694 ) ;
#6096=ORIENTED_EDGE ( 'NONE', *, *, #27645, .T. ) ;
#6097=DIRECTION ( 'NONE',  ( -1.000000000000000000, 0.000000000000000000, 0.000000000000000000 ) ) ;
#6106=CARTESIAN_POINT ( 'NONE',  ( 7.999999999999992895, -3.840921266749481422, -47.34345070675177425 ) ) ;
#6108=ORIENTED_EDGE ( 'NONE', *, *, #23790, .F. ) ;
#6112=VERTEX_POINT ( 'NONE', #13250 ) ;
#6116=AXIS2_PLACEMENT_3D ( 'NONE', #7192, #5230, #32752 ) ;
#6120=ADVANCED_FACE ( 'NONE', ( #18811 ), #15735, .T. ) ;
#6122=CIRCLE ( 'NONE', #30295, 47.49900000000002365 ) ;
#6124=CYLINDRICAL_SURFACE ( 'NONE', #3948, 52.00000000000000711 ) ;
#6125=ORIENTED_EDGE ( 'NONE', *, *, #8140, .T. ) ;
#6131=CIRCLE ( 'NONE', #21670, 20.00000000000000711 ) ;
#6139=CARTESIAN_POINT ( 'NONE',  ( 0.000000000000000000, -46.19362259308839214, 8.585149169758333088 ) ) ;
#6141=EDGE_LOOP ( 'NONE', ( #34222, #8828, #24679, #1220 ) ) ;
#6142=VERTEX_POINT ( 'NONE', #7822 ) ;
#6143=DIRECTION ( 'NONE',  ( 0.000000000000000000, 0.000000000000000000, 1.000000000000000000 ) ) ;
#6156=ORIENTED_EDGE ( 'NONE', *, *, #4523, .F. ) ;
#6162=CIRCLE ( 'NONE', #10175, 52.00000000000000711 ) ;
#6164=ORIENTED_EDGE ( 'NONE', *, *, #14417, .T. ) ;
#6171=VERTEX_POINT ( 'NONE', #24058 ) ;
#6173=FACE_OUTER_BOUND ( 'NONE', #17130, .T. ) ;
#6174=CIRCLE ( 'NONE', #14801, 20.00000000000000711 ) ;
#6177=DIRECTION ( 'NONE',  ( -1.000000000000000000, 0.000000000000000000, -0.000000000000000000 ) ) ;
#6179=EDGE_CURVE ( 'NONE', #28842, #26596, #17565, .T. ) ;
#6188=DIRECTION ( 'NONE',  ( -1.000000000000000000, 0.000000000000000000, 0.000000000000000000 ) ) ;
#6194=CARTESIAN_POINT ( 'NONE',  ( 7.999999999999992895, 13.56094713063641599, -50.20060470671727870 ) ) ;
#6197=DIRECTION ( 'NONE',  ( 0.000000000000000000, 0.000000000000000000, 1.000000000000000000 ) ) ;
#6206=ORIENTED_EDGE ( 'NONE', *, *, #6179, .F. ) ;
#6208=VECTOR ( 'NONE', #31660, 1000.000000000000000 ) ;
#6212=LINE ( 'NONE', #6383, #3420 ) ;
#6213=EDGE_CURVE ( 'NONE', #7819, #17248, #15255, .T. ) ;
#6217=FACE_OUTER_BOUND ( 'NONE', #13998, .T. ) ;
#6219=DIRECTION ( 'NONE',  ( -1.000000000000000000, 0.000000000000000000, 0.000000000000000000 ) ) ;
#6221=ADVANCED_FACE ( 'NONE', ( #18989 ), #16802, .T. ) ;
#6229=CIRCLE ( 'NONE', #5656, 52.00000000000000711 ) ;
#6230=LINE ( 'NONE', #1191, #23965 ) ;
#6234=DIRECTION ( 'NONE',  ( 0.000000000000000000, -0.9822872507286904975, 0.1873813145857149698 ) ) ;
#6237=DIRECTION ( 'NONE',  ( 1.000000000000000000, 0.000000000000000000, 0.000000000000000000 ) ) ;
#6238=DIRECTION ( 'NONE',  ( 0.000000000000000000, 0.6845471059286846183, 0.7289686274214154382 ) ) ;
#6245=CYLINDRICAL_SURFACE ( 'NONE', #7171, 47.49900000000001654 ) ;
#6256=EDGE_LOOP ( 'NONE', ( #24084, #14496, #10962, #18442 ) ) ;
#6258=CARTESIAN_POINT ( 'NONE',  ( 0.000000000000000000, 46.90537658765334328, -2.727856614653800804 ) ) ;
#6268=DIRECTION ( 'NONE',  ( -1.000000000000000000, 0.000000000000000000, 0.000000000000000000 ) ) ;
#6269=DIRECTION ( 'NONE',  ( -1.000000000000000000, -0.000000000000000000, 0.000000000000000000 ) ) ;
#6271=DIRECTION ( 'NONE',  ( 0.000000000000000000, 0.6845471059286899473, -0.7289686274214103312 ) ) ;
#6283=ADVANCED_FACE ( 'NONE', ( #22208 ), #19158, .T. ) ;
#6289=CARTESIAN_POINT ( 'NONE',  ( 7.999999999999992895, -11.90021268425521939, -45.45261810511225065 ) ) ;
#6301=AXIS2_PLACEMENT_3D ( 'NONE', #32743, #13319, #34936 ) ;
#6304=DIRECTION ( 'NONE',  ( 0.000000000000000000, 0.000000000000000000, 1.000000000000000000 ) ) ;
#6305=AXIS2_PLACEMENT_3D ( 'NONE', #8571, #33415, #27152 ) ;
#6313=ORIENTED_EDGE ( 'NONE', *, *, #32391, .F. ) ;
#6318=ORIENTED_EDGE ( 'NONE', *, *, #6213, .T. ) ;
#6321=EDGE_CURVE ( 'NONE', #28112, #10384, #3795, .T. ) ;
#6325=AXIS2_PLACEMENT_3D ( 'NONE', #7279, #29072, #31235 ) ;
#6337=DIRECTION ( 'NONE',  ( 0.000000000000000000, 0.1253332335642974305, 0.9921147013144787641 ) ) ;
#6347=CARTESIAN_POINT ( 'NONE',  ( 0.000000000000000000, 51.19683565102457834, -9.104066087302935983 ) ) ;
#6348=AXIS2_PLACEMENT_3D ( 'NONE', #26650, #26824, #951 ) ;
#6349=CARTESIAN_POINT ( 'NONE',  ( 7.999999999999992895, 17.08890430202814059, -43.76671000081924490 ) ) ;
#6353=AXIS2_PLACEMENT_3D ( 'NONE', #28242, #6269, #23184 ) ;
#6354=DIRECTION ( 'NONE',  ( -1.000000000000000000, -0.000000000000000000, 0.000000000000000000 ) ) ;
#6362=CARTESIAN_POINT ( 'NONE',  ( 7.999999999999992895, 44.47301969247445896, 16.68249143361927267 ) ) ;
#6368=DIRECTION ( 'NONE',  ( -1.000000000000000000, 0.000000000000000000, 0.000000000000000000 ) ) ;
#6371=DIRECTION ( 'NONE',  ( 0.000000000000000000, 0.9510565162951544194, -0.3090169943749447867 ) ) ;
#6376=VECTOR ( 'NONE', #9493, 1000.000000000000000 ) ;
#6382=VERTEX_POINT ( 'NONE', #6362 ) ;
#6383=CARTESIAN_POINT ( 'NONE',  ( 4.000000000000003553, -0.6505223195686533622, 51.99593080916758936 ) ) ;
#6390=DIRECTION ( 'NONE',  ( 0.000000000000000000, 0.2486898871648482723, 0.9685831611286327414 ) ) ;
#6397=DIRECTION ( 'NONE',  ( 0.000000000000000000, 0.000000000000000000, 1.000000000000000000 ) ) ;
#6404=ORIENTED_EDGE ( 'NONE', *, *, #7552, .F. ) ;
#6407=AXIS2_PLACEMENT_3D ( 'NONE', #10651, #10836, #16572 ) ;
#6413=VERTEX_POINT ( 'NONE', #9246 ) ;
#6414=CYLINDRICAL_SURFACE ( 'NONE', #11406, 20.00000000000000355 ) ;
#6416=ORIENTED_EDGE ( 'NONE', *, *, #26210, .T. ) ;
#6424=ORIENTED_EDGE ( 'NONE', *, *, #16067, .F. ) ;
#6428=AXIS2_PLACEMENT_3D ( 'NONE', #3087, #2916, #191 ) ;
#6429=ORIENTED_EDGE ( 'NONE', *, *, #23019, .F. ) ;
#6430=CIRCLE ( 'NONE', #20805, 52.00000000000000711 ) ;
#6432=EDGE_CURVE ( 'NONE', #7164, #4091, #15276, .T. ) ;
#6443=AXIS2_PLACEMENT_3D ( 'NONE', #18806, #29806, #8171 ) ;
#6446=ORIENTED_EDGE ( 'NONE', *, *, #14515, .T. ) ;
#6447=DIRECTION ( 'NONE',  ( -1.000000000000000000, 0.000000000000000000, -0.000000000000000000 ) ) ;
#6449=EDGE_CURVE ( 'NONE', #25742, #3119, #9602, .T. ) ;
#6457=VECTOR ( 'NONE', #22153, 1000.000000000000000 ) ;
#6458=CARTESIAN_POINT ( 'NONE',  ( 7.999999999999992895, -37.91532898920900863, -28.61088654061680359 ) ) ;
#6462=CIRCLE ( 'NONE', #26028, 20.00000000000000355 ) ;
#6465=ORIENTED_EDGE ( 'NONE', *, *, #29013, .T. ) ;
#6475=EDGE_CURVE ( 'NONE', #21098, #19242, #1498, .T. ) ;
#6481=DIRECTION ( 'NONE',  ( -1.000000000000000000, -0.000000000000000000, 0.000000000000000000 ) ) ;
#6483=CARTESIAN_POINT ( 'NONE',  ( 7.999999999999992895, -36.34385289850609979, 29.77717097092063980 ) ) ;
#6491=DIRECTION ( 'NONE',  ( -1.000000000000000000, 0.000000000000000000, 0.000000000000000000 ) ) ;
#6492=ORIENTED_EDGE ( 'NONE', *, *, #27324, .T. ) ;
#6500=VERTEX_POINT ( 'NONE', #25638 ) ;
#6506=ORIENTED_EDGE ( 'NONE', *, *, #29728, .F. ) ;
#6508=AXIS2_PLACEMENT_3D ( 'NONE', #5684, #16642, #14293 ) ;
#6514=ORIENTED_EDGE ( 'NONE', *, *, #35277, .T. ) ;
#6516=ORIENTED_EDGE ( 'NONE', *, *, #1405, .T. ) ;
#6519=VECTOR ( 'NONE', #24387, 1000.000000000000000 ) ;
#6527=AXIS2_PLACEMENT_3D ( 'NONE', #9907, #6491, #12075 ) ;
#6529=EDGE_CURVE ( 'NONE', #15756, #27135, #31981, .T. ) ;
#6537=DIRECTION ( 'NONE',  ( 1.000000000000000000, -0.000000000000000000, -0.000000000000000000 ) ) ;
#6544=DIRECTION ( 'NONE',  ( -1.000000000000000000, 0.000000000000000000, 0.000000000000000000 ) ) ;
#6545=VERTEX_POINT ( 'NONE', #33912 ) ;
#6548=ORIENTED_EDGE ( 'NONE', *, *, #20713, .F. ) ;
#6557=CARTESIAN_POINT ( 'NONE',  ( 0.000000000000000000, -34.03046037009280411, 33.13733193845794034 ) ) ;
#6558=EDGE_CURVE ( 'NONE', #29784, #1742, #16999, .T. ) ;
#6561=DIRECTION ( 'NONE',  ( 0.000000000000000000, 0.000000000000000000, 1.000000000000000000 ) ) ;
#6562=DIRECTION ( 'NONE',  ( 0.000000000000000000, 0.000000000000000000, 1.000000000000000000 ) ) ;
#6563=ORIENTED_EDGE ( 'NONE', *, *, #13484, .F. ) ;
#6564=EDGE_CURVE ( 'NONE', #4061, #169, #35437, .T. ) ;
#6568=CARTESIAN_POINT ( 'NONE',  ( 0.000000000000000000, 0.000000000000000000, 0.000000000000000000 ) ) ;
#6570=EDGE_CURVE ( 'NONE', #22667, #29876, #26226, .T. ) ;
#6571=FACE_OUTER_BOUND ( 'NONE', #883, .T. ) ;
#6572=CARTESIAN_POINT ( 'NONE',  ( 0.000000000000000000, 0.000000000000000000, 0.000000000000000000 ) ) ;
#6574=CIRCLE ( 'NONE', #27869, 20.00000000000000711 ) ;
#6575=DIRECTION ( 'NONE',  ( -1.000000000000000000, -0.000000000000000000, -0.000000000000000000 ) ) ;
#6579=DIRECTION ( 'NONE',  ( 1.000000000000000000, 0.000000000000000000, 0.000000000000000000 ) ) ;
#6580=CARTESIAN_POINT ( 'NONE',  ( 7.999999999999992895, 0.000000000000000000, 0.000000000000000000 ) ) ;
#6581=CIRCLE ( 'NONE', #23261, 20.00000000000000711 ) ;
#6583=VERTEX_POINT ( 'NONE', #18588 ) ;
#6588=ORIENTED_EDGE ( 'NONE', *, *, #14355, .F. ) ;
#6592=CARTESIAN_POINT ( 'NONE',  ( 0.000000000000000000, 0.000000000000000000, 0.000000000000000000 ) ) ;
#6596=ORIENTED_EDGE ( 'NONE', *, *, #16924, .F. ) ;
#6597=CIRCLE ( 'NONE', #12941, 20.00000000000000000 ) ;
#6598=EDGE_CURVE ( 'NONE', #33486, #13700, #14130, .T. ) ;
#6602=ADVANCED_FACE ( 'NONE', ( #7247 ), #4754, .T. ) ;
#6609=FACE_OUTER_BOUND ( 'NONE', #20831, .T. ) ;
#6610=CIRCLE ( 'NONE', #20968, 47.49900000000000944 ) ;
#6612=DIRECTION ( 'NONE',  ( 0.000000000000000000, 0.000000000000000000, 1.000000000000000000 ) ) ;
#6620=DIRECTION ( 'NONE',  ( 0.000000000000000000, 0.000000000000000000, 1.000000000000000000 ) ) ;
#6630=CARTESIAN_POINT ( 'NONE',  ( -9.999999999999994671, 0.000000000000000000, 0.000000000000000000 ) ) ;
#6636=AXIS2_PLACEMENT_3D ( 'NONE', #32322, #23874, #34501 ) ;
#6641=EDGE_CURVE ( 'NONE', #9660, #1640, #19866, .T. ) ;
#6644=AXIS2_PLACEMENT_3D ( 'NONE', #8440, #33291, #8609 ) ;
#6655=DIRECTION ( 'NONE',  ( 0.000000000000000000, 0.000000000000000000, 1.000000000000000000 ) ) ;
#6657=DIRECTION ( 'NONE',  ( 0.000000000000000000, -0.3681245526846654292, -0.9297764858882562322 ) ) ;
#6663=AXIS2_PLACEMENT_3D ( 'NONE', #33594, #8927, #9115 ) ;
#6665=CARTESIAN_POINT ( 'NONE',  ( 0.000000000000000000, 0.2227391519123156360, -46.98410307550729215 ) ) ;
#6679=EDGE_CURVE ( 'NONE', #21338, #18999, #13578, .T. ) ;
#6684=VERTEX_POINT ( 'NONE', #5801 ) ;
#6689=DIRECTION ( 'NONE',  ( -1.000000000000000000, 0.000000000000000000, 0.000000000000000000 ) ) ;
#6690=VERTEX_POINT ( 'NONE', #27420 ) ;
#6691=VERTEX_POINT ( 'NONE', #19113 ) ;
#6693=CIRCLE ( 'NONE', #26837, 47.49900000000001654 ) ;
#6696=EDGE_CURVE ( 'NONE', #19390, #24892, #11029, .T. ) ;
#6697=VERTEX_POINT ( 'NONE', #22166 ) ;
#6703=CARTESIAN_POINT ( 'NONE',  ( 0.000000000000000000, -24.72041153920704915, -40.55929306992714345 ) ) ;
#6716=CARTESIAN_POINT ( 'NONE',  ( 7.999999999999992895, 36.05989434073656241, -30.12041790338579261 ) ) ;
#6717=DIRECTION ( 'NONE',  ( 0.000000000000000000, 0.3681245526846718685, 0.9297764858882537897 ) ) ;
#6719=CIRCLE ( 'NONE', #26869, 20.00000000000000711 ) ;
#6729=CARTESIAN_POINT ( 'NONE',  ( 0.000000000000000000, 17.08890430202814059, -43.76671000081924490 ) ) ;
#6730=ORIENTED_EDGE ( 'NONE', *, *, #10860, .T. ) ;
#6731=EDGE_LOOP ( 'NONE', ( #19453, #23229, #34731, #21837 ) ) ;
#6733=ORIENTED_EDGE ( 'NONE', *, *, #16996, .T. ) ;
#6742=VECTOR ( 'NONE', #16901, 1000.000000000000000 ) ;
#6744=CARTESIAN_POINT ( 'NONE',  ( 0.000000000000000000, 47.32430374665932504, 21.55018039121545215 ) ) ;
#6749=DIRECTION ( 'NONE',  ( -1.000000000000000000, 0.000000000000000000, 0.000000000000000000 ) ) ;
#6750=ORIENTED_EDGE ( 'NONE', *, *, #29774, .T. ) ;
#6753=DIRECTION ( 'NONE',  ( 0.000000000000000000, 0.000000000000000000, 1.000000000000000000 ) ) ;
#6761=DIRECTION ( 'NONE',  ( 1.000000000000000000, 0.000000000000000000, 0.000000000000000000 ) ) ;
#6765=DIRECTION ( 'NONE',  ( 0.000000000000000000, 0.000000000000000000, -1.000000000000000000 ) ) ;
#6769=ORIENTED_EDGE ( 'NONE', *, *, #33030, .F. ) ;
#6770=VECTOR ( 'NONE', #32379, 1000.000000000000000 ) ;
#6774=EDGE_LOOP ( 'NONE', ( #2512, #3235, #14123, #24497 ) ) ;
#6783=DIRECTION ( 'NONE',  ( -1.000000000000000000, 0.000000000000000000, -0.000000000000000000 ) ) ;
#6788=EDGE_LOOP ( 'NONE', ( #16668, #27613, #31091, #16967 ) ) ;
#6789=DIRECTION ( 'NONE',  ( 0.000000000000000000, 0.000000000000000000, 1.000000000000000000 ) ) ;
#6793=VECTOR ( 'NONE', #25345, 1000.000000000000000 ) ;
#6796=DIRECTION ( 'NONE',  ( 0.000000000000000000, 0.000000000000000000, -1.000000000000000000 ) ) ;
#6799=CIRCLE ( 'NONE', #31537, 20.00000000000000711 ) ;
#6800=EDGE_CURVE ( 'NONE', #7480, #4435, #25664, .T. ) ;
#6810=ORIENTED_EDGE ( 'NONE', *, *, #1121, .F. ) ;
#6814=ORIENTED_EDGE ( 'NONE', *, *, #20259, .F. ) ;
#6815=EDGE_CURVE ( 'NONE', #20492, #13488, #8405, .T. ) ;
#6827=ORIENTED_EDGE ( 'NONE', *, *, #23440, .T. ) ;
#6831=CARTESIAN_POINT ( 'NONE',  ( 7.999999999999992895, 6.109652351741788223, 46.58570277113510372 ) ) ;
#6839=DIRECTION ( 'NONE',  ( -1.000000000000000000, 0.000000000000000000, -0.000000000000000000 ) ) ;
#6851=VERTEX_POINT ( 'NONE', #32812 ) ;
#6852=CARTESIAN_POINT ( 'NONE',  ( 7.999999999999992895, 3.840921266749832252, 47.34345070675172451 ) ) ;
#6860=VERTEX_POINT ( 'NONE', #13548 ) ;
#6863=CARTESIAN_POINT ( 'NONE',  ( 0.000000000000000000, 0.000000000000000000, 0.000000000000000000 ) ) ;
#6870=DIRECTION ( 'NONE',  ( -1.000000000000000000, 0.000000000000000000, -0.000000000000000000 ) ) ;
#6873=CIRCLE ( 'NONE', #32196, 47.49900000000001654 ) ;
#6876=AXIS2_PLACEMENT_3D ( 'NONE', #10315, #27059, #27236 ) ;
#6878=ORIENTED_EDGE ( 'NONE', *, *, #22301, .T. ) ;
#6879=VERTEX_POINT ( 'NONE', #10855 ) ;
#6887=DIRECTION ( 'NONE',  ( 0.000000000000000000, 0.000000000000000000, 1.000000000000000000 ) ) ;
#6890=CYLINDRICAL_SURFACE ( 'NONE', #24611, 20.00000000000000711 ) ;
#6892=CARTESIAN_POINT ( 'NONE',  ( 0.000000000000000000, 14.30000000000000071, -3.000000000000002665 ) ) ;
#6898=EDGE_CURVE ( 'NONE', #3192, #1965, #7277, .T. ) ;
#6900=CIRCLE ( 'NONE', #18388, 47.49900000000003075 ) ;
#6902=EDGE_CURVE ( 'NONE', #12983, #5428, #26856, .T. ) ;
#6907=CARTESIAN_POINT ( 'NONE',  ( 7.999999999999992895, 0.000000000000000000, 0.000000000000000000 ) ) ;
#6919=CARTESIAN_POINT ( 'NONE',  ( 7.999999999999992895, 12.30077720129168384, -50.52416135122070528 ) ) ;
#6921=ADVANCED_BREP_SHAPE_REPRESENTATION ( '', ( #10310, #21307 ), #32275 ) ;
#6942=CIRCLE ( 'NONE', #31662, 52.00000000000000711 ) ;
#6944=DIRECTION ( 'NONE',  ( -1.000000000000000000, 0.000000000000000000, -0.000000000000000000 ) ) ;
#6948=LINE ( 'NONE', #9656, #13649 ) ;
#6958=DIRECTION ( 'NONE',  ( 1.000000000000000000, -0.000000000000000000, -0.000000000000000000 ) ) ;
#6967=CARTESIAN_POINT ( 'NONE',  ( 7.999999999999992895, 0.000000000000000000, 0.000000000000000000 ) ) ;
#6972=CIRCLE ( 'NONE', #3546, 47.49900000000003075 ) ;
#6976=FACE_OUTER_BOUND ( 'NONE', #14018, .T. ) ;
#6979=CARTESIAN_POINT ( 'NONE',  ( 7.999999999999992895, 0.000000000000000000, 0.000000000000000000 ) ) ;
#6987=EDGE_LOOP ( 'NONE', ( #30402, #3907, #15269, #25509 ) ) ;
#6996=AXIS2_PLACEMENT_3D ( 'NONE', #35067, #15403, #18833 ) ;
#6998=CARTESIAN_POINT ( 'NONE',  ( 0.000000000000000000, 0.000000000000000000, 0.000000000000000000 ) ) ;
#7019=CARTESIAN_POINT ( 'NONE',  ( 7.999999999999992895, 42.60732521687599217, -19.80331771201615609 ) ) ;
#7029=EDGE_LOOP ( 'NONE', ( #22265, #30490, #5233, #33520 ) ) ;
#7031=CARTESIAN_POINT ( 'NONE',  ( 4.000000000000003553, -51.93417535146743802, 2.615612846549014492 ) ) ;
#7035=CIRCLE ( 'NONE', #31761, 20.00000000000000355 ) ;
#7038=ORIENTED_EDGE ( 'NONE', *, *, #16599, .F. ) ;
#7042=CARTESIAN_POINT ( 'NONE',  ( 7.999999999999992895, 19.44205635905603202, -43.33776004284589334 ) ) ;
#7044=EDGE_LOOP ( 'NONE', ( #32899, #16237, #5879, #692 ) ) ;
#7057=EDGE_CURVE ( 'NONE', #21218, #27996, #9376, .T. ) ;
#7076=DIRECTION ( 'NONE',  ( 0.000000000000000000, 0.9048270524660205760, -0.4257792915650702170 ) ) ;
#7078=VERTEX_POINT ( 'NONE', #19032 ) ;
#7088=ORIENTED_EDGE ( 'NONE', *, *, #13862, .F. ) ;
#7092=CARTESIAN_POINT ( 'NONE',  ( 7.999999999999992895, 36.05989434073613609, 30.12041790338630776 ) ) ;
#7093=CARTESIAN_POINT ( 'NONE',  ( 7.999999999999992895, -38.92705108641750655, 27.21837053747785973 ) ) ;
#7096=CIRCLE ( 'NONE', #2526, 47.49900000000000944 ) ;
#7099=AXIS2_PLACEMENT_3D ( 'NONE', #791, #30867, #20579 ) ;
#7112=AXIS2_PLACEMENT_3D ( 'NONE', #27097, #21311, #15907 ) ;
#7119=CARTESIAN_POINT ( 'NONE',  ( 7.999999999999992895, -17.50309955389642269, 43.60271849949356948 ) ) ;
#7126=VECTOR ( 'NONE', #18441, 1000.000000000000000 ) ;
#7127=CARTESIAN_POINT ( 'NONE',  ( 7.999999999999992895, -51.93417535146744513, 2.615612846549014492 ) ) ;
#7130=ORIENTED_EDGE ( 'NONE', *, *, #21777, .T. ) ;
#7136=CARTESIAN_POINT ( 'NONE',  ( 7.999999999999992895, -32.00046193115124282, -34.40241257139719977 ) ) ;
#7137=CARTESIAN_POINT ( 'NONE',  ( 0.000000000000000000, 29.60891106212789126, 37.14118181634776050 ) ) ;
#7141=CARTESIAN_POINT ( 'NONE',  ( 7.999999999999992895, -11.90021268425521939, -45.45261810511225065 ) ) ;
#7162=DIRECTION ( 'NONE',  ( 1.000000000000000000, -0.000000000000000000, -0.000000000000000000 ) ) ;
#7164=VERTEX_POINT ( 'NONE', #24627 ) ;
#7165=ORIENTED_EDGE ( 'NONE', *, *, #15653, .F. ) ;
#7170=ORIENTED_EDGE ( 'NONE', *, *, #28176, .T. ) ;
#7171=AXIS2_PLACEMENT_3D ( 'NONE', #5718, #17205, #16856 ) ;
#7173=DIRECTION ( 'NONE',  ( -1.000000000000000000, 0.000000000000000000, 0.000000000000000000 ) ) ;
#7175=CARTESIAN_POINT ( 'NONE',  ( 7.999999999999992895, 0.6505223195690454929, -51.99593080916758936 ) ) ;
#7181=CARTESIAN_POINT ( 'NONE',  ( 0.000000000000000000, -51.85248208264521708, 3.914090171286008335 ) ) ;
#7182=DIRECTION ( 'NONE',  ( -1.000000000000000000, 0.000000000000000000, -0.000000000000000000 ) ) ;
#7185=AXIS2_PLACEMENT_3D ( 'NONE', #18038, #6354, #26156 ) ;
#7192=CARTESIAN_POINT ( 'NONE',  ( -9.999999999999994671, 0.000000000000000000, 0.000000000000000000 ) ) ;
#7194=ORIENTED_EDGE ( 'NONE', *, *, #33012, .T. ) ;
#7195=CARTESIAN_POINT ( 'NONE',  ( 7.999999999999992895, 46.11014828289831513, 9.022736828081523441 ) ) ;
#7201=LINE ( 'NONE', #13168, #33051 ) ;
#7202=AXIS2_PLACEMENT_3D ( 'NONE', #15924, #24063, #23322 ) ;
#7203=ORIENTED_EDGE ( 'NONE', *, *, #32332, .F. ) ;
#7210=EDGE_LOOP ( 'NONE', ( #13587, #2343, #21836, #15938 ) ) ;
#7212=CIRCLE ( 'NONE', #14095, 20.00000000000000711 ) ;
#7213=CARTESIAN_POINT ( 'NONE',  ( 0.000000000000000000, 0.000000000000000000, 0.000000000000000000 ) ) ;
#7214=EDGE_CURVE ( 'NONE', #25525, #3192, #10942, .T. ) ;
#7218=EDGE_CURVE ( 'NONE', #27160, #9066, #6122, .T. ) ;
#7221=LINE ( 'NONE', #7042, #4671 ) ;
#7228=DIRECTION ( 'NONE',  ( -1.000000000000000000, 0.000000000000000000, 0.000000000000000000 ) ) ;
#7230=ORIENTED_EDGE ( 'NONE', *, *, #24239, .F. ) ;
#7241=ORIENTED_EDGE ( 'NONE', *, *, #3374, .F. ) ;
#7244=CARTESIAN_POINT ( 'NONE',  ( 0.000000000000000000, -40.47821179127691238, -32.64221760512803172 ) ) ;
#7246=ORIENTED_EDGE ( 'NONE', *, *, #19133, .F. ) ;
#7247=FACE_OUTER_BOUND ( 'NONE', #14787, .T. ) ;
#7261=VERTEX_POINT ( 'NONE', #649 ) ;
#7263=EDGE_CURVE ( 'NONE', #453, #28247, #8224, .T. ) ;
#7266=AXIS2_PLACEMENT_3D ( 'NONE', #8889, #17161, #22567 ) ;
#7268=DIRECTION ( 'NONE',  ( 1.000000000000000000, -0.000000000000000000, -0.000000000000000000 ) ) ;
#7269=ORIENTED_EDGE ( 'NONE', *, *, #30037, .T. ) ;
#7270=VERTEX_POINT ( 'NONE', #30551 ) ;
#7277=CIRCLE ( 'NONE', #23973, 20.00000000000000355 ) ;
#7279=CARTESIAN_POINT ( 'NONE',  ( 7.999999999999992895, -36.34385289850568057, -29.77717097092114074 ) ) ;
#7280=AXIS2_PLACEMENT_3D ( 'NONE', #28373, #22780, #20067 ) ;
#7297=LINE ( 'NONE', #9817, #18202 ) ;
#7302=CYLINDRICAL_SURFACE ( 'NONE', #15853, 47.49900000000001654 ) ;
#7305=ORIENTED_EDGE ( 'NONE', *, *, #31327, .T. ) ;
#7313=ORIENTED_EDGE ( 'NONE', *, *, #11127, .T. ) ;
#7315=AXIS2_PLACEMENT_3D ( 'NONE', #30081, #16370, #10992 ) ;
#7321=CIRCLE ( 'NONE', #2159, 52.00000000000000711 ) ;
#7324=DIRECTION ( 'NONE',  ( -1.000000000000000000, -0.000000000000000000, -0.000000000000000000 ) ) ;
#7330=DIRECTION ( 'NONE',  ( 0.000000000000000000, -0.2486898871648622888, 0.9685831611286290777 ) ) ;
#7343=AXIS2_PLACEMENT_3D ( 'NONE', #15130, #17669, #28669 ) ;
#7344=DIRECTION ( 'NONE',  ( 1.000000000000000000, 0.000000000000000000, 0.000000000000000000 ) ) ;
#7348=EDGE_CURVE ( 'NONE', #6171, #34917, #31468, .T. ) ;
#7355=ORIENTED_EDGE ( 'NONE', *, *, #11892, .T. ) ;
#7364=CIRCLE ( 'NONE', #28053, 20.00000000000001066 ) ;
#7365=CARTESIAN_POINT ( 'NONE',  ( 7.999999999999992895, -39.78933988720132220, 24.98727647984988565 ) ) ;
#7368=CARTESIAN_POINT ( 'NONE',  ( 7.999999999999992895, 0.000000000000000000, 0.000000000000000000 ) ) ;
#7369=VERTEX_POINT ( 'NONE', #22084 ) ;
#7370=ORIENTED_EDGE ( 'NONE', *, *, #22769, .T. ) ;
#7377=LINE ( 'NONE', #5391, #27015 ) ;
#7387=FACE_OUTER_BOUND ( 'NONE', #30294, .T. ) ;
#7389=CYLINDRICAL_SURFACE ( 'NONE', #8929, 47.49900000000001654 ) ;
#7390=CARTESIAN_POINT ( 'NONE',  ( -9.999999999999994671, 0.000000000000000000, 0.000000000000000000 ) ) ;
#7395=AXIS2_PLACEMENT_3D ( 'NONE', #20620, #31980, #4278 ) ;
#7397=CARTESIAN_POINT ( 'NONE',  ( 7.999999999999992895, -40.47821179127691948, -32.64221760512803172 ) ) ;
#7398=EDGE_LOOP ( 'NONE', ( #34738, #12311, #30821, #23289 ) ) ;
#7399=VECTOR ( 'NONE', #9307, 1000.000000000000000 ) ;
#7404=CARTESIAN_POINT ( 'NONE',  ( 7.999999999999992895, -6.109652351741458709, -46.58570277113513214 ) ) ;
#7405=CARTESIAN_POINT ( 'NONE',  ( 7.999999999999992895, 46.90537658765334328, -2.727856614653800804 ) ) ;
#7406=VERTEX_POINT ( 'NONE', #27451 ) ;
#7410=ORIENTED_EDGE ( 'NONE', *, *, #7425, .T. ) ;
#7411=ORIENTED_EDGE ( 'NONE', *, *, #18010, .T. ) ;
#7416=DIRECTION ( 'NONE',  ( -1.000000000000000000, 0.000000000000000000, 0.000000000000000000 ) ) ;
#7420=DIRECTION ( 'NONE',  ( 0.000000000000000000, 0.6845471059286846183, 0.7289686274214154382 ) ) ;
#7425=EDGE_CURVE ( 'NONE', #4708, #9210, #18793, .T. ) ;
#7437=CYLINDRICAL_SURFACE ( 'NONE', #1563, 20.00000000000000355 ) ;
#7438=VERTEX_POINT ( 'NONE', #32839 ) ;
#7447=CARTESIAN_POINT ( 'NONE',  ( 7.999999999999992895, -32.32520163883607722, 34.09746168776025854 ) ) ;
#7480=VERTEX_POINT ( 'NONE', #7990 ) ;
#7481=VERTEX_POINT ( 'NONE', #29433 ) ;
#7496=CARTESIAN_POINT ( 'NONE',  ( -9.999999999999994671, 0.000000000000000000, 0.000000000000000000 ) ) ;
#7501=DIRECTION ( 'NONE',  ( -1.000000000000000000, 0.000000000000000000, -0.000000000000000000 ) ) ;
#7504=CIRCLE ( 'NONE', #21920, 20.00000000000000355 ) ;
#7512=FACE_OUTER_BOUND ( 'NONE', #27935, .T. ) ;
#7516=EDGE_CURVE ( 'NONE', #4505, #8054, #26738, .T. ) ;
#7519=AXIS2_PLACEMENT_3D ( 'NONE', #1660, #1123, #4365 ) ;
#7529=VERTEX_POINT ( 'NONE', #29614 ) ;
#7532=CARTESIAN_POINT ( 'NONE',  ( 7.999999999999992895, 0.000000000000000000, 0.000000000000000000 ) ) ;
#7536=CARTESIAN_POINT ( 'NONE',  ( 7.999999999999992895, -45.78515115856053797, 12.64416602183649019 ) ) ;
#7542=DIRECTION ( 'NONE',  ( 0.000000000000000000, 0.000000000000000000, 1.000000000000000000 ) ) ;
#7549=EDGE_CURVE ( 'NONE', #19623, #453, #33190, .T. ) ;
#7551=DIRECTION ( 'NONE',  ( 0.000000000000000000, 0.000000000000000000, 1.000000000000000000 ) ) ;
#7552=EDGE_CURVE ( 'NONE', #13661, #13787, #992, .T. ) ;
#7567=VECTOR ( 'NONE', #12998, 1000.000000000000000 ) ;
#7574=ORIENTED_EDGE ( 'NONE', *, *, #29836, .T. ) ;
#7575=EDGE_LOOP ( 'NONE', ( #21540, #23839, #7355, #19749 ) ) ;
#7583=DIRECTION ( 'NONE',  ( 0.000000000000000000, 0.8443279255020164076, -0.5358267949789946583 ) ) ;
#7587=DIRECTION ( 'NONE',  ( 0.000000000000000000, 0.2486898871648483555, 0.9685831611286328524 ) ) ;
#7588=DIRECTION ( 'NONE',  ( 0.000000000000000000, 0.000000000000000000, 1.000000000000000000 ) ) ;
#7594=ORIENTED_EDGE ( 'NONE', *, *, #26167, .T. ) ;
#7597=FACE_OUTER_BOUND ( 'NONE', #26050, .T. ) ;
#7598=EDGE_LOOP ( 'NONE', ( #21202, #26690, #24766, #18163 ) ) ;
#7604=FACE_OUTER_BOUND ( 'NONE', #34444, .T. ) ;
#7609=ORIENTED_EDGE ( 'NONE', *, *, #8189, .T. ) ;
#7610=VERTEX_POINT ( 'NONE', #25268 ) ;
#7613=AXIS2_PLACEMENT_3D ( 'NONE', #32663, #19306, #35369 ) ;
#7618=EDGE_CURVE ( 'NONE', #2675, #2022, #591, .T. ) ;
#7621=AXIS2_PLACEMENT_3D ( 'NONE', #17691, #18224, #20737 ) ;
#7624=AXIS2_PLACEMENT_3D ( 'NONE', #29626, #4965, #22207 ) ;
#7634=CIRCLE ( 'NONE', #27786, 20.00000000000000711 ) ;
#7636=DIRECTION ( 'NONE',  ( 0.000000000000000000, 0.000000000000000000, 1.000000000000000000 ) ) ;
#7643=DIRECTION ( 'NONE',  ( 0.000000000000000000, 0.000000000000000000, -1.000000000000000000 ) ) ;
#7648=AXIS2_PLACEMENT_3D ( 'NONE', #16692, #30222, #21393 ) ;
#7649=ORIENTED_EDGE ( 'NONE', *, *, #10240, .F. ) ;
#7651=CIRCLE ( 'NONE', #19638, 20.00000000000000355 ) ;
#7658=ORIENTED_EDGE ( 'NONE', *, *, #17331, .F. ) ;
#7659=VERTEX_POINT ( 'NONE', #11746 ) ;
#7661=EDGE_CURVE ( 'NONE', #28491, #15607, #32597, .T. ) ;
#7666=VERTEX_POINT ( 'NONE', #25627 ) ;
#7673=DIRECTION ( 'NONE',  ( -1.000000000000000000, -0.000000000000000000, 0.000000000000000000 ) ) ;
#7682=CIRCLE ( 'NONE', #19179, 52.00000000000000711 ) ;
#7684=CARTESIAN_POINT ( 'NONE',  ( 7.999999999999992895, 0.000000000000000000, 0.000000000000000000 ) ) ;
#7688=EDGE_CURVE ( 'NONE', #540, #1374, #9595, .T. ) ;
#7690=ORIENTED_EDGE ( 'NONE', *, *, #35407, .T. ) ;
#7695=EDGE_LOOP ( 'NONE', ( #23712, #21767, #29109, #21504 ) ) ;
#7703=DIRECTION ( 'NONE',  ( 0.000000000000000000, 0.4817536741017100499, 0.8763066800438663595 ) ) ;
#7713=CARTESIAN_POINT ( 'NONE',  ( 7.999999999999992895, -35.11945359308084846, -38.34871548466050939 ) ) ;
#7723=CARTESIAN_POINT ( 'NONE',  ( 7.999999999999992895, 0.000000000000000000, 0.000000000000000000 ) ) ;
#7733=EDGE_CURVE ( 'NONE', #22530, #9085, #26280, .T. ) ;
#7736=AXIS2_PLACEMENT_3D ( 'NONE', #30487, #14162, #11295 ) ;
#7738=CIRCLE ( 'NONE', #26754, 20.00000000000000711 ) ;
#7739=EDGE_CURVE ( 'NONE', #23477, #1430, #30876, .T. ) ;
#7745=CARTESIAN_POINT ( 'NONE',  ( 0.000000000000000000, 39.64889472655731595, 33.64468972902522381 ) ) ;
#7748=EDGE_CURVE ( 'NONE', #7835, #20427, #25178, .T. ) ;
#7749=DIRECTION ( 'NONE',  ( 0.000000000000000000, 0.000000000000000000, 1.000000000000000000 ) ) ;
#7759=ADVANCED_FACE ( 'NONE', ( #22192 ), #33193, .T. ) ;
#7760=AXIS2_PLACEMENT_3D ( 'NONE', #16708, #19064, #11326 ) ;
#7764=CYLINDRICAL_SURFACE ( 'NONE', #23709, 20.00000000000000355 ) ;
#7766=AXIS2_PLACEMENT_3D ( 'NONE', #18324, #26259, #4672 ) ;
#7768=CARTESIAN_POINT ( 'NONE',  ( -9.999999999999994671, 0.000000000000000000, 0.000000000000000000 ) ) ;
#7776=ORIENTED_EDGE ( 'NONE', *, *, #10887, .F. ) ;
#7781=ADVANCED_FACE ( 'NONE', ( #18120 ), #13109, .T. ) ;
#7784=ORIENTED_EDGE ( 'NONE', *, *, #29774, .F. ) ;
#7789=VERTEX_POINT ( 'NONE', #31996 ) ;
#7795=FACE_OUTER_BOUND ( 'NONE', #20220, .T. ) ;
#7797=ORIENTED_EDGE ( 'NONE', *, *, #29587, .T. ) ;
#7799=AXIS2_PLACEMENT_3D ( 'NONE', #11209, #20174, #33700 ) ;
#7802=DIRECTION ( 'NONE',  ( -1.000000000000000000, 0.000000000000000000, 0.000000000000000000 ) ) ;
#7808=DIRECTION ( 'NONE',  ( -1.000000000000000000, 0.000000000000000000, -0.000000000000000000 ) ) ;
#7809=AXIS2_PLACEMENT_3D ( 'NONE', #16045, #26536, #12484 ) ;
#7810=CARTESIAN_POINT ( 'NONE',  ( 0.000000000000000000, -31.08872492059985859, 41.68322423723089543 ) ) ;
#7819=VERTEX_POINT ( 'NONE', #26240 ) ;
#7821=CARTESIAN_POINT ( 'NONE',  ( 4.000000000000003553, 18.53613841426789932, 48.58406706613910586 ) ) ;
#7822=CARTESIAN_POINT ( 'NONE',  ( 7.999999999999992895, -49.65209126885753221, -15.44894276735603356 ) ) ;
#7823=ADVANCED_FACE ( 'NONE', ( #4474 ), #4654, .T. ) ;
#7829=ORIENTED_EDGE ( 'NONE', *, *, #35524, .F. ) ;
#7835=VERTEX_POINT ( 'NONE', #1941 ) ;
#7838=VERTEX_POINT ( 'NONE', #21183 ) ;
#7847=AXIS2_PLACEMENT_3D ( 'NONE', #13079, #21687, #23875 ) ;
#7853=CARTESIAN_POINT ( 'NONE',  ( 7.999999999999992895, 0.000000000000000000, 0.000000000000000000 ) ) ;
#7858=DIRECTION ( 'NONE',  ( -1.000000000000000000, -0.000000000000000000, 0.000000000000000000 ) ) ;
#7865=DIRECTION ( 'NONE',  ( 0.000000000000000000, 0.000000000000000000, 1.000000000000000000 ) ) ;
#7876=DIRECTION ( 'NONE',  ( 0.000000000000000000, 0.000000000000000000, 1.000000000000000000 ) ) ;
#7907=LINE ( 'NONE', #18891, #16843 ) ;
#7909=CYLINDRICAL_SURFACE ( 'NONE', #16426, 20.00000000000000355 ) ;
#7911=EDGE_CURVE ( 'NONE', #22574, #20209, #21352, .T. ) ;
#7922=DIRECTION ( 'NONE',  ( 0.000000000000000000, 0.9822872507286879440, 0.1873813145857285423 ) ) ;
#7923=AXIS2_PLACEMENT_3D ( 'NONE', #9719, #28636, #26473 ) ;
#7930=CARTESIAN_POINT ( 'NONE',  ( 7.999999999999992895, 35.11945359308111847, 38.34871548466027491 ) ) ;
#7932=VERTEX_POINT ( 'NONE', #13800 ) ;
#7937=ORIENTED_EDGE ( 'NONE', *, *, #33983, .F. ) ;
#7966=CARTESIAN_POINT ( 'NONE',  ( 7.999999999999992895, -6.109652351742118626, 46.58570277113506819 ) ) ;
#7968=EDGE_LOOP ( 'NONE', ( #34520, #2771, #11921, #15688 ) ) ;
#7975=EDGE_CURVE ( 'NONE', #12363, #22667, #26970, .T. ) ;
#7982=SHAPE_REPRESENTATION ( 'spur gear_iso_ISO - Spur gear 2M 50T 20PA 8FW ---S50A75H50L22.0R1', ( #21307 ), #32275 ) ;
#7990=CARTESIAN_POINT ( 'NONE',  ( 7.999999999999992895, -0.6505223195679143977, -51.99593080916758936 ) ) ;
#7998=CARTESIAN_POINT ( 'NONE',  ( 4.000000000000003553, 13.56094713063571078, 50.20060470671747055 ) ) ;
#8000=EDGE_CURVE ( 'NONE', #25742, #28491, #13111, .T. ) ;
#8006=FACE_OUTER_BOUND ( 'NONE', #15206, .T. ) ;
#8008=AXIS2_PLACEMENT_3D ( 'NONE', #14237, #33678, #9013 ) ;
#8014=CARTESIAN_POINT ( 'NONE',  ( 7.999999999999992895, -44.61570720899084819, -14.73072383765613935 ) ) ;
#8018=ORIENTED_EDGE ( 'NONE', *, *, #21518, .F. ) ;
#8021=VERTEX_POINT ( 'NONE', #13969 ) ;
#8036=CIRCLE ( 'NONE', #28754, 47.49900000000001654 ) ;
#8038=CARTESIAN_POINT ( 'NONE',  ( 7.999999999999992895, 0.000000000000000000, 0.000000000000000000 ) ) ;
#8039=DIRECTION ( 'NONE',  ( 0.000000000000000000, -0.7705132427757949154, 0.6374239897486828621 ) ) ;
#8046=ORIENTED_EDGE ( 'NONE', *, *, #21473, .T. ) ;
#8054=VERTEX_POINT ( 'NONE', #11269 ) ;
#8056=VERTEX_POINT ( 'NONE', #22071 ) ;
#8066=EDGE_CURVE ( 'NONE', #29366, #1167, #19401, .T. ) ;
#8082=DIRECTION ( 'NONE',  ( -1.000000000000000000, 0.000000000000000000, 0.000000000000000000 ) ) ;
#8090=DIRECTION ( 'NONE',  ( 0.000000000000000000, 0.8443279255020164076, -0.5358267949789946583 ) ) ;
#8094=CARTESIAN_POINT ( 'NONE',  ( 0.000000000000000000, 0.000000000000000000, 0.000000000000000000 ) ) ;
#8098=FACE_OUTER_BOUND ( 'NONE', #17463, .T. ) ;
#8102=CARTESIAN_POINT ( 'NONE',  ( 0.000000000000000000, -47.00885577955408223, -6.806061952192771436 ) ) ;
#8110=EDGE_CURVE ( 'NONE', #31137, #10989, #22413, .T. ) ;
#8118=DIRECTION ( 'NONE',  ( 1.000000000000000000, 0.000000000000000000, 0.000000000000000000 ) ) ;
#8126=VECTOR ( 'NONE', #28828, 1000.000000000000000 ) ;
#8131=LINE ( 'NONE', #2048, #26651 ) ;
#8140=EDGE_CURVE ( 'NONE', #11039, #21916, #30349, .T. ) ;
#8143=ORIENTED_EDGE ( 'NONE', *, *, #29104, .T. ) ;
#8146=LINE ( 'NONE', #15891, #9494 ) ;
#8148=VERTEX_POINT ( 'NONE', #30280 ) ;
#8150=CARTESIAN_POINT ( 'NONE',  ( 7.999999999999992895, -32.00046193115173310, 34.40241257139674502 ) ) ;
#8151=EDGE_CURVE ( 'NONE', #128, #29395, #35031, .T. ) ;
#8155=AXIS2_PLACEMENT_3D ( 'NONE', #12361, #9667, #20624 ) ;
#8156=DIRECTION ( 'NONE',  ( -1.000000000000000000, 0.000000000000000000, -0.000000000000000000 ) ) ;
#8166=VECTOR ( 'NONE', #22378, 1000.000000000000000 ) ;
#8167=CARTESIAN_POINT ( 'NONE',  ( 7.999999999999992895, -13.85708833600001277, 45.43276465116660745 ) ) ;
#8170=CYLINDRICAL_SURFACE ( 'NONE', #16517, 20.00000000000000355 ) ;
#8171=DIRECTION ( 'NONE',  ( 0.000000000000000000, 0.000000000000000000, 1.000000000000000000 ) ) ;
#8172=CARTESIAN_POINT ( 'NONE',  ( 0.000000000000000000, -19.74581912682808493, -48.10512059033414545 ) ) ;
#8173=CARTESIAN_POINT ( 'NONE',  ( 7.999999999999992895, 40.47821179127715396, 32.64221760512774040 ) ) ;
#8174=ORIENTED_EDGE ( 'NONE', *, *, #11371, .F. ) ;
#8175=DIRECTION ( 'NONE',  ( 0.000000000000000000, -0.8443279255020087470, -0.5358267949790064266 ) ) ;
#8177=AXIS2_PLACEMENT_3D ( 'NONE', #34987, #13718, #10308 ) ;
#8188=DIRECTION ( 'NONE',  ( 0.000000000000000000, 0.000000000000000000, 1.000000000000000000 ) ) ;
#8189=EDGE_CURVE ( 'NONE', #11629, #10719, #32562, .T. ) ;
#8191=ORIENTED_EDGE ( 'NONE', *, *, #19560, .T. ) ;
#8197=ORIENTED_EDGE ( 'NONE', *, *, #5932, .T. ) ;
#8200=EDGE_CURVE ( 'NONE', #30516, #15107, #10814, .T. ) ;
#8204=AXIS2_PLACEMENT_3D ( 'NONE', #16443, #35381, #11067 ) ;
#8208=DIRECTION ( 'NONE',  ( -1.000000000000000000, -0.000000000000000000, -0.000000000000000000 ) ) ;
#8224=LINE ( 'NONE', #27514, #1524 ) ;
#8226=EDGE_CURVE ( 'NONE', #14995, #4091, #902, .T. ) ;
#8230=DIRECTION ( 'NONE',  ( 1.000000000000000000, 0.000000000000000000, 0.000000000000000000 ) ) ;
#8238=EDGE_CURVE ( 'NONE', #9311, #33836, #23039, .T. ) ;
#8240=DIRECTION ( 'NONE',  ( 1.000000000000000000, -0.000000000000000000, -0.000000000000000000 ) ) ;
#8250=AXIS2_PLACEMENT_3D ( 'NONE', #20231, #11983, #17361 ) ;
#8254=CARTESIAN_POINT ( 'NONE',  ( 0.000000000000000000, 0.000000000000000000, 0.000000000000000000 ) ) ;
#8267=CIRCLE ( 'NONE', #32415, 20.00000000000000711 ) ;
#8269=EDGE_CURVE ( 'NONE', #31708, #22574, #3255, .T. ) ;
#8270=CYLINDRICAL_SURFACE ( 'NONE', #10261, 20.00000000000000711 ) ;
#8271=LINE ( 'NONE', #32417, #10577 ) ;
#8282=ORIENTED_EDGE ( 'NONE', *, *, #19989, .T. ) ;
#8283=VERTEX_POINT ( 'NONE', #14401 ) ;
#8286=ORIENTED_EDGE ( 'NONE', *, *, #18141, .F. ) ;
#8289=CARTESIAN_POINT ( 'NONE',  ( 4.000000000000003553, 12.30077720129095553, 50.52416135122086871 ) ) ;
#8290=CARTESIAN_POINT ( 'NONE',  ( 7.999999999999992895, 0.000000000000000000, 0.000000000000000000 ) ) ;
#8292=CARTESIAN_POINT ( 'NONE',  ( 4.000000000000003553, 5.871425383722286284, -51.66745943012276854 ) ) ;
#8294=DIRECTION ( 'NONE',  ( 1.000000000000000000, 0.000000000000000000, 0.000000000000000000 ) ) ;
#8296=AXIS2_PLACEMENT_3D ( 'NONE', #14332, #8580, #3554 ) ;
#8301=CIRCLE ( 'NONE', #21526, 20.00000000000000711 ) ;
#8302=ORIENTED_EDGE ( 'NONE', *, *, #17452, .T. ) ;
#8304=ORIENTED_EDGE ( 'NONE', *, *, #12355, .F. ) ;
#8310=VERTEX_POINT ( 'NONE', #31680 ) ;
#8323=DIRECTION ( 'NONE',  ( 0.000000000000000000, 0.000000000000000000, 1.000000000000000000 ) ) ;
#8327=AXIS2_PLACEMENT_3D ( 'NONE', #35430, #16498, #11460 ) ;
#8334=ADVANCED_FACE ( 'NONE', ( #11704 ), #9002, .T. ) ;
#8338=CYLINDRICAL_SURFACE ( 'NONE', #800, 20.00000000000000711 ) ;
#8339=ORIENTED_EDGE ( 'NONE', *, *, #35310, .F. ) ;
#8341=CARTESIAN_POINT ( 'NONE',  ( 0.000000000000000000, 19.74581912682842244, 48.10512059033400334 ) ) ;
#8344=DIRECTION ( 'NONE',  ( 0.000000000000000000, 0.000000000000000000, 1.000000000000000000 ) ) ;
#8353=CARTESIAN_POINT ( 'NONE',  ( 0.000000000000000000, -5.871425383721907920, 51.66745943012281117 ) ) ;
#8357=DIRECTION ( 'NONE',  ( -1.000000000000000000, -0.000000000000000000, -0.000000000000000000 ) ) ;
#8358=DIRECTION ( 'NONE',  ( -1.000000000000000000, 0.000000000000000000, 0.000000000000000000 ) ) ;
#8359=CARTESIAN_POINT ( 'NONE',  ( 7.999999999999992895, 47.00885577955413908, 6.806061952192451692 ) ) ;
#8368=ORIENTED_EDGE ( 'NONE', *, *, #31705, .F. ) ;
#8373=DIRECTION ( 'NONE',  ( -1.000000000000000000, -0.000000000000000000, 0.000000000000000000 ) ) ;
#8383=CARTESIAN_POINT ( 'NONE',  ( 0.000000000000000000, -39.78933988720095982, -24.98727647985043987 ) ) ;
#8386=CIRCLE ( 'NONE', #11275, 20.00000000000000711 ) ;
#8388=AXIS2_PLACEMENT_3D ( 'NONE', #23362, #15424, #32005 ) ;
#8393=SURFACE_STYLE_FILL_AREA ( #9859 ) ;
#8398=CARTESIAN_POINT ( 'NONE',  ( 0.000000000000000000, 25.61928775981107265, -45.25098998563451147 ) ) ;
#8402=ORIENTED_EDGE ( 'NONE', *, *, #11892, .F. ) ;
#8405=CIRCLE ( 'NONE', #19317, 47.49900000000001654 ) ;
#8407=EDGE_LOOP ( 'NONE', ( #20741, #3838, #26322, #9175 ) ) ;
#8408=ORIENTED_EDGE ( 'NONE', *, *, #15624, .T. ) ;
#8412=CIRCLE ( 'NONE', #9579, 20.00000000000000711 ) ;
#8419=ORIENTED_EDGE ( 'NONE', *, *, #877, .T. ) ;
#8420=CARTESIAN_POINT ( 'NONE',  ( 7.999999999999992895, 0.000000000000000000, 0.000000000000000000 ) ) ;
#8422=ORIENTED_EDGE ( 'NONE', *, *, #25928, .F. ) ;
#8424=ADVANCED_FACE ( 'NONE', ( #13326 ), #10616, .T. ) ;
#8430=EDGE_CURVE ( 'NONE', #13072, #6142, #26658, .T. ) ;
#8435=ORIENTED_EDGE ( 'NONE', *, *, #4246, .T. ) ;
#8436=AXIS2_PLACEMENT_3D ( 'NONE', #33251, #8570, #5877 ) ;
#8440=CARTESIAN_POINT ( 'NONE',  ( 7.999999999999992895, 0.000000000000000000, 0.000000000000000000 ) ) ;
#8441=CARTESIAN_POINT ( 'NONE',  ( 7.999999999999992895, 17.08890430202750110, 43.76671000081951490 ) ) ;
#8443=FACE_OUTER_BOUND ( 'NONE', #17658, .T. ) ;
#8449=DIRECTION ( 'NONE',  ( 0.000000000000000000, 0.000000000000000000, 1.000000000000000000 ) ) ;
#8452=EDGE_LOOP ( 'NONE', ( #1959, #4903, #28912, #5813 ) ) ;
#8456=ORIENTED_EDGE ( 'NONE', *, *, #7552, .T. ) ;
#8474=AXIS2_PLACEMENT_3D ( 'NONE', #22220, #14292, #11248 ) ;
#8489=ORIENTED_EDGE ( 'NONE', *, *, #25488, .F. ) ;
#8492=AXIS2_PLACEMENT_3D ( 'NONE', #29840, #5181, #16120 ) ;
#8496=DIRECTION ( 'NONE',  ( 0.000000000000000000, -0.9510565162951500895, -0.3090169943749581649 ) ) ;
#8497=ORIENTED_EDGE ( 'NONE', *, *, #27350, .T. ) ;
#8516=CIRCLE ( 'NONE', #29821, 20.00000000000001066 ) ;
#8525=CARTESIAN_POINT ( 'NONE',  ( 7.999999999999992895, 0.000000000000000000, 0.000000000000000000 ) ) ;
#8527=ADVANCED_FACE ( 'NONE', ( #31860 ), #5052, .T. ) ;
#8533=DIRECTION ( 'NONE',  ( 0.000000000000000000, 0.000000000000000000, -1.000000000000000000 ) ) ;
#8545=ORIENTED_EDGE ( 'NONE', *, *, #3781, .F. ) ;
#8550=DIRECTION ( 'NONE',  ( -1.000000000000000000, 0.000000000000000000, 0.000000000000000000 ) ) ;
#8558=CARTESIAN_POINT ( 'NONE',  ( 7.999999999999992895, 0.000000000000000000, 0.000000000000000000 ) ) ;
#8559=CARTESIAN_POINT ( 'NONE',  ( 4.000000000000003553, -50.95304419620817526, -10.38206564895716255 ) ) ;
#8561=AXIS2_PLACEMENT_3D ( 'NONE', #5823, #22364, #25447 ) ;
#8563=EDGE_CURVE ( 'NONE', #28842, #9210, #8985, .T. ) ;
#8567=DIRECTION ( 'NONE',  ( 0.000000000000000000, 0.000000000000000000, 1.000000000000000000 ) ) ;
#8570=DIRECTION ( 'NONE',  ( -1.000000000000000000, -0.000000000000000000, 0.000000000000000000 ) ) ;
#8571=CARTESIAN_POINT ( 'NONE',  ( 0.000000000000000000, 0.000000000000000000, 0.000000000000000000 ) ) ;
#8576=CARTESIAN_POINT ( 'NONE',  ( 7.999999999999992895, 0.000000000000000000, 0.000000000000000000 ) ) ;
#8578=ORIENTED_EDGE ( 'NONE', *, *, #8796, .T. ) ;
#8580=DIRECTION ( 'NONE',  ( -1.000000000000000000, -0.000000000000000000, -0.000000000000000000 ) ) ;
#8585=DIRECTION ( 'NONE',  ( 0.000000000000000000, -0.5877852522924801315, 0.8090169943749422332 ) ) ;
#8589=ORIENTED_EDGE ( 'NONE', *, *, #4009, .T. ) ;
#8606=DIRECTION ( 'NONE',  ( 0.000000000000000000, 0.1253332335642974860, 0.9921147013144787641 ) ) ;
#8607=CARTESIAN_POINT ( 'NONE',  ( 0.000000000000000000, 25.61928775981044026, 45.25098998563487385 ) ) ;
#8609=DIRECTION ( 'NONE',  ( 0.000000000000000000, -0.9048270524660146918, -0.4257792915650830956 ) ) ;
#8612=DIRECTION ( 'NONE',  ( 0.000000000000000000, -0.1253332335643113082, 0.9921147013144769877 ) ) ;
#8613=VERTEX_POINT ( 'NONE', #33110 ) ;
#8617=AXIS2_PLACEMENT_3D ( 'NONE', #320, #5561, #32923 ) ;
#8621=VERTEX_POINT ( 'NONE', #329 ) ;
#8626=DIRECTION ( 'NONE',  ( 1.000000000000000000, 0.000000000000000000, -0.000000000000000000 ) ) ;
#8630=EDGE_LOOP ( 'NONE', ( #10739, #30864, #30559, #26776 ) ) ;
#8632=AXIS2_PLACEMENT_3D ( 'NONE', #15902, #27266, #35558 ) ;
#8643=CIRCLE ( 'NONE', #9803, 52.00000000000000711 ) ;
#8649=DIRECTION ( 'NONE',  ( -1.000000000000000000, 0.000000000000000000, 0.000000000000000000 ) ) ;
#8655=ORIENTED_EDGE ( 'NONE', *, *, #1703, .T. ) ;
#8656=VERTEX_POINT ( 'NONE', #3052 ) ;
#8662=ORIENTED_EDGE ( 'NONE', *, *, #8840, .F. ) ;
#8664=CARTESIAN_POINT ( 'NONE',  ( 4.000000000000003553, -19.74581912682874929, 48.10512059033386834 ) ) ;
#8676=EDGE_LOOP ( 'NONE', ( #1244, #15355, #1148, #22106 ) ) ;
#8679=VERTEX_POINT ( 'NONE', #22819 ) ;
#8682=CARTESIAN_POINT ( 'NONE',  ( 7.999999999999992895, -44.47301969247457976, 16.68249143361895293 ) ) ;
#8686=DIRECTION ( 'NONE',  ( 0.000000000000000000, -0.9048270524660235736, 0.4257792915650639998 ) ) ;
#8688=LINE ( 'NONE', #31016, #17855 ) ;
#8694=DIRECTION ( 'NONE',  ( -1.000000000000000000, 0.000000000000000000, 0.000000000000000000 ) ) ;
#8699=DIRECTION ( 'NONE',  ( -1.000000000000000000, -0.000000000000000000, -0.000000000000000000 ) ) ;
#8705=CARTESIAN_POINT ( 'NONE',  ( 4.000000000000003553, 25.61928775981044026, 45.25098998563487385 ) ) ;
#8709=EDGE_CURVE ( 'NONE', #17425, #20467, #23390, .T. ) ;
#8718=ORIENTED_EDGE ( 'NONE', *, *, #8805, .T. ) ;
#8725=DIRECTION ( 'NONE',  ( -1.000000000000000000, -0.000000000000000000, -0.000000000000000000 ) ) ;
#8732=CIRCLE ( 'NONE', #33472, 47.49900000000001654 ) ;
#8742=DIRECTION ( 'NONE',  ( 1.000000000000000000, 0.000000000000000000, 0.000000000000000000 ) ) ;
#8750=EDGE_LOOP ( 'NONE', ( #3635, #10679, #31101, #8018 ) ) ;
#8751=ADVANCED_FACE ( 'NONE', ( #25724 ), #34178, .T. ) ;
#8755=CIRCLE ( 'NONE', #13385, 20.00000000000000355 ) ;
#8756=FACE_OUTER_BOUND ( 'NONE', #15675, .T. ) ;
#8764=CYLINDRICAL_SURFACE ( 'NONE', #8617, 47.49900000000001654 ) ;
#8769=CARTESIAN_POINT ( 'NONE',  ( 7.999999999999992895, 0.000000000000000000, 0.000000000000000000 ) ) ;
#8779=CARTESIAN_POINT ( 'NONE',  ( 50.00005079999998969, 0.000000000000000000, 11.00000000000000000 ) ) ;
#8781=DIRECTION ( 'NONE',  ( -1.000000000000000000, 0.000000000000000000, 0.000000000000000000 ) ) ;
#8782=CIRCLE ( 'NONE', #17387, 52.00000000000000711 ) ;
#8784=CIRCLE ( 'NONE', #19692, 20.00000000000000711 ) ;
#8790=ORIENTED_EDGE ( 'NONE', *, *, #34637, .T. ) ;
#8796=EDGE_CURVE ( 'NONE', #27467, #32382, #24561, .T. ) ;
#8801=DIRECTION ( 'NONE',  ( -1.000000000000000000, 0.000000000000000000, 0.000000000000000000 ) ) ;
#8804=CARTESIAN_POINT ( 'NONE',  ( 7.999999999999992895, 11.90021268425554624, 45.45261810511217959 ) ) ;
#8805=EDGE_CURVE ( 'NONE', #4061, #11629, #22809, .T. ) ;
#8809=ORIENTED_EDGE ( 'NONE', *, *, #973, .F. ) ;
#8818=DIRECTION ( 'NONE',  ( -1.000000000000000000, -0.000000000000000000, 0.000000000000000000 ) ) ;
#8825=CARTESIAN_POINT ( 'NONE',  ( 7.999999999999992895, -44.75336757549767697, -14.30704879393654494 ) ) ;
#8828=ORIENTED_EDGE ( 'NONE', *, *, #28851, .F. ) ;
#8834=ORIENTED_EDGE ( 'NONE', *, *, #30037, .F. ) ;
#8836=VECTOR ( 'NONE', #26744, 1000.000000000000000 ) ;
#8838=CARTESIAN_POINT ( 'NONE',  ( 0.000000000000000000, 0.000000000000000000, 0.000000000000000000 ) ) ;
#8840=EDGE_CURVE ( 'NONE', #1331, #17998, #14769, .T. ) ;
#8844=ORIENTED_EDGE ( 'NONE', *, *, #15774, .F. ) ;
#8846=CARTESIAN_POINT ( 'NONE',  ( 7.999999999999992895, -22.82995208772657492, -41.06517797613687293 ) ) ;
#8853=CARTESIAN_POINT ( 'NONE',  ( 0.000000000000000000, 8.053585752062575764, -46.81126742072014224 ) ) ;
#8854=AXIS2_PLACEMENT_3D ( 'NONE', #8525, #14445, #32351 ) ;
#8859=ORIENTED_EDGE ( 'NONE', *, *, #22905, .T. ) ;
#8862=AXIS2_PLACEMENT_3D ( 'NONE', #32727, #18504, #4677 ) ;
#8868=ADVANCED_FACE ( 'NONE', ( #18662 ), #20814, .T. ) ;
#8870=FACE_OUTER_BOUND ( 'NONE', #25063, .T. ) ;
#8876=CARTESIAN_POINT ( 'NONE',  ( 7.999999999999992895, -5.667686777401384823, -46.64153600743608763 ) ) ;
#8889=CARTESIAN_POINT ( 'NONE',  ( 7.999999999999992895, 42.60732521687570795, 19.80331771201672453 ) ) ;
#8891=CARTESIAN_POINT ( 'NONE',  ( 7.999999999999992895, 43.83938735307269496, 18.28286404005814703 ) ) ;
#8892=CARTESIAN_POINT ( 'NONE',  ( 0.000000000000000000, -42.60732521687556584, -19.80331771201704427 ) ) ;
#8893=EDGE_LOOP ( 'NONE', ( #23925, #10419, #34822, #18139 ) ) ;
#8896=CIRCLE ( 'NONE', #18095, 20.00000000000000711 ) ;
#8910=PRODUCT ( 'spur gear_iso_ISO - Spur gear 2M 50T 20PA 8FW ---S50A75H50L22.0R1', 'spur gear_iso_ISO - Spur gear 2M 50T 20PA 8FW ---S50A75H50L22.0R1', '', ( #12010 ) ) ;
#8912=CARTESIAN_POINT ( 'NONE',  ( 7.999999999999992895, 43.83938735307295076, -18.28286404005752175 ) ) ;
#8916=AXIS2_PLACEMENT_3D ( 'NONE', #11079, #16636, #22045 ) ;
#8927=DIRECTION ( 'NONE',  ( -1.000000000000000000, 0.000000000000000000, 0.000000000000000000 ) ) ;
#8928=VERTEX_POINT ( 'NONE', #26433 ) ;
#8929=AXIS2_PLACEMENT_3D ( 'NONE', #23590, #4709, #13331 ) ;
#8930=ORIENTED_EDGE ( 'NONE', *, *, #18067, .T. ) ;
#8941=ORIENTED_EDGE ( 'NONE', *, *, #13862, .T. ) ;
#8943=DIRECTION ( 'NONE',  ( -1.000000000000000000, -0.000000000000000000, -0.000000000000000000 ) ) ;
#8946=DIRECTION ( 'NONE',  ( -1.000000000000000000, 0.000000000000000000, -0.000000000000000000 ) ) ;
#8951=APPLICATION_CONTEXT ( 'automotive_design' ) ;
#8955=CARTESIAN_POINT ( 'NONE',  ( 0.000000000000000000, -26.17370628620682638, 39.63700417846155233 ) ) ;
#8967=AXIS2_PLACEMENT_3D ( 'NONE', #6139, #8294, #13886 ) ;
#8969=CIRCLE ( 'NONE', #24492, 20.00000000000001066 ) ;
#8971=ORIENTED_EDGE ( 'NONE', *, *, #6529, .T. ) ;
#8972=VERTEX_POINT ( 'NONE', #34357 ) ;
#8979=CARTESIAN_POINT ( 'NONE',  ( 7.999999999999992895, 0.000000000000000000, 0.000000000000000000 ) ) ;
#8981=ORIENTED_EDGE ( 'NONE', *, *, #26888, .F. ) ;
#8985=CIRCLE ( 'NONE', #33719, 47.49900000000001654 ) ;
#8990=DIRECTION ( 'NONE',  ( 0.000000000000000000, 0.000000000000000000, 1.000000000000000000 ) ) ;
#9002=PLANE ( 'NONE',  #28056 ) ;
#9007=DIRECTION ( 'NONE',  ( 0.000000000000000000, 0.000000000000000000, 1.000000000000000000 ) ) ;
#9013=DIRECTION ( 'NONE',  ( 0.000000000000000000, 0.9048270524660205760, -0.4257792915650702170 ) ) ;
#9028=ORIENTED_EDGE ( 'NONE', *, *, #28412, .T. ) ;
#9038=FACE_OUTER_BOUND ( 'NONE', #30589, .T. ) ;
#9044=PRODUCT_DEFINITION_CONTEXT ( 'detailed design', #8951, 'design' ) ;
#9046=CYLINDRICAL_SURFACE ( 'NONE', #11446, 47.49900000000001654 ) ;
#9053=CARTESIAN_POINT ( 'NONE',  ( 7.999999999999992895, -39.78933988720095982, -24.98727647985043987 ) ) ;
#9054=EDGE_CURVE ( 'NONE', #26454, #19047, #13625, .T. ) ;
#9066=VERTEX_POINT ( 'NONE', #19192 ) ;
#9068=CARTESIAN_POINT ( 'NONE',  ( 0.000000000000000000, 44.61570720899074161, 14.73072383765644489 ) ) ;
#9075=CARTESIAN_POINT ( 'NONE',  ( 7.999999999999992895, -8.053585752061602321, -46.81126742072033409 ) ) ;
#9076=DIRECTION ( 'NONE',  ( 0.000000000000000000, 0.6845471059286846183, 0.7289686274214152162 ) ) ;
#9084=ORIENTED_EDGE ( 'NONE', *, *, #19363, .F. ) ;
#9085=VERTEX_POINT ( 'NONE', #30191 ) ;
#9086=CARTESIAN_POINT ( 'NONE',  ( 0.000000000000000000, -30.93515269692089120, -36.04401931830286543 ) ) ;
#9088=AXIS2_PLACEMENT_3D ( 'NONE', #32370, #8230, #35269 ) ;
#9093=CYLINDRICAL_SURFACE ( 'NONE', #12606, 52.00000000000000711 ) ;
#9099=CARTESIAN_POINT ( 'NONE',  ( 7.999999999999992895, 26.17370628620710349, -39.63700417846138890 ) ) ;
#9106=CARTESIAN_POINT ( 'NONE',  ( 0.000000000000000000, 35.11945359308164427, -38.34871548465979174 ) ) ;
#9115=DIRECTION ( 'NONE',  ( 0.000000000000000000, -0.4817536741017223179, 0.8763066800438598092 ) ) ;
#9122=ORIENTED_EDGE ( 'NONE', *, *, #29873, .F. ) ;
#9123=EDGE_CURVE ( 'NONE', #6690, #28558, #29195, .T. ) ;
#9135=EDGE_LOOP ( 'NONE', ( #32880, #2929, #23600, #22125 ) ) ;
#9139=DIRECTION ( 'NONE',  ( 0.000000000000000000, 0.000000000000000000, 1.000000000000000000 ) ) ;
#9146=CYLINDRICAL_SURFACE ( 'NONE', #11830, 52.00000000000000711 ) ;
#9148=ORIENTED_EDGE ( 'NONE', *, *, #14940, .F. ) ;
#9155=VECTOR ( 'NONE', #7416, 1000.000000000000000 ) ;
#9157=DIRECTION ( 'NONE',  ( -1.000000000000000000, -0.000000000000000000, 0.000000000000000000 ) ) ;
#9159=ORIENTED_EDGE ( 'NONE', *, *, #23573, .T. ) ;
#9161=CIRCLE ( 'NONE', #13778, 47.49900000000001654 ) ;
#9168=LINE ( 'NONE', #20132, #23642 ) ;
#9175=ORIENTED_EDGE ( 'NONE', *, *, #25127, .F. ) ;
#9179=DIRECTION ( 'NONE',  ( 0.000000000000000000, 0.000000000000000000, 1.000000000000000000 ) ) ;
#9181=( GEOMETRIC_REPRESENTATION_CONTEXT ( 3 ) GLOBAL_UNCERTAINTY_ASSIGNED_CONTEXT ( ( #20058 ) ) GLOBAL_UNIT_ASSIGNED_CONTEXT ( ( #24441, #21903, #5534 ) ) REPRESENTATION_CONTEXT ( 'NONE', 'WORKASPACE' ) );
#9182=CYLINDRICAL_SURFACE ( 'NONE', #10032, 20.00000000000000355 ) ;
#9185=DIRECTION ( 'NONE',  ( 0.000000000000000000, 0.8443279255020126328, 0.5358267949790005424 ) ) ;
#9188=ORIENTED_EDGE ( 'NONE', *, *, #12717, .F. ) ;
#9191=ORIENTED_EDGE ( 'NONE', *, *, #15817, .F. ) ;
#9202=VECTOR ( 'NONE', #29259, 1000.000000000000000 ) ;
#9210=VERTEX_POINT ( 'NONE', #32893 ) ;
#9223=ORIENTED_EDGE ( 'NONE', *, *, #16151, .F. ) ;
#9225=DIRECTION ( 'NONE',  ( -1.000000000000000000, 0.000000000000000000, 0.000000000000000000 ) ) ;
#9229=DIRECTION ( 'NONE',  ( -1.000000000000000000, -0.000000000000000000, -0.000000000000000000 ) ) ;
#9236=AXIS2_PLACEMENT_3D ( 'NONE', #28869, #1873, #31915 ) ;
#9239=DIRECTION ( 'NONE',  ( -1.000000000000000000, 0.000000000000000000, 0.000000000000000000 ) ) ;
#9240=AXIS2_PLACEMENT_3D ( 'NONE', #2743, #27390, #18915 ) ;
#9242=EDGE_CURVE ( 'NONE', #29785, #6500, #25145, .T. ) ;
#9246=CARTESIAN_POINT ( 'NONE',  ( 0.000000000000000000, 47.00885577955413908, 6.806061952192451692 ) ) ;
#9252=DIRECTION ( 'NONE',  ( 0.000000000000000000, 0.000000000000000000, 1.000000000000000000 ) ) ;
#9260=ADVANCED_FACE ( 'NONE', ( #3537 ), #14663, .T. ) ;
#9264=DIRECTION ( 'NONE',  ( 0.000000000000000000, -1.000000000000000000, -0.000000000000000000 ) ) ;
#9266=VECTOR ( 'NONE', #22881, 1000.000000000000000 ) ;
#9281=CARTESIAN_POINT ( 'NONE',  ( 7.999999999999992895, 0.000000000000000000, 0.000000000000000000 ) ) ;
#9291=ADVANCED_FACE ( 'NONE', ( #32311 ), #26567, .T. ) ;
#9301=EDGE_CURVE ( 'NONE', #17256, #31962, #6174, .T. ) ;
#9303=EDGE_CURVE ( 'NONE', #1167, #3384, #5317, .T. ) ;
#9307=DIRECTION ( 'NONE',  ( -1.000000000000000000, 0.000000000000000000, -0.000000000000000000 ) ) ;
#9309=ADVANCED_FACE ( 'NONE', ( #30149 ), #13936, .T. ) ;
#9311=VERTEX_POINT ( 'NONE', #22202 ) ;
#9315=EDGE_LOOP ( 'NONE', ( #15933, #15471, #33876, #33302 ) ) ;
#9330=ADVANCED_FACE ( 'NONE', ( #13582 ), #8170, .T. ) ;
#9339=CIRCLE ( 'NONE', #4197, 47.49900000000000944 ) ;
#9345=ADVANCED_FACE ( 'NONE', ( #16626 ), #24393, .T. ) ;
#9346=CARTESIAN_POINT ( 'NONE',  ( 0.000000000000000000, -40.47821179127737423, 32.64221760512746329 ) ) ;
#9352=ORIENTED_EDGE ( 'NONE', *, *, #20078, .F. ) ;
#9354=DIRECTION ( 'NONE',  ( 0.000000000000000000, 0.000000000000000000, 1.000000000000000000 ) ) ;
#9355=VERTEX_POINT ( 'NONE', #8341 ) ;
#9361=FACE_OUTER_BOUND ( 'NONE', #9963, .T. ) ;
#9364=CARTESIAN_POINT ( 'NONE',  ( 7.999999999999992895, 46.87740477351712798, 3.172455868806031809 ) ) ;
#9376=LINE ( 'NONE', #34228, #15899 ) ;
#9382=ORIENTED_EDGE ( 'NONE', *, *, #29836, .F. ) ;
#9387=CIRCLE ( 'NONE', #32967, 20.00000000000000355 ) ;
#9388=ORIENTED_EDGE ( 'NONE', *, *, #15653, .T. ) ;
#9389=VERTEX_POINT ( 'NONE', #21857 ) ;
#9392=CARTESIAN_POINT ( 'NONE',  ( 0.000000000000000000, 0.000000000000000000, 0.000000000000000000 ) ) ;
#9393=ORIENTED_EDGE ( 'NONE', *, *, #20447, .F. ) ;
#9403=DIRECTION ( 'NONE',  ( 1.000000000000000000, 0.000000000000000000, -0.000000000000000000 ) ) ;
#9407=DIRECTION ( 'NONE',  ( -1.000000000000000000, 0.000000000000000000, 0.000000000000000000 ) ) ;
#9408=AXIS2_PLACEMENT_3D ( 'NONE', #21776, #4886, #32771 ) ;
#9421=CARTESIAN_POINT ( 'NONE',  ( 7.999999999999992895, -46.90537658765333617, 2.727856614654147638 ) ) ;
#9422=CARTESIAN_POINT ( 'NONE',  ( 0.000000000000000000, 27.79676263918186052, 37.88001506494778425 ) ) ;
#9424=DIRECTION ( 'NONE',  ( -1.000000000000000000, 0.000000000000000000, 0.000000000000000000 ) ) ;
#9430=EDGE_LOOP ( 'NONE', ( #3803, #141, #4500, #11157 ) ) ;
#9431=FILL_AREA_STYLE_COLOUR ( '', #28830 ) ;
#9436=CIRCLE ( 'NONE', #236, 20.00000000000000355 ) ;
#9437=CARTESIAN_POINT ( 'NONE',  ( 0.000000000000000000, 39.78933988720114456, 24.98727647985016276 ) ) ;
#9451=DIRECTION ( 'NONE',  ( -1.000000000000000000, 0.000000000000000000, -0.000000000000000000 ) ) ;
#9460=DIRECTION ( 'NONE',  ( 0.000000000000000000, 0.000000000000000000, 1.000000000000000000 ) ) ;
#9464=CARTESIAN_POINT ( 'NONE',  ( 7.999999999999992895, 29.60891106212789126, 37.14118181634776050 ) ) ;
#9480=EDGE_CURVE ( 'NONE', #30694, #23286, #17681, .T. ) ;
#9481=CARTESIAN_POINT ( 'NONE',  ( 0.000000000000000000, 49.65209126885784485, -15.44894276735497840 ) ) ;
#9489=VERTEX_POINT ( 'NONE', #23087 ) ;
#9493=DIRECTION ( 'NONE',  ( 1.000000000000000000, -0.000000000000000000, -0.000000000000000000 ) ) ;
#9494=VECTOR ( 'NONE', #16061, 1000.000000000000000 ) ;
#9500=EDGE_CURVE ( 'NONE', #32704, #8928, #33217, .T. ) ;
#9502=DIRECTION ( 'NONE',  ( 0.000000000000000000, -0.3681245526846853022, 0.9297764858882484607 ) ) ;
#9504=VECTOR ( 'NONE', #1447, 1000.000000000000000 ) ;
#9505=DIRECTION ( 'NONE',  ( -1.000000000000000000, -0.000000000000000000, 0.000000000000000000 ) ) ;
#9507=CARTESIAN_POINT ( 'NONE',  ( 7.999999999999992895, -35.11945359308137427, 38.34871548466002622 ) ) ;
#9512=EDGE_CURVE ( 'NONE', #1926, #34437, #32652, .T. ) ;
#9520=ORIENTED_EDGE ( 'NONE', *, *, #28690, .F. ) ;
#9521=VECTOR ( 'NONE', #27286, 1000.000000000000000 ) ;
#9526=EDGE_CURVE ( 'NONE', #16934, #9489, #11958, .T. ) ;
#9530=ORIENTED_EDGE ( 'NONE', *, *, #34559, .T. ) ;
#9533=CARTESIAN_POINT ( 'NONE',  ( 7.999999999999992895, 14.30000000000000071, 0.000000000000000000 ) ) ;
#9543=ADVANCED_FACE ( 'NONE', ( #17322 ), #16797, .T. ) ;
#9546=VECTOR ( 'NONE', #11591, 1000.000000000000000 ) ;
#9551=DIRECTION ( 'NONE',  ( 1.000000000000000000, 0.000000000000000000, 0.000000000000000000 ) ) ;
#9556=AXIS2_PLACEMENT_3D ( 'NONE', #4402, #28705, #25649 ) ;
#9562=DIRECTION ( 'NONE',  ( -1.000000000000000000, -0.000000000000000000, 0.000000000000000000 ) ) ;
#9571=CARTESIAN_POINT ( 'NONE',  ( 7.999999999999992895, 0.000000000000000000, 0.000000000000000000 ) ) ;
#9577=EDGE_LOOP ( 'NONE', ( #4982, #4791, #13532, #23805 ) ) ;
#9579=AXIS2_PLACEMENT_3D ( 'NONE', #2630, #29818, #4798 ) ;
#9583=ORIENTED_EDGE ( 'NONE', *, *, #33214, .T. ) ;
#9593=CARTESIAN_POINT ( 'NONE',  ( 7.999999999999992895, -46.87740477351715640, -3.172455868805712509 ) ) ;
#9595=CIRCLE ( 'NONE', #29731, 52.00000000000000711 ) ;
#9596=FACE_OUTER_BOUND ( 'NONE', #13868, .T. ) ;
#9602=LINE ( 'NONE', #23093, #2117 ) ;
#9606=VECTOR ( 'NONE', #22789, 1000.000000000000000 ) ;
#9609=EDGE_LOOP ( 'NONE', ( #12803, #19796, #9972, #4988 ) ) ;
#9610=CARTESIAN_POINT ( 'NONE',  ( 7.999999999999992895, -29.60891106212813995, 37.14118181634756866 ) ) ;
#9618=AXIS2_PLACEMENT_3D ( 'NONE', #16662, #288, #22247 ) ;
#9620=ORIENTED_EDGE ( 'NONE', *, *, #15092, .F. ) ;
#9625=DIRECTION ( 'NONE',  ( -1.000000000000000000, -0.000000000000000000, -0.000000000000000000 ) ) ;
#9630=EDGE_CURVE ( 'NONE', #22033, #14164, #7364, .T. ) ;
#9643=DIRECTION ( 'NONE',  ( -1.000000000000000000, 0.000000000000000000, 0.000000000000000000 ) ) ;
#9650=CIRCLE ( 'NONE', #1643, 47.49900000000002365 ) ;
#9652=VECTOR ( 'NONE', #5212, 1000.000000000000000 ) ;
#9655=ORIENTED_EDGE ( 'NONE', *, *, #28317, .F. ) ;
#9656=CARTESIAN_POINT ( 'NONE',  ( 7.999999999999992895, 47.49120266317496686, 0.8606222198176832761 ) ) ;
#9657=CARTESIAN_POINT ( 'NONE',  ( 7.999999999999992895, 17.08890430202750110, 43.76671000081951490 ) ) ;
#9660=VERTEX_POINT ( 'NONE', #11944 ) ;
#9666=CARTESIAN_POINT ( 'NONE',  ( 7.999999999999992895, 22.43957647427161461, 41.27978878573636479 ) ) ;
#9667=DIRECTION ( 'NONE',  ( -1.000000000000000000, -0.000000000000000000, -0.000000000000000000 ) ) ;
#9669=VERTEX_POINT ( 'NONE', #2046 ) ;
#9681=CARTESIAN_POINT ( 'NONE',  ( 7.999999999999992895, 9.744342220503382279, 46.48873837489803407 ) ) ;
#9685=FACE_OUTER_BOUND ( 'NONE', #22148, .T. ) ;
#9686=DIRECTION ( 'NONE',  ( -1.000000000000000000, 0.000000000000000000, 0.000000000000000000 ) ) ;
#9689=VERTEX_POINT ( 'NONE', #31379 ) ;
#9691=LINE ( 'NONE', #33635, #10115 ) ;
#9702=EDGE_CURVE ( 'NONE', #5670, #32263, #15333, .T. ) ;
#9706=ADVANCED_FACE ( 'NONE', ( #31734 ), #6890, .T. ) ;
#9714=DIRECTION ( 'NONE',  ( -1.000000000000000000, 0.000000000000000000, 0.000000000000000000 ) ) ;
#9719=CARTESIAN_POINT ( 'NONE',  ( 7.999999999999992895, 36.34385289850589373, 29.77717097092089205 ) ) ;
#9721=CARTESIAN_POINT ( 'NONE',  ( 7.999999999999992895, -2.123073309834833111, -47.45152853935339010 ) ) ;
#9728=CYLINDRICAL_SURFACE ( 'NONE', #28409, 20.00000000000000711 ) ;
#9731=VERTEX_POINT ( 'NONE', #26347 ) ;
#9736=ORIENTED_EDGE ( 'NONE', *, *, #25532, .F. ) ;
#9740=CARTESIAN_POINT ( 'NONE',  ( 7.999999999999992895, 0.000000000000000000, 0.000000000000000000 ) ) ;
#9741=ADVANCED_FACE ( 'NONE', ( #9596 ), #23640, .T. ) ;
#9742=ORIENTED_EDGE ( 'NONE', *, *, #6475, .F. ) ;
#9754=ORIENTED_EDGE ( 'NONE', *, *, #4728, .F. ) ;
#9761=VERTEX_POINT ( 'NONE', #4576 ) ;
#9762=CIRCLE ( 'NONE', #25885, 52.00000000000000711 ) ;
#9771=ORIENTED_EDGE ( 'NONE', *, *, #8189, .F. ) ;
#9788=CARTESIAN_POINT ( 'NONE',  ( 0.000000000000000000, 0.000000000000000000, 0.000000000000000000 ) ) ;
#9797=DIRECTION ( 'NONE',  ( -1.000000000000000000, 0.000000000000000000, -0.000000000000000000 ) ) ;
#9803=AXIS2_PLACEMENT_3D ( 'NONE', #5767, #3075, #30437 ) ;
#9807=DIRECTION ( 'NONE',  ( 1.000000000000000000, 0.000000000000000000, 0.000000000000000000 ) ) ;
#9808=ORIENTED_EDGE ( 'NONE', *, *, #32550, .T. ) ;
#9812=LINE ( 'NONE', #17731, #32044 ) ;
#9813=VERTEX_POINT ( 'NONE', #32628 ) ;
#9817=CARTESIAN_POINT ( 'NONE',  ( 7.999999999999992895, -2.123073309835510791, 47.45152853935334747 ) ) ;
#9819=ORIENTED_EDGE ( 'NONE', *, *, #11439, .T. ) ;
#9821=LINE ( 'NONE', #20785, #17545 ) ;
#9831=AXIS2_PLACEMENT_3D ( 'NONE', #34066, #6689, #17672 ) ;
#9844=CARTESIAN_POINT ( 'NONE',  ( 7.999999999999992895, 27.79676263918241119, -37.88001506494740056 ) ) ;
#9850=VECTOR ( 'NONE', #2166, 1000.000000000000000 ) ;
#9859=FILL_AREA_STYLE ('',( #23544 ) ) ;
#9862=FACE_OUTER_BOUND ( 'NONE', #11515, .T. ) ;
#9864=ORIENTED_EDGE ( 'NONE', *, *, #9918, .T. ) ;
#9868=ORIENTED_EDGE ( 'NONE', *, *, #35283, .T. ) ;
#9869=EDGE_CURVE ( 'NONE', #6851, #11728, #10811, .T. ) ;
#9872=CYLINDRICAL_SURFACE ( 'NONE', #5072, 52.00000000000000711 ) ;
#9875=CIRCLE ( 'NONE', #16757, 52.00000000000000711 ) ;
#9882=CYLINDRICAL_SURFACE ( 'NONE', #14911, 20.00000000000000355 ) ;
#9883=ORIENTED_EDGE ( 'NONE', *, *, #28132, .F. ) ;
#9885=EDGE_CURVE ( 'NONE', #18097, #15079, #28618, .T. ) ;
#9896=DIRECTION ( 'NONE',  ( -1.000000000000000000, -0.000000000000000000, -0.000000000000000000 ) ) ;
#9907=CARTESIAN_POINT ( 'NONE',  ( 7.999999999999992895, 0.000000000000000000, 0.000000000000000000 ) ) ;
#9910=DIRECTION ( 'NONE',  ( 0.000000000000000000, 0.8443279255020125218, 0.5358267949790005424 ) ) ;
#9913=CARTESIAN_POINT ( 'NONE',  ( 0.000000000000000000, -6.109652351741458709, -46.58570277113513214 ) ) ;
#9916=ORIENTED_EDGE ( 'NONE', *, *, #17409, .T. ) ;
#9918=EDGE_CURVE ( 'NONE', #28703, #28380, #12044, .T. ) ;
#9919=CIRCLE ( 'NONE', #11060, 20.00000000000000355 ) ;
#9931=DIRECTION ( 'NONE',  ( 0.000000000000000000, 0.000000000000000000, 1.000000000000000000 ) ) ;
#9944=DIRECTION ( 'NONE',  ( -1.000000000000000000, -0.000000000000000000, 0.000000000000000000 ) ) ;
#9953=DIRECTION ( 'NONE',  ( 0.000000000000000000, 0.000000000000000000, 1.000000000000000000 ) ) ;
#9958=FACE_OUTER_BOUND ( 'NONE', #14682, .T. ) ;
#9963=EDGE_LOOP ( 'NONE', ( #945, #34378, #9754, #25206 ) ) ;
#9970=SURFACE_STYLE_FILL_AREA ( #20389 ) ;
#9972=ORIENTED_EDGE ( 'NONE', *, *, #15213, .T. ) ;
#9983=CARTESIAN_POINT ( 'NONE',  ( 4.000000000000003553, 18.53613841426857789, -48.58406706613882875 ) ) ;
#9985=LINE ( 'NONE', #12513, #18004 ) ;
#9998=DIRECTION ( 'NONE',  ( 0.000000000000000000, -0.4817536741017037771, -0.8763066800438699122 ) ) ;
#9999=DIRECTION ( 'NONE',  ( -1.000000000000000000, -0.000000000000000000, 0.000000000000000000 ) ) ;
#10004=VERTEX_POINT ( 'NONE', #11896 ) ;
#10010=VERTEX_POINT ( 'NONE', #731 ) ;
#10014=ORIENTED_EDGE ( 'NONE', *, *, #15774, .T. ) ;
#10015=ORIENTED_EDGE ( 'NONE', *, *, #6570, .F. ) ;
#10024=DIRECTION ( 'NONE',  ( 0.000000000000000000, 0.000000000000000000, 1.000000000000000000 ) ) ;
#10027=CARTESIAN_POINT ( 'NONE',  ( 0.000000000000000000, 31.08872492059957793, 41.68322423723111569 ) ) ;
#10028=DIRECTION ( 'NONE',  ( 0.000000000000000000, 0.000000000000000000, 1.000000000000000000 ) ) ;
#10030=CIRCLE ( 'NONE', #7736, 20.00000000000000711 ) ;
#10032=AXIS2_PLACEMENT_3D ( 'NONE', #23958, #26839, #35304 ) ;
#10037=CYLINDRICAL_SURFACE ( 'NONE', #33968, 20.00000000000000355 ) ;
#10046=VERTEX_POINT ( 'NONE', #28290 ) ;
#10048=FACE_OUTER_BOUND ( 'NONE', #1081, .T. ) ;
#10049=EDGE_LOOP ( 'NONE', ( #8844, #29713, #18211, #11777 ) ) ;
#10058=DIRECTION ( 'NONE',  ( -1.000000000000000000, -0.000000000000000000, -0.000000000000000000 ) ) ;
#10065=DIRECTION ( 'NONE',  ( 0.000000000000000000, 0.5877852522924685852, 0.8090169943749506709 ) ) ;
#10071=DIRECTION ( 'NONE',  ( 0.000000000000000000, -0.5877852522924802425, 0.8090169943749421222 ) ) ;
#10073=CARTESIAN_POINT ( 'NONE',  ( 0.000000000000000000, -36.06787431788650622, -37.45808914225528952 ) ) ;
#10074=ADVANCED_FACE ( 'NONE', ( #22340 ), #33501, .T. ) ;
#10079=ORIENTED_EDGE ( 'NONE', *, *, #10138, .T. ) ;
#10088=CARTESIAN_POINT ( 'NONE',  ( 0.000000000000000000, 31.08872492060014991, -41.68322423723069647 ) ) ;
#10093=CARTESIAN_POINT ( 'NONE',  ( 0.000000000000000000, 0.000000000000000000, 0.000000000000000000 ) ) ;
#10103=ORIENTED_EDGE ( 'NONE', *, *, #11056, .F. ) ;
#10104=EDGE_LOOP ( 'NONE', ( #30028, #9148, #14033, #26872 ) ) ;
#10106=EDGE_CURVE ( 'NONE', #8056, #11602, #28728, .T. ) ;
#10115=VECTOR ( 'NONE', #3764, 1000.000000000000000 ) ;
#10121=ADVANCED_FACE ( 'NONE', ( #14057 ), #22872, .T. ) ;
#10124=DIRECTION ( 'NONE',  ( -1.000000000000000000, 0.000000000000000000, 0.000000000000000000 ) ) ;
#10132=AXIS2_PLACEMENT_3D ( 'NONE', #29939, #27601, #16591 ) ;
#10138=EDGE_CURVE ( 'NONE', #30069, #23788, #558, .T. ) ;
#10139=VECTOR ( 'NONE', #29317, 1000.000000000000000 ) ;
#10140=ORIENTED_EDGE ( 'NONE', *, *, #12517, .F. ) ;
#10145=ORIENTED_EDGE ( 'NONE', *, *, #3496, .T. ) ;
#10147=CIRCLE ( 'NONE', #26270, 20.00000000000000711 ) ;
#10155=EDGE_CURVE ( 'NONE', #29894, #15796, #27765, .T. ) ;
#10156=EDGE_CURVE ( 'NONE', #2175, #30986, #32734, .T. ) ;
#10165=EDGE_CURVE ( 'NONE', #966, #27135, #22387, .T. ) ;
#10173=DIRECTION ( 'NONE',  ( -1.000000000000000000, 0.000000000000000000, 0.000000000000000000 ) ) ;
#10175=AXIS2_PLACEMENT_3D ( 'NONE', #6863, #17835, #12446 ) ;
#10191=ORIENTED_EDGE ( 'NONE', *, *, #19121, .T. ) ;
#10199=AXIS2_PLACEMENT_3D ( 'NONE', #14629, #33913, #28160 ) ;
#10201=EDGE_LOOP ( 'NONE', ( #15532, #15346, #8655, #15112 ) ) ;
#10202=ORIENTED_EDGE ( 'NONE', *, *, #29807, .T. ) ;
#10228=CARTESIAN_POINT ( 'NONE',  ( 7.999999999999992895, 0.000000000000000000, 0.000000000000000000 ) ) ;
#10237=EDGE_CURVE ( 'NONE', #4138, #28129, #9161, .T. ) ;
#10238=EDGE_LOOP ( 'NONE', ( #22498, #13339, #2422, #17755 ) ) ;
#10239=VERTEX_POINT ( 'NONE', #18496 ) ;
#10240=EDGE_CURVE ( 'NONE', #20113, #7164, #4834, .T. ) ;
#10245=ORIENTED_EDGE ( 'NONE', *, *, #33511, .F. ) ;
#10247=DIRECTION ( 'NONE',  ( 0.000000000000000000, 0.000000000000000000, -1.000000000000000000 ) ) ;
#10261=AXIS2_PLACEMENT_3D ( 'NONE', #19245, #16552, #2898 ) ;
#10262=DIRECTION ( 'NONE',  ( -1.000000000000000000, 0.000000000000000000, 0.000000000000000000 ) ) ;
#10272=ORIENTED_EDGE ( 'NONE', *, *, #29104, .F. ) ;
#10274=CARTESIAN_POINT ( 'NONE',  ( 0.000000000000000000, -47.49120266317495975, -0.8606222198180163430 ) ) ;
#10285=ADVANCED_FACE ( 'NONE', ( #2146 ), #13122, .T. ) ;
#10287=ORIENTED_EDGE ( 'NONE', *, *, #24718, .T. ) ;
#10293=ORIENTED_EDGE ( 'NONE', *, *, #32391, .T. ) ;
#10294=CARTESIAN_POINT ( 'NONE',  ( 0.000000000000000000, 0.000000000000000000, 0.000000000000000000 ) ) ;
#10295=ADVANCED_FACE ( 'NONE', ( #12574 ), #5009, .T. ) ;
#10308=DIRECTION ( 'NONE',  ( 0.000000000000000000, 0.000000000000000000, 1.000000000000000000 ) ) ;
#10310=MANIFOLD_SOLID_BREP ( 'Keyway', #33639 ) ;
#10312=DIRECTION ( 'NONE',  ( -1.000000000000000000, 0.000000000000000000, 0.000000000000000000 ) ) ;
#10315=CARTESIAN_POINT ( 'NONE',  ( 0.000000000000000000, 0.000000000000000000, 0.000000000000000000 ) ) ;
#10319=CARTESIAN_POINT ( 'NONE',  ( 0.000000000000000000, -39.78933988720132220, 24.98727647984988565 ) ) ;
#10320=EDGE_CURVE ( 'NONE', #18391, #4328, #21531, .T. ) ;
#10323=EDGE_CURVE ( 'NONE', #30561, #2044, #30486, .T. ) ;
#10324=CIRCLE ( 'NONE', #32729, 20.00000000000000711 ) ;
#10327=ORIENTED_EDGE ( 'NONE', *, *, #19377, .T. ) ;
#10353=ORIENTED_EDGE ( 'NONE', *, *, #21387, .F. ) ;
#10354=COLOUR_RGB ( '', 0.66274510, 0.83137255, 0.94901961) ;
#10358=CARTESIAN_POINT ( 'NONE',  ( 0.000000000000000000, -32.32520163883607722, 34.09746168776025854 ) ) ;
#10362=DIRECTION ( 'NONE',  ( -1.000000000000000000, 0.000000000000000000, 0.000000000000000000 ) ) ;
#10364=EDGE_CURVE ( 'NONE', #31652, #34767, #17214, .T. ) ;
#10381=ORIENTED_EDGE ( 'NONE', *, *, #2910, .T. ) ;
#10384=VERTEX_POINT ( 'NONE', #15031 ) ;
#10387=AXIS2_PLACEMENT_3D ( 'NONE', #24585, #21685, #13592 ) ;
#10391=ORIENTED_EDGE ( 'NONE', *, *, #30160, .T. ) ;
#10392=DIRECTION ( 'NONE',  ( 0.000000000000000000, -0.1253332335643113082, 0.9921147013144768767 ) ) ;
#10396=CARTESIAN_POINT ( 'NONE',  ( -9.999999999999994671, 0.000000000000000000, 0.000000000000000000 ) ) ;
#10398=ADVANCED_FACE ( 'NONE', ( #3718 ), #22961, .T. ) ;
#10400=CARTESIAN_POINT ( 'NONE',  ( 0.000000000000000000, 0.000000000000000000, 0.000000000000000000 ) ) ;
#10406=CARTESIAN_POINT ( 'NONE',  ( 7.999999999999992895, -46.19362259308839214, 8.585149169758333088 ) ) ;
#10409=DIRECTION ( 'NONE',  ( -1.000000000000000000, -0.000000000000000000, -0.000000000000000000 ) ) ;
#10419=ORIENTED_EDGE ( 'NONE', *, *, #886, .F. ) ;
#10427=DIRECTION ( 'NONE',  ( -1.000000000000000000, 0.000000000000000000, 0.000000000000000000 ) ) ;
#10440=EDGE_CURVE ( 'NONE', #24590, #24598, #4612, .T. ) ;
#10450=DIRECTION ( 'NONE',  ( 0.000000000000000000, 0.000000000000000000, 1.000000000000000000 ) ) ;
#10459=EDGE_LOOP ( 'NONE', ( #9393, #4810, #28846, #19473 ) ) ;
#10466=DIRECTION ( 'NONE',  ( 0.000000000000000000, 0.6845471059286900584, -0.7289686274214103312 ) ) ;
#10470=FACE_OUTER_BOUND ( 'NONE', #8407, .T. ) ;
#10475=DIRECTION ( 'NONE',  ( -1.000000000000000000, 0.000000000000000000, -0.000000000000000000 ) ) ;
#10476=ORIENTED_EDGE ( 'NONE', *, *, #15650, .F. ) ;
#10478=EDGE_CURVE ( 'NONE', #18497, #11997, #6900, .T. ) ;
#10490=CARTESIAN_POINT ( 'NONE',  ( 0.000000000000000000, -5.871425383721172508, -51.66745943012291065 ) ) ;
#10493=DIRECTION ( 'NONE',  ( 1.000000000000000000, 0.000000000000000000, 0.000000000000000000 ) ) ;
#10501=VECTOR ( 'NONE', #23259, 1000.000000000000000 ) ;
#10502=ORIENTED_EDGE ( 'NONE', *, *, #30655, .F. ) ;
#10512=CARTESIAN_POINT ( 'NONE',  ( 0.000000000000000000, 46.21320724403649649, 10.97699764141971102 ) ) ;
#10515=EDGE_CURVE ( 'NONE', #15970, #3935, #11502, .T. ) ;
#10525=EDGE_CURVE ( 'NONE', #5751, #2191, #14491, .T. ) ;
#10526=CIRCLE ( 'NONE', #15102, 20.00000000000000711 ) ;
#10528=DIRECTION ( 'NONE',  ( -1.000000000000000000, -0.000000000000000000, 0.000000000000000000 ) ) ;
#10537=CARTESIAN_POINT ( 'NONE',  ( 4.000000000000003553, 35.11945359308111847, 38.34871548466026070 ) ) ;
#10545=CARTESIAN_POINT ( 'NONE',  ( 7.999999999999992895, 0.000000000000000000, 0.000000000000000000 ) ) ;
#10547=ORIENTED_EDGE ( 'NONE', *, *, #33723, .F. ) ;
#10550=EDGE_CURVE ( 'NONE', #29785, #28091, #29920, .T. ) ;
#10555=VECTOR ( 'NONE', #30108, 1000.000000000000000 ) ;
#10561=FACE_OUTER_BOUND ( 'NONE', #29186, .T. ) ;
#10563=EDGE_CURVE ( 'NONE', #19637, #32720, #32763, .T. ) ;
#10577=VECTOR ( 'NONE', #15829, 1000.000000000000000 ) ;
#10579=CARTESIAN_POINT ( 'NONE',  ( 7.999999999999992895, -45.78515115856034612, -12.64416602183715455 ) ) ;
#10583=FACE_OUTER_BOUND ( 'NONE', #3738, .T. ) ;
#10585=CARTESIAN_POINT ( 'NONE',  ( 7.999999999999992895, -17.50309955389579386, -43.60271849949381817 ) ) ;
#10587=ORIENTED_EDGE ( 'NONE', *, *, #22212, .F. ) ;
#10588=CIRCLE ( 'NONE', #21484, 20.00000000000000711 ) ;
#10593=EDGE_CURVE ( 'NONE', #29687, #15571, #12889, .T. ) ;
#10594=DIRECTION ( 'NONE',  ( -1.000000000000000000, 0.000000000000000000, -0.000000000000000000 ) ) ;
#10602=VECTOR ( 'NONE', #29328, 1000.000000000000000 ) ;
#10607=DIRECTION ( 'NONE',  ( -1.000000000000000000, -0.000000000000000000, -0.000000000000000000 ) ) ;
#10608=ORIENTED_EDGE ( 'NONE', *, *, #15367, .T. ) ;
#10616=CYLINDRICAL_SURFACE ( 'NONE', #32004, 20.00000000000000355 ) ;
#10617=EDGE_CURVE ( 'NONE', #34778, #892, #30504, .T. ) ;
#10622=FACE_OUTER_BOUND ( 'NONE', #35238, .T. ) ;
#10641=VERTEX_POINT ( 'NONE', #29092 ) ;
#10646=VECTOR ( 'NONE', #26885, 1000.000000000000000 ) ;
#10648=ORIENTED_EDGE ( 'NONE', *, *, #31759, .F. ) ;
#10651=CARTESIAN_POINT ( 'NONE',  ( 7.999999999999992895, 0.000000000000000000, 0.000000000000000000 ) ) ;
#10658=DIRECTION ( 'NONE',  ( 0.000000000000000000, 0.3681245526846786964, -0.9297764858882511252 ) ) ;
#10659=FACE_OUTER_BOUND ( 'NONE', #10201, .T. ) ;
#10661=VECTOR ( 'NONE', #11625, 1000.000000000000000 ) ;
#10664=AXIS2_PLACEMENT_3D ( 'NONE', #33092, #19042, #8585 ) ;
#10666=VERTEX_POINT ( 'NONE', #32319 ) ;
#10668=CARTESIAN_POINT ( 'NONE',  ( 0.000000000000000000, 0.000000000000000000, 0.000000000000000000 ) ) ;
#10670=AXIS2_PLACEMENT_3D ( 'NONE', #12070, #23413, #33863 ) ;
#10672=DIRECTION ( 'NONE',  ( -1.000000000000000000, -0.000000000000000000, 0.000000000000000000 ) ) ;
#10679=ORIENTED_EDGE ( 'NONE', *, *, #24951, .T. ) ;
#10685=ORIENTED_EDGE ( 'NONE', *, *, #24960, .F. ) ;
#10702=CARTESIAN_POINT ( 'NONE',  ( 7.999999999999992895, 0.000000000000000000, 0.000000000000000000 ) ) ;
#10715=CARTESIAN_POINT ( 'NONE',  ( 0.000000000000000000, -46.87740477351715640, -3.172455868805712509 ) ) ;
#10717=LINE ( 'NONE', #13779, #9521 ) ;
#10719=VERTEX_POINT ( 'NONE', #30513 ) ;
#10739=ORIENTED_EDGE ( 'NONE', *, *, #33511, .T. ) ;
#10742=DIRECTION ( 'NONE',  ( 1.000000000000000000, -0.000000000000000000, 0.000000000000000000 ) ) ;
#10746=CIRCLE ( 'NONE', #14759, 47.49900000000001654 ) ;
#10749=DIRECTION ( 'NONE',  ( 0.000000000000000000, 0.6845471059286846183, 0.7289686274214153272 ) ) ;
#10756=AXIS2_PLACEMENT_3D ( 'NONE', #20011, #11935, #5659 ) ;
#10763=DIRECTION ( 'NONE',  ( 0.000000000000000000, 0.000000000000000000, 1.000000000000000000 ) ) ;
#10770=DIRECTION ( 'NONE',  ( 0.000000000000000000, 0.9980267284282712259, 0.06279051952931682945 ) ) ;
#10772=EDGE_CURVE ( 'NONE', #12651, #30694, #25909, .T. ) ;
#10775=ORIENTED_EDGE ( 'NONE', *, *, #34299, .F. ) ;
#10782=ORIENTED_EDGE ( 'NONE', *, *, #2731, .T. ) ;
#10785=VECTOR ( 'NONE', #30623, 1000.000000000000000 ) ;
#10788=EDGE_LOOP ( 'NONE', ( #16608, #24749, #32910, #20250 ) ) ;
#10792=CIRCLE ( 'NONE', #12506, 47.49900000000000944 ) ;
#10801=DIRECTION ( 'NONE',  ( -1.000000000000000000, -0.000000000000000000, -0.000000000000000000 ) ) ;
#10803=ORIENTED_EDGE ( 'NONE', *, *, #5691, .F. ) ;
#10804=CARTESIAN_POINT ( 'NONE',  ( 4.000000000000003553, 30.03615769709793426, -42.44795908868959344 ) ) ;
#10811=CIRCLE ( 'NONE', #23451, 20.00000000000000711 ) ;
#10813=ORIENTED_EDGE ( 'NONE', *, *, #1405, .F. ) ;
#10814=CIRCLE ( 'NONE', #26337, 20.00000000000000711 ) ;
#10824=DIRECTION ( 'NONE',  ( -1.000000000000000000, 0.000000000000000000, -0.000000000000000000 ) ) ;
#10826=VERTEX_POINT ( 'NONE', #16805 ) ;
#10836=DIRECTION ( 'NONE',  ( -1.000000000000000000, 0.000000000000000000, 0.000000000000000000 ) ) ;
#10840=LINE ( 'NONE', #21798, #24640 ) ;
#10847=CARTESIAN_POINT ( 'NONE',  ( 7.999999999999992895, 51.19683565102445044, 9.104066087303644750 ) ) ;
#10850=EDGE_CURVE ( 'NONE', #21098, #3168, #22560, .T. ) ;
#10855=CARTESIAN_POINT ( 'NONE',  ( 7.999999999999992895, 31.08872492059958148, 41.68322423723111569 ) ) ;
#10860=EDGE_CURVE ( 'NONE', #4114, #32945, #3497, .T. ) ;
#10871=EDGE_CURVE ( 'NONE', #9085, #20492, #30858, .T. ) ;
#10872=LINE ( 'NONE', #21296, #21559 ) ;
#10878=LINE ( 'NONE', #32834, #16629 ) ;
#10881=CARTESIAN_POINT ( 'NONE',  ( 7.999999999999992895, 44.75336757549778355, 14.30704879393622520 ) ) ;
#10886=DIRECTION ( 'NONE',  ( 0.000000000000000000, 0.2486898871648552389, -0.9685831611286309650 ) ) ;
#10887=EDGE_CURVE ( 'NONE', #31530, #7529, #14454, .T. ) ;
#10889=ORIENTED_EDGE ( 'NONE', *, *, #21777, .F. ) ;
#10890=AXIS2_PLACEMENT_3D ( 'NONE', #25892, #20628, #17759 ) ;
#10892=DIRECTION ( 'NONE',  ( 0.000000000000000000, 0.000000000000000000, 1.000000000000000000 ) ) ;
#10898=CARTESIAN_POINT ( 'NONE',  ( 7.999999999999992895, 26.17370628620655637, 39.63700417846175128 ) ) ;
#10903=AXIS2_PLACEMENT_3D ( 'NONE', #377, #11376, #26254 ) ;
#10906=ORIENTED_EDGE ( 'NONE', *, *, #23573, .F. ) ;
#10909=DIRECTION ( 'NONE',  ( 0.000000000000000000, 0.9048270524660205760, -0.4257792915650703836 ) ) ;
#10911=ORIENTED_EDGE ( 'NONE', *, *, #16025, .T. ) ;
#10924=LINE ( 'NONE', #10976, #2625 ) ;
#10926=VECTOR ( 'NONE', #22280, 1000.000000000000000 ) ;
#10934=FACE_OUTER_BOUND ( 'NONE', #13823, .T. ) ;
#10937=SURFACE_SIDE_STYLE ('',( #8393 ) ) ;
#10942=LINE ( 'NONE', #6852, #17622 ) ;
#10944=ORIENTED_EDGE ( 'NONE', *, *, #30449, .T. ) ;
#10947=LINE ( 'NONE', #19207, #24429 ) ;
#10962=ORIENTED_EDGE ( 'NONE', *, *, #31285, .F. ) ;
#10976=CARTESIAN_POINT ( 'NONE',  ( 7.999999999999992895, -34.03046037009280411, 33.13733193845794034 ) ) ;
#10977=DIRECTION ( 'NONE',  ( -1.000000000000000000, -0.000000000000000000, -0.000000000000000000 ) ) ;
#10979=ORIENTED_EDGE ( 'NONE', *, *, #15449, .F. ) ;
#10980=DIRECTION ( 'NONE',  ( -1.000000000000000000, 0.000000000000000000, 0.000000000000000000 ) ) ;
#10982=EDGE_CURVE ( 'NONE', #12448, #16934, #33942, .T. ) ;
#10986=ORIENTED_EDGE ( 'NONE', *, *, #1285, .T. ) ;
#10989=VERTEX_POINT ( 'NONE', #22385 ) ;
#10992=DIRECTION ( 'NONE',  ( 0.000000000000000000, 0.000000000000000000, 1.000000000000000000 ) ) ;
#10993=EDGE_LOOP ( 'NONE', ( #23531, #4686, #19987, #30426 ) ) ;
#10995=CYLINDRICAL_SURFACE ( 'NONE', #3353, 20.00000000000000355 ) ;
#11004=CARTESIAN_POINT ( 'NONE',  ( 7.999999999999992895, -36.05989434073592292, -30.12041790338657066 ) ) ;
#11006=CARTESIAN_POINT ( 'NONE',  ( 7.999999999999992895, 29.60891106212840285, -37.14118181634734839 ) ) ;
#11007=EDGE_CURVE ( 'NONE', #30, #2768, #33380, .T. ) ;
#11011=AXIS2_PLACEMENT_3D ( 'NONE', #5185, #24257, #35244 ) ;
#11012=DIRECTION ( 'NONE',  ( -1.000000000000000000, -0.000000000000000000, -0.000000000000000000 ) ) ;
#11029=LINE ( 'NONE', #24535, #27944 ) ;
#11030=ORIENTED_EDGE ( 'NONE', *, *, #524, .F. ) ;
#11033=CARTESIAN_POINT ( 'NONE',  ( 4.000000000000003553, 47.32430374665962347, -21.55018039121478424 ) ) ;
#11039=VERTEX_POINT ( 'NONE', #1150 ) ;
#11047=LINE ( 'NONE', #20980, #31528 ) ;
#11053=DIRECTION ( 'NONE',  ( 0.000000000000000000, 0.3681245526846787519, -0.9297764858882511252 ) ) ;
#11056=EDGE_CURVE ( 'NONE', #28075, #1935, #16133, .T. ) ;
#11060=AXIS2_PLACEMENT_3D ( 'NONE', #16442, #22553, #3854 ) ;
#11067=DIRECTION ( 'NONE',  ( 0.000000000000000000, 0.000000000000000000, 1.000000000000000000 ) ) ;
#11073=AXIS2_PLACEMENT_3D ( 'NONE', #14973, #1855, #1304 ) ;
#11078=CIRCLE ( 'NONE', #32917, 20.00000000000000711 ) ;
#11079=CARTESIAN_POINT ( 'NONE',  ( 7.999999999999992895, 0.000000000000000000, 0.000000000000000000 ) ) ;
#11095=AXIS2_PLACEMENT_3D ( 'NONE', #8876, #24927, #33375 ) ;
#11101=DIRECTION ( 'NONE',  ( 0.000000000000000000, 0.000000000000000000, 1.000000000000000000 ) ) ;
#11103=CARTESIAN_POINT ( 'NONE',  ( 7.999999999999992895, 0.000000000000000000, 0.000000000000000000 ) ) ;
#11105=CARTESIAN_POINT ( 'NONE',  ( 0.000000000000000000, 0.000000000000000000, 0.000000000000000000 ) ) ;
#11108=DIRECTION ( 'NONE',  ( 0.000000000000000000, 0.000000000000000000, 1.000000000000000000 ) ) ;
#11110=CYLINDRICAL_SURFACE ( 'NONE', #5556, 20.00000000000000711 ) ;
#11115=CARTESIAN_POINT ( 'NONE',  ( 7.999999999999992895, -46.87740477351719193, 3.172455868805032608 ) ) ;
#11116=DIRECTION ( 'NONE',  ( -1.000000000000000000, 0.000000000000000000, 0.000000000000000000 ) ) ;
#11120=VECTOR ( 'NONE', #5798, 1000.000000000000000 ) ;
#11126=EDGE_CURVE ( 'NONE', #26553, #10239, #12119, .T. ) ;
#11127=EDGE_CURVE ( 'NONE', #3384, #4138, #13294, .T. ) ;
#11129=CARTESIAN_POINT ( 'NONE',  ( 4.000000000000003553, 51.85248208264525260, -3.914090171285633524 ) ) ;
#11137=DIRECTION ( 'NONE',  ( 0.000000000000000000, 0.000000000000000000, 1.000000000000000000 ) ) ;
#11148=DIRECTION ( 'NONE',  ( 0.000000000000000000, 0.000000000000000000, 1.000000000000000000 ) ) ;
#11151=DIRECTION ( 'NONE',  ( 0.000000000000000000, 0.000000000000000000, 1.000000000000000000 ) ) ;
#11152=ORIENTED_EDGE ( 'NONE', *, *, #22212, .T. ) ;
#11157=ORIENTED_EDGE ( 'NONE', *, *, #7739, .T. ) ;
#11164=AXIS2_PLACEMENT_3D ( 'NONE', #172, #531, #25558 ) ;
#11167=AXIS2_PLACEMENT_3D ( 'NONE', #7390, #28074, #11151 ) ;
#11170=DIRECTION ( 'NONE',  ( -1.000000000000000000, 0.000000000000000000, -0.000000000000000000 ) ) ;
#11190=EDGE_LOOP ( 'NONE', ( #17262, #1740, #15110, #19552 ) ) ;
#11196=VERTEX_POINT ( 'NONE', #18048 ) ;
#11200=DIRECTION ( 'NONE',  ( -1.000000000000000000, 0.000000000000000000, -0.000000000000000000 ) ) ;
#11201=ORIENTED_EDGE ( 'NONE', *, *, #3391, .F. ) ;
#11205=ORIENTED_EDGE ( 'NONE', *, *, #18232, .T. ) ;
#11209=CARTESIAN_POINT ( 'NONE',  ( 7.999999999999992895, 27.79676263918241119, -37.88001506494740056 ) ) ;
#11225=DIRECTION ( 'NONE',  ( 0.000000000000000000, -0.6845471059286791782, -0.7289686274214204342 ) ) ;
#11235=DIRECTION ( 'NONE',  ( 0.000000000000000000, 0.000000000000000000, 1.000000000000000000 ) ) ;
#11240=AXIS2_PLACEMENT_3D ( 'NONE', #26939, #23866, #4793 ) ;
#11244=DIRECTION ( 'NONE',  ( 0.000000000000000000, 0.000000000000000000, 1.000000000000000000 ) ) ;
#11248=DIRECTION ( 'NONE',  ( 0.000000000000000000, 0.000000000000000000, 1.000000000000000000 ) ) ;
#11249=LINE ( 'NONE', #33222, #28359 ) ;
#11263=AXIS2_PLACEMENT_3D ( 'NONE', #6716, #17696, #33551 ) ;
#11266=CYLINDRICAL_SURFACE ( 'NONE', #30927, 47.49900000000001654 ) ;
#11267=AXIS2_PLACEMENT_3D ( 'NONE', #14444, #8694, #25454 ) ;
#11269=CARTESIAN_POINT ( 'NONE',  ( 0.000000000000000000, 26.17370628620710349, -39.63700417846138890 ) ) ;
#11275=AXIS2_PLACEMENT_3D ( 'NONE', #20035, #31039, #6371 ) ;
#11278=AXIS2_PLACEMENT_3D ( 'NONE', #4830, #15772, #31819 ) ;
#11285=EDGE_CURVE ( 'NONE', #34584, #33861, #5453, .T. ) ;
#11295=DIRECTION ( 'NONE',  ( 0.000000000000000000, 0.000000000000000000, -1.000000000000000000 ) ) ;
#11299=EDGE_CURVE ( 'NONE', #8148, #19482, #23639, .T. ) ;
#11300=CIRCLE ( 'NONE', #4398, 47.49900000000000944 ) ;
#11303=CARTESIAN_POINT ( 'NONE',  ( 0.000000000000000000, -7.162210897275381072, -51.50439529848838305 ) ) ;
#11310=VERTEX_POINT ( 'NONE', #32992 ) ;
#11312=LINE ( 'NONE', #33613, #10926 ) ;
#11325=CARTESIAN_POINT ( 'NONE',  ( 7.999999999999992895, 0.000000000000000000, 0.000000000000000000 ) ) ;
#11326=DIRECTION ( 'NONE',  ( 0.000000000000000000, 0.9822872507286879440, 0.1873813145857286533 ) ) ;
#11333=CARTESIAN_POINT ( 'NONE',  ( 7.999999999999992895, -39.55064067543046491, -25.36340625197400200 ) ) ;
#11338=DIRECTION ( 'NONE',  ( -1.000000000000000000, 0.000000000000000000, 0.000000000000000000 ) ) ;
#11342=DIRECTION ( 'NONE',  ( 0.000000000000000000, 0.000000000000000000, 1.000000000000000000 ) ) ;
#11348=LINE ( 'NONE', #33646, #25750 ) ;
#11350=ORIENTED_EDGE ( 'NONE', *, *, #33214, .F. ) ;
#11352=CIRCLE ( 'NONE', #5602, 20.00000000000000711 ) ;
#11358=CIRCLE ( 'NONE', #26233, 47.49900000000001654 ) ;
#11363=CYLINDRICAL_SURFACE ( 'NONE', #7923, 20.00000000000000355 ) ;
#11368=AXIS2_PLACEMENT_3D ( 'NONE', #3498, #3143, #6009 ) ;
#11369=LINE ( 'NONE', #22335, #34301 ) ;
#11370=LINE ( 'NONE', #22337, #22143 ) ;
#11371=EDGE_CURVE ( 'NONE', #15707, #14196, #33977, .T. ) ;
#11376=DIRECTION ( 'NONE',  ( 1.000000000000000000, 0.000000000000000000, 0.000000000000000000 ) ) ;
#11378=VECTOR ( 'NONE', #19017, 1000.000000000000000 ) ;
#11398=ORIENTED_EDGE ( 'NONE', *, *, #34979, .F. ) ;
#11401=ORIENTED_EDGE ( 'NONE', *, *, #24224, .F. ) ;
#11402=CARTESIAN_POINT ( 'NONE',  ( 7.999999999999992895, 0.000000000000000000, 0.000000000000000000 ) ) ;
#11406=AXIS2_PLACEMENT_3D ( 'NONE', #14331, #5887, #22606 ) ;
#11409=DIRECTION ( 'NONE',  ( -1.000000000000000000, -0.000000000000000000, -0.000000000000000000 ) ) ;
#11415=CARTESIAN_POINT ( 'NONE',  ( 4.000000000000003553, -49.25004636492376875, -16.68630974939810940 ) ) ;
#11420=DIRECTION ( 'NONE',  ( -1.000000000000000000, 0.000000000000000000, -0.000000000000000000 ) ) ;
#11429=CARTESIAN_POINT ( 'NONE',  ( 0.000000000000000000, 13.56094713063641599, -50.20060470671727870 ) ) ;
#11430=CARTESIAN_POINT ( 'NONE',  ( 7.999999999999992895, -9.744342220503080298, -46.48873837489808380 ) ) ;
#11431=ORIENTED_EDGE ( 'NONE', *, *, #20076, .T. ) ;
#11439=EDGE_CURVE ( 'NONE', #23782, #10046, #1801, .T. ) ;
#11442=DIRECTION ( 'NONE',  ( 0.000000000000000000, 0.000000000000000000, 1.000000000000000000 ) ) ;
#11446=AXIS2_PLACEMENT_3D ( 'NONE', #11402, #16953, #16784 ) ;
#11447=ADVANCED_FACE ( 'NONE', ( #30473 ), #20162, .T. ) ;
#11448=EDGE_CURVE ( 'NONE', #892, #30005, #33998, .T. ) ;
#11458=EDGE_CURVE ( 'NONE', #15970, #16062, #25390, .T. ) ;
#11460=DIRECTION ( 'NONE',  ( 0.000000000000000000, 0.000000000000000000, 1.000000000000000000 ) ) ;
#11463=EDGE_CURVE ( 'NONE', #25236, #6112, #6972, .T. ) ;
#11465=ORIENTED_EDGE ( 'NONE', *, *, #21473, .F. ) ;
#11477=VERTEX_POINT ( 'NONE', #22346 ) ;
#11480=DIRECTION ( 'NONE',  ( 0.000000000000000000, 0.6845471059286899473, -0.7289686274214103312 ) ) ;
#11482=ORIENTED_EDGE ( 'NONE', *, *, #14158, .F. ) ;
#11485=CARTESIAN_POINT ( 'NONE',  ( 7.999999999999992895, 45.78515115856044559, 12.64416602183680816 ) ) ;
#11492=EDGE_CURVE ( 'NONE', #18961, #28703, #33340, .T. ) ;
#11496=CIRCLE ( 'NONE', #25305, 52.00000000000000711 ) ;
#11502=CIRCLE ( 'NONE', #16081, 20.00000000000000355 ) ;
#11505=AXIS2_PLACEMENT_3D ( 'NONE', #19168, #35397, #24070 ) ;
#11514=LINE ( 'NONE', #14211, #14807 ) ;
#11515=EDGE_LOOP ( 'NONE', ( #8859, #21598, #29459, #8578 ) ) ;
#11527=EDGE_CURVE ( 'NONE', #2304, #30694, #17828, .T. ) ;
#11529=AXIS2_PLACEMENT_3D ( 'NONE', #13866, #10824, #2904 ) ;
#11530=ORIENTED_EDGE ( 'NONE', *, *, #32639, .T. ) ;
#11534=DIRECTION ( 'NONE',  ( -1.000000000000000000, -0.000000000000000000, 0.000000000000000000 ) ) ;
#11536=LINE ( 'NONE', #9721, #4783 ) ;
#11537=EDGE_CURVE ( 'NONE', #6545, #30873, #15300, .T. ) ;
#11543=EDGE_LOOP ( 'NONE', ( #17221, #96, #24374, #25839 ) ) ;
#11547=DIRECTION ( 'NONE',  ( -1.000000000000000000, 0.000000000000000000, 0.000000000000000000 ) ) ;
#11562=ORIENTED_EDGE ( 'NONE', *, *, #29712, .T. ) ;
#11565=CARTESIAN_POINT ( 'NONE',  ( 7.999999999999992895, 0.000000000000000000, 0.000000000000000000 ) ) ;
#11567=ORIENTED_EDGE ( 'NONE', *, *, #25536, .F. ) ;
#11576=DIRECTION ( 'NONE',  ( 0.000000000000000000, -0.8443279255020201823, 0.5358267949789886631 ) ) ;
#11585=CARTESIAN_POINT ( 'NONE',  ( 7.999999999999992895, 51.19683565102457834, -9.104066087302935983 ) ) ;
#11586=ORIENTED_EDGE ( 'NONE', *, *, #32309, .T. ) ;
#11590=DIRECTION ( 'NONE',  ( -1.000000000000000000, 0.000000000000000000, -0.000000000000000000 ) ) ;
#11591=DIRECTION ( 'NONE',  ( -1.000000000000000000, 0.000000000000000000, 0.000000000000000000 ) ) ;
#11592=DIRECTION ( 'NONE',  ( 0.000000000000000000, 0.5877852522924685852, 0.8090169943749507819 ) ) ;
#11593=ORIENTED_EDGE ( 'NONE', *, *, #26784, .T. ) ;
#11594=CYLINDRICAL_SURFACE ( 'NONE', #917, 47.49900000000001654 ) ;
#11602=VERTEX_POINT ( 'NONE', #23785 ) ;
#11604=PLANE ( 'NONE',  #20027 ) ;
#11607=DIRECTION ( 'NONE',  ( -1.000000000000000000, -0.000000000000000000, 0.000000000000000000 ) ) ;
#11613=DIRECTION ( 'NONE',  ( -1.000000000000000000, -0.000000000000000000, 0.000000000000000000 ) ) ;
#11625=DIRECTION ( 'NONE',  ( -1.000000000000000000, 0.000000000000000000, 0.000000000000000000 ) ) ;
#11627=EDGE_CURVE ( 'NONE', #13488, #33428, #32274, .T. ) ;
#11629=VERTEX_POINT ( 'NONE', #31877 ) ;
#11639=EDGE_CURVE ( 'NONE', #14247, #21046, #24241, .T. ) ;
#11643=CARTESIAN_POINT ( 'NONE',  ( 4.000000000000003553, 0.6505223195682995341, 51.99593080916758936 ) ) ;
#11654=CARTESIAN_POINT ( 'NONE',  ( 7.999999999999992895, -45.78515115856053797, 12.64416602183649019 ) ) ;
#11659=CARTESIAN_POINT ( 'NONE',  ( 7.999999999999992895, 47.49120266317496686, -0.8606222198176971538 ) ) ;
#11662=CARTESIAN_POINT ( 'NONE',  ( 7.999999999999992895, -46.87740477351719193, 3.172455868805032608 ) ) ;
#11668=VECTOR ( 'NONE', #23406, 1000.000000000000000 ) ;
#11669=CARTESIAN_POINT ( 'NONE',  ( 0.000000000000000000, 42.03146605346787368, 22.12489237027333289 ) ) ;
#11673=DIRECTION ( 'NONE',  ( 1.000000000000000000, 0.000000000000000000, 0.000000000000000000 ) ) ;
#11678=LINE ( 'NONE', #22479, #32668 ) ;
#11679=CARTESIAN_POINT ( 'NONE',  ( 7.999999999999992895, 0.000000000000000000, 0.000000000000000000 ) ) ;
#11680=VERTEX_POINT ( 'NONE', #11485 ) ;
#11684=VERTEX_POINT ( 'NONE', #11654 ) ;
#11689=CARTESIAN_POINT ( 'NONE',  ( 7.999999999999992895, -29.60891106212763191, -37.14118181634798788 ) ) ;
#11696=CARTESIAN_POINT ( 'NONE',  ( -9.999999999999994671, 0.000000000000000000, 0.000000000000000000 ) ) ;
#11704=FACE_OUTER_BOUND ( 'NONE', #7695, .T. ) ;
#11710=ORIENTED_EDGE ( 'NONE', *, *, #31199, .F. ) ;
#11711=CARTESIAN_POINT ( 'NONE',  ( 7.999999999999992895, -39.55064067543080597, 25.36340625197344778 ) ) ;
#11713=ADVANCED_FACE ( 'NONE', ( #20275 ), #849, .T. ) ;
#11714=ORIENTED_EDGE ( 'NONE', *, *, #11639, .T. ) ;
#11718=AXIS2_PLACEMENT_3D ( 'NONE', #12515, #18801, #29802 ) ;
#11726=DIRECTION ( 'NONE',  ( 1.000000000000000000, 0.000000000000000000, -0.000000000000000000 ) ) ;
#11728=VERTEX_POINT ( 'NONE', #33618 ) ;
#11740=ORIENTED_EDGE ( 'NONE', *, *, #32747, .F. ) ;
#11744=AXIS2_PLACEMENT_3D ( 'NONE', #12071, #34583, #4536 ) ;
#11746=CARTESIAN_POINT ( 'NONE',  ( 0.000000000000000000, -51.19683565102450729, 9.104066087303298360 ) ) ;
#11751=DIRECTION ( 'NONE',  ( 0.000000000000000000, 0.000000000000000000, 1.000000000000000000 ) ) ;
#11752=DIRECTION ( 'NONE',  ( 0.000000000000000000, -0.9048270524660235736, 0.4257792915650641663 ) ) ;
#11765=DIRECTION ( 'NONE',  ( -1.000000000000000000, 0.000000000000000000, 0.000000000000000000 ) ) ;
#11766=ORIENTED_EDGE ( 'NONE', *, *, #29293, .T. ) ;
#11773=ORIENTED_EDGE ( 'NONE', *, *, #20076, .F. ) ;
#11777=ORIENTED_EDGE ( 'NONE', *, *, #18109, .F. ) ;
#11778=ORIENTED_EDGE ( 'NONE', *, *, #31008, .T. ) ;
#11787=CARTESIAN_POINT ( 'NONE',  ( 7.999999999999992895, 22.43957647427220081, -41.27978878573601662 ) ) ;
#11788=VECTOR ( 'NONE', #32935, 1000.000000000000000 ) ;
#11792=ORIENTED_EDGE ( 'NONE', *, *, #15896, .F. ) ;
#11799=AXIS2_PLACEMENT_3D ( 'NONE', #32292, #13749, #21835 ) ;
#11801=FACE_OUTER_BOUND ( 'NONE', #16727, .T. ) ;
#11803=ORIENTED_EDGE ( 'NONE', *, *, #9303, .F. ) ;
#11806=CARTESIAN_POINT ( 'NONE',  ( 7.999999999999992895, -13.85708833599938217, -45.43276465116679930 ) ) ;
#11808=AXIS2_PLACEMENT_3D ( 'NONE', #35303, #9896, #10450 ) ;
#11810=CARTESIAN_POINT ( 'NONE',  ( 7.999999999999992895, -47.49120266317497396, 0.8606222198173640869 ) ) ;
#11811=DIRECTION ( 'NONE',  ( -1.000000000000000000, 0.000000000000000000, 0.000000000000000000 ) ) ;
#11815=ORIENTED_EDGE ( 'NONE', *, *, #24154, .T. ) ;
#11818=LINE ( 'NONE', #22798, #7399 ) ;
#11820=VECTOR ( 'NONE', #23263, 1000.000000000000000 ) ;
#11823=ORIENTED_EDGE ( 'NONE', *, *, #7975, .F. ) ;
#11830=AXIS2_PLACEMENT_3D ( 'NONE', #19927, #14893, #1234 ) ;
#11843=AXIS2_PLACEMENT_3D ( 'NONE', #32452, #4927, #15872 ) ;
#11844=ORIENTED_EDGE ( 'NONE', *, *, #30200, .F. ) ;
#11845=EDGE_CURVE ( 'NONE', #2557, #33795, #14465, .T. ) ;
#11865=VERTEX_POINT ( 'NONE', #15318 ) ;
#11870=VECTOR ( 'NONE', #17990, 1000.000000000000000 ) ;
#11871=EDGE_LOOP ( 'NONE', ( #6588, #19200, #17019, #24811 ) ) ;
#11881=CARTESIAN_POINT ( 'NONE',  ( 0.000000000000000000, 0.000000000000000000, 0.000000000000000000 ) ) ;
#11886=CARTESIAN_POINT ( 'NONE',  ( 7.999999999999992895, -25.61928775981074935, 45.25098998563468911 ) ) ;
#11892=EDGE_CURVE ( 'NONE', #2418, #10666, #20893, .T. ) ;
#11895=ADVANCED_FACE ( 'NONE', ( #15497 ), #29216, .T. ) ;
#11896=CARTESIAN_POINT ( 'NONE',  ( 7.999999999999992895, 30.03615769709734451, 42.44795908869000556 ) ) ;
#11897=LINE ( 'NONE', #3634, #11120 ) ;
#11910=EDGE_CURVE ( 'NONE', #13661, #1926, #21077, .T. ) ;
#11911=AXIS2_PLACEMENT_3D ( 'NONE', #4933, #4758, #26540 ) ;
#11915=EDGE_LOOP ( 'NONE', ( #3775, #20931, #8456, #15439 ) ) ;
#11916=CIRCLE ( 'NONE', #29741, 47.49900000000000944 ) ;
#11919=AXIS2_PLACEMENT_3D ( 'NONE', #32421, #24328, #10466 ) ;
#11921=ORIENTED_EDGE ( 'NONE', *, *, #35497, .T. ) ;
#11933=ADVANCED_FACE ( 'NONE', ( #34787 ), #4564, .T. ) ;
#11935=DIRECTION ( 'NONE',  ( -1.000000000000000000, -0.000000000000000000, 0.000000000000000000 ) ) ;
#11943=EDGE_CURVE ( 'NONE', #16982, #26196, #15033, .T. ) ;
#11944=CARTESIAN_POINT ( 'NONE',  ( 7.999999999999992895, 40.47821179127763003, -32.64221760512717196 ) ) ;
#11956=DIRECTION ( 'NONE',  ( 0.000000000000000000, 0.000000000000000000, 1.000000000000000000 ) ) ;
#11958=CIRCLE ( 'NONE', #5646, 47.49900000000001654 ) ;
#11963=ORIENTED_EDGE ( 'NONE', *, *, #15171, .T. ) ;
#11969=VERTEX_POINT ( 'NONE', #15674 ) ;
#11974=EDGE_CURVE ( 'NONE', #15571, #29853, #35193, .T. ) ;
#11981=CYLINDRICAL_SURFACE ( 'NONE', #26615, 20.00000000000000355 ) ;
#11983=DIRECTION ( 'NONE',  ( -1.000000000000000000, 0.000000000000000000, 0.000000000000000000 ) ) ;
#11989=DIRECTION ( 'NONE',  ( 0.000000000000000000, 0.4817536741017163782, -0.8763066800438630288 ) ) ;
#11994=DIRECTION ( 'NONE',  ( 0.000000000000000000, 0.000000000000000000, 1.000000000000000000 ) ) ;
#11997=VERTEX_POINT ( 'NONE', #18026 ) ;
#11999=CYLINDRICAL_SURFACE ( 'NONE', #35392, 20.00000000000000355 ) ;
#12002=ORIENTED_EDGE ( 'NONE', *, *, #11127, .F. ) ;
#12010=PRODUCT_CONTEXT ( 'NONE', #31941, 'mechanical' ) ;
#12011=DIRECTION ( 'NONE',  ( 0.000000000000000000, 0.000000000000000000, 1.000000000000000000 ) ) ;
#12012=ORIENTED_EDGE ( 'NONE', *, *, #18508, .F. ) ;
#12015=EDGE_CURVE ( 'NONE', #20300, #17882, #31723, .T. ) ;
#12019=CARTESIAN_POINT ( 'NONE',  ( -9.999999999999994671, 0.000000000000000000, 0.000000000000000000 ) ) ;
#12035=CARTESIAN_POINT ( 'NONE',  ( 7.999999999999992895, 0.000000000000000000, 0.000000000000000000 ) ) ;
#12039=ORIENTED_EDGE ( 'NONE', *, *, #10364, .F. ) ;
#12044=CIRCLE ( 'NONE', #6876, 52.00000000000000711 ) ;
#12056=ORIENTED_EDGE ( 'NONE', *, *, #21968, .T. ) ;
#12070=CARTESIAN_POINT ( 'NONE',  ( 7.999999999999992895, 0.000000000000000000, 0.000000000000000000 ) ) ;
#12071=CARTESIAN_POINT ( 'NONE',  ( 7.999999999999992895, 0.000000000000000000, 0.000000000000000000 ) ) ;
#12075=DIRECTION ( 'NONE',  ( 0.000000000000000000, 0.5877852522924685852, 0.8090169943749507819 ) ) ;
#12081=CARTESIAN_POINT ( 'NONE',  ( 7.999999999999992895, -51.19683565102450729, 9.104066087303298360 ) ) ;
#12082=AXIS2_PLACEMENT_3D ( 'NONE', #22942, #17532, #1349 ) ;
#12096=ORIENTED_EDGE ( 'NONE', *, *, #16687, .T. ) ;
#12097=ORIENTED_EDGE ( 'NONE', *, *, #23308, .F. ) ;
#12100=EDGE_CURVE ( 'NONE', #6142, #31456, #27142, .T. ) ;
#12115=UNCERTAINTY_MEASURE_WITH_UNIT (LENGTH_MEASURE( 1.000000000000000082E-05 ), #4060, 'distance_accuracy_value', 'NONE');
#12116=CARTESIAN_POINT ( 'NONE',  ( 0.000000000000000000, -24.47917365149978153, 45.87777302070926311 ) ) ;
#12119=CIRCLE ( 'NONE', #12693, 52.00000000000000711 ) ;
#12120=DIRECTION ( 'NONE',  ( 0.000000000000000000, -0.6845471059286951654, 0.7289686274214054462 ) ) ;
#12126=DIRECTION ( 'NONE',  ( -1.000000000000000000, 0.000000000000000000, -0.000000000000000000 ) ) ;
#12129=ADVANCED_FACE ( 'NONE', ( #24338 ), #35506, .T. ) ;
#12133=ADVANCED_FACE ( 'NONE', ( #24862 ), #5611, .T. ) ;
#12145=ADVANCED_FACE ( 'NONE', ( #30268 ), #27579, .T. ) ;
#12196=CARTESIAN_POINT ( 'NONE',  ( 7.999999999999992895, -39.64889472655756464, 33.64468972902493960 ) ) ;
#12199=CIRCLE ( 'NONE', #18513, 20.00000000000000711 ) ;
#12203=DIRECTION ( 'NONE',  ( -1.000000000000000000, -0.000000000000000000, -0.000000000000000000 ) ) ;
#12205=DIRECTION ( 'NONE',  ( -1.000000000000000000, -0.000000000000000000, -0.000000000000000000 ) ) ;
#12209=CARTESIAN_POINT ( 'NONE',  ( 0.000000000000000000, -43.83938735307256707, -18.28286404005846677 ) ) ;
#12210=CIRCLE ( 'NONE', #20816, 52.00000000000000711 ) ;
#12213=CARTESIAN_POINT ( 'NONE',  ( 7.999999999999992895, 44.61570720899095477, -14.73072383765580717 ) ) ;
#12214=ORIENTED_EDGE ( 'NONE', *, *, #5165, .F. ) ;
#12225=DIRECTION ( 'NONE',  ( 0.000000000000000000, -0.9510565162951565288, 0.3090169943749383474 ) ) ;
#12233=DIRECTION ( 'NONE',  ( -1.000000000000000000, 0.000000000000000000, 0.000000000000000000 ) ) ;
#12234=ORIENTED_EDGE ( 'NONE', *, *, #18508, .T. ) ;
#12241=ORIENTED_EDGE ( 'NONE', *, *, #587, .T. ) ;
#12252=EDGE_LOOP ( 'NONE', ( #10191, #7038, #33614, #16507 ) ) ;
#12253=CARTESIAN_POINT ( 'NONE',  ( 0.000000000000000000, 0.000000000000000000, 0.000000000000000000 ) ) ;
#12254=DIRECTION ( 'NONE',  ( 1.000000000000000000, 0.000000000000000000, 0.000000000000000000 ) ) ;
#12258=DIRECTION ( 'NONE',  ( -1.000000000000000000, 0.000000000000000000, 0.000000000000000000 ) ) ;
#12275=FACE_OUTER_BOUND ( 'NONE', #1061, .T. ) ;
#12280=ORIENTED_EDGE ( 'NONE', *, *, #4919, .F. ) ;
#12284=ORIENTED_EDGE ( 'NONE', *, *, #2120, .T. ) ;
#12288=CARTESIAN_POINT ( 'NONE',  ( 7.999999999999992895, 42.03146605346787368, 22.12489237027333289 ) ) ;
#12291=FACE_OUTER_BOUND ( 'NONE', #7029, .T. ) ;
#12306=CIRCLE ( 'NONE', #806, 52.00000000000000711 ) ;
#12307=VERTEX_POINT ( 'NONE', #34163 ) ;
#12308=CARTESIAN_POINT ( 'NONE',  ( 7.999999999999992895, -46.77034588191288833, -22.72740077717277885 ) ) ;
#12311=ORIENTED_EDGE ( 'NONE', *, *, #24960, .T. ) ;
#12318=ORIENTED_EDGE ( 'NONE', *, *, #27523, .T. ) ;
#12320=AXIS2_PLACEMENT_3D ( 'NONE', #31833, #34191, #23555 ) ;
#12321=CIRCLE ( 'NONE', #11744, 52.00000000000000711 ) ;
#12325=CARTESIAN_POINT ( 'NONE',  ( 4.000000000000003553, -39.64889472655708857, -33.64468972902551513 ) ) ;
#12329=CARTESIAN_POINT ( 'NONE',  ( 7.999999999999992895, -36.06787431788704623, 37.45808914225477793 ) ) ;
#12337=CARTESIAN_POINT ( 'NONE',  ( 7.999999999999992895, 51.85248208264524550, -3.914090171285633524 ) ) ;
#12342=CARTESIAN_POINT ( 'NONE',  ( 7.999999999999992895, 0.000000000000000000, 0.000000000000000000 ) ) ;
#12349=AXIS2_PLACEMENT_3D ( 'NONE', #30591, #11338, #22304 ) ;
#12351=ORIENTED_EDGE ( 'NONE', *, *, #7661, .F. ) ;
#12355=EDGE_CURVE ( 'NONE', #31732, #12363, #21384, .T. ) ;
#12359=LINE ( 'NONE', #26410, #16578 ) ;
#12360=CARTESIAN_POINT ( 'NONE',  ( 7.999999999999992895, 2.123073309835184830, 47.45152853935336168 ) ) ;
#12361=CARTESIAN_POINT ( 'NONE',  ( 0.000000000000000000, 42.41764978026606059, -20.20639853260303198 ) ) ;
#12362=ORIENTED_EDGE ( 'NONE', *, *, #21354, .T. ) ;
#12363=VERTEX_POINT ( 'NONE', #4990 ) ;
#12370=EDGE_CURVE ( 'NONE', #25880, #4840, #1885, .T. ) ;
#12386=DIRECTION ( 'NONE',  ( 0.000000000000000000, 0.9510565162951521989, 0.3090169943749515036 ) ) ;
#12387=ORIENTED_EDGE ( 'NONE', *, *, #34596, .F. ) ;
#12394=ORIENTED_EDGE ( 'NONE', *, *, #28206, .T. ) ;
#12396=DIRECTION ( 'NONE',  ( 0.000000000000000000, 0.000000000000000000, -1.000000000000000000 ) ) ;
#12398=FACE_OUTER_BOUND ( 'NONE', #31871, .T. ) ;
#12403=ADVANCED_FACE ( 'NONE', ( #10561 ), #13443, .T. ) ;
#12412=CARTESIAN_POINT ( 'NONE',  ( 7.999999999999992895, 5.667686777402359155, -46.64153600743598105 ) ) ;
#12418=AXIS2_PLACEMENT_3D ( 'NONE', #17510, #14452, #17870 ) ;
#12419=CYLINDRICAL_SURFACE ( 'NONE', #24061, 47.49900000000001654 ) ;
#12421=CARTESIAN_POINT ( 'NONE',  ( 0.000000000000000000, 0.000000000000000000, 0.000000000000000000 ) ) ;
#12424=CIRCLE ( 'NONE', #5548, 20.00000000000000355 ) ;
#12425=AXIS2_PLACEMENT_3D ( 'NONE', #687, #21945, #30068 ) ;
#12430=DIRECTION ( 'NONE',  ( -1.000000000000000000, -0.000000000000000000, -0.000000000000000000 ) ) ;
#12431=FACE_OUTER_BOUND ( 'NONE', #16458, .T. ) ;
#12446=DIRECTION ( 'NONE',  ( 0.000000000000000000, 0.000000000000000000, 1.000000000000000000 ) ) ;
#12448=VERTEX_POINT ( 'NONE', #21708 ) ;
#12449=ORIENTED_EDGE ( 'NONE', *, *, #33171, .T. ) ;
#12454=DIRECTION ( 'NONE',  ( -1.000000000000000000, 0.000000000000000000, 0.000000000000000000 ) ) ;
#12456=ORIENTED_EDGE ( 'NONE', *, *, #275, .T. ) ;
#12468=CARTESIAN_POINT ( 'NONE',  ( 4.000000000000003553, -44.25018368420724357, -27.31155879685229237 ) ) ;
#12473=LINE ( 'NONE', #28857, #11820 ) ;
#12474=CYLINDRICAL_SURFACE ( 'NONE', #29041, 20.00000000000000711 ) ;
#12476=ORIENTED_EDGE ( 'NONE', *, *, #18756, .F. ) ;
#12484=DIRECTION ( 'NONE',  ( 0.000000000000000000, 0.9822872507286892763, -0.1873813145857214646 ) ) ;
#12491=CARTESIAN_POINT ( 'NONE',  ( 0.000000000000000000, 49.25004636492413823, -16.68630974939705425 ) ) ;
#12502=DIRECTION ( 'NONE',  ( -1.000000000000000000, 0.000000000000000000, -0.000000000000000000 ) ) ;
#12506=AXIS2_PLACEMENT_3D ( 'NONE', #5942, #19445, #25031 ) ;
#12510=ADVANCED_FACE ( 'NONE', ( #34886 ), #27305, .T. ) ;
#12511=AXIS2_PLACEMENT_3D ( 'NONE', #10545, #35585, #10909 ) ;
#12513=CARTESIAN_POINT ( 'NONE',  ( 7.999999999999992895, 38.92705108641732892, 27.21837053747812263 ) ) ;
#12515=CARTESIAN_POINT ( 'NONE',  ( 7.999999999999992895, 42.41764978026606769, 20.20639853260304619 ) ) ;
#12517=EDGE_CURVE ( 'NONE', #7610, #34437, #23578, .T. ) ;
#12523=AXIS2_PLACEMENT_3D ( 'NONE', #28503, #30680, #25093 ) ;
#12532=FACE_OUTER_BOUND ( 'NONE', #8630, .T. ) ;
#12551=ORIENTED_EDGE ( 'NONE', *, *, #33117, .F. ) ;
#12552=EDGE_CURVE ( 'NONE', #28129, #18999, #24956, .T. ) ;
#12554=CARTESIAN_POINT ( 'NONE',  ( 7.999999999999992895, 41.20225022064637699, 23.63323037071417332 ) ) ;
#12556=EDGE_CURVE ( 'NONE', #31962, #26553, #16475, .T. ) ;
#12558=DIRECTION ( 'NONE',  ( 0.000000000000000000, 0.000000000000000000, 1.000000000000000000 ) ) ;
#12559=DIRECTION ( 'NONE',  ( -1.000000000000000000, -0.000000000000000000, -0.000000000000000000 ) ) ;
#12571=DIRECTION ( 'NONE',  ( 0.000000000000000000, 0.000000000000000000, -1.000000000000000000 ) ) ;
#12574=FACE_OUTER_BOUND ( 'NONE', #28922, .T. ) ;
#12575=ORIENTED_EDGE ( 'NONE', *, *, #6007, .T. ) ;
#12577=LINE ( 'NONE', #24104, #34798 ) ;
#12581=DIRECTION ( 'NONE',  ( 1.000000000000000000, 0.000000000000000000, 0.000000000000000000 ) ) ;
#12584=ORIENTED_EDGE ( 'NONE', *, *, #20902, .F. ) ;
#12586=AXIS2_PLACEMENT_3D ( 'NONE', #32267, #32439, #10658 ) ;
#12594=CARTESIAN_POINT ( 'NONE',  ( 7.999999999999992895, 0.000000000000000000, 0.000000000000000000 ) ) ;
#12606=AXIS2_PLACEMENT_3D ( 'NONE', #33402, #8725, #30535 ) ;
#12612=CARTESIAN_POINT ( 'NONE',  ( 0.000000000000000000, 35.20873326984081331, 31.88259874184044662 ) ) ;
#12623=ORIENTED_EDGE ( 'NONE', *, *, #16121, .F. ) ;
#12629=VERTEX_POINT ( 'NONE', #12612 ) ;
#12643=AXIS2_PLACEMENT_3D ( 'NONE', #17802, #31147, #1086 ) ;
#12651=VERTEX_POINT ( 'NONE', #21758 ) ;
#12659=FACE_OUTER_BOUND ( 'NONE', #23340, .T. ) ;
#12663=CARTESIAN_POINT ( 'NONE',  ( -9.999999999999994671, 0.000000000000000000, 0.000000000000000000 ) ) ;
#12667=CIRCLE ( 'NONE', #35115, 47.49900000000002365 ) ;
#12668=DIRECTION ( 'NONE',  ( 0.000000000000000000, 0.000000000000000000, 1.000000000000000000 ) ) ;
#12673=VECTOR ( 'NONE', #8626, 1000.000000000000000 ) ;
#12674=CIRCLE ( 'NONE', #32791, 52.00000000000000711 ) ;
#12678=ADVANCED_FACE ( 'NONE', ( #16348 ), #19231, .T. ) ;
#12679=DIRECTION ( 'NONE',  ( 0.000000000000000000, 0.000000000000000000, 1.000000000000000000 ) ) ;
#12682=ORIENTED_EDGE ( 'NONE', *, *, #34440, .F. ) ;
#12685=ORIENTED_EDGE ( 'NONE', *, *, #3578, .F. ) ;
#12693=AXIS2_PLACEMENT_3D ( 'NONE', #34813, #15340, #21102 ) ;
#12696=LINE ( 'NONE', #4607, #24910 ) ;
#12698=CYLINDRICAL_SURFACE ( 'NONE', #16308, 47.49900000000001654 ) ;
#12705=ORIENTED_EDGE ( 'NONE', *, *, #5977, .F. ) ;
#12708=CARTESIAN_POINT ( 'NONE',  ( 50.00005079999998969, 14.30000000000000071, -3.000000000000002665 ) ) ;
#12717=EDGE_CURVE ( 'NONE', #4367, #34778, #12667, .T. ) ;
#12719=FACE_OUTER_BOUND ( 'NONE', #34783, .T. ) ;
#12722=EDGE_LOOP ( 'NONE', ( #11465, #3603, #5222, #31894 ) ) ;
#12723=AXIS2_PLACEMENT_3D ( 'NONE', #26898, #1111, #19800 ) ;
#12725=DIRECTION ( 'NONE',  ( 0.000000000000000000, 0.000000000000000000, 1.000000000000000000 ) ) ;
#12728=CARTESIAN_POINT ( 'NONE',  ( 0.000000000000000000, -9.744342220503712682, 46.48873837489796301 ) ) ;
#12730=EDGE_CURVE ( 'NONE', #4610, #169, #11496, .T. ) ;
#12732=ORIENTED_EDGE ( 'NONE', *, *, #30751, .T. ) ;
#12746=DIRECTION ( 'NONE',  ( -1.000000000000000000, 0.000000000000000000, 0.000000000000000000 ) ) ;
#12748=DIRECTION ( 'NONE',  ( 0.000000000000000000, 0.000000000000000000, 1.000000000000000000 ) ) ;
#12750=DIRECTION ( 'NONE',  ( -1.000000000000000000, -0.000000000000000000, 0.000000000000000000 ) ) ;
#12760=ORIENTED_EDGE ( 'NONE', *, *, #9054, .T. ) ;
#12763=ORIENTED_EDGE ( 'NONE', *, *, #20089, .T. ) ;
#12773=ORIENTED_EDGE ( 'NONE', *, *, #12100, .T. ) ;
#12787=EDGE_CURVE ( 'NONE', #25508, #23788, #13236, .T. ) ;
#12789=FACE_OUTER_BOUND ( 'NONE', #32290, .T. ) ;
#12803=ORIENTED_EDGE ( 'NONE', *, *, #1360, .F. ) ;
#12824=EDGE_LOOP ( 'NONE', ( #33333, #22681, #20976, #9868 ) ) ;
#12829=LINE ( 'NONE', #12288, #10501 ) ;
#12831=EDGE_CURVE ( 'NONE', #20345, #13985, #5201, .T. ) ;
#12834=VECTOR ( 'NONE', #23753, 1000.000000000000000 ) ;
#12839=CARTESIAN_POINT ( 'NONE',  ( 4.000000000000003553, 24.47917365149946534, 45.87777302070943364 ) ) ;
#12840=DIRECTION ( 'NONE',  ( -1.000000000000000000, -0.000000000000000000, 0.000000000000000000 ) ) ;
#12845=AXIS2_PLACEMENT_3D ( 'NONE', #27712, #5742, #30754 ) ;
#12860=( LENGTH_UNIT ( ) NAMED_UNIT ( * ) SI_UNIT ( .MILLI., .METRE. ) );
#12864=VERTEX_POINT ( 'NONE', #25904 ) ;
#12867=DIRECTION ( 'NONE',  ( -1.000000000000000000, 0.000000000000000000, -0.000000000000000000 ) ) ;
#12869=CIRCLE ( 'NONE', #13458, 47.49900000000001654 ) ;
#12876=EDGE_CURVE ( 'NONE', #26795, #5670, #2329, .T. ) ;
#12881=CARTESIAN_POINT ( 'NONE',  ( 7.999999999999992895, 44.47301969247469344, -16.68249143361863318 ) ) ;
#12883=DIRECTION ( 'NONE',  ( 0.000000000000000000, 0.000000000000000000, -1.000000000000000000 ) ) ;
#12889=LINE ( 'NONE', #18453, #22437 ) ;
#12892=DIRECTION ( 'NONE',  ( 0.000000000000000000, 0.000000000000000000, -1.000000000000000000 ) ) ;
#12895=VERTEX_POINT ( 'NONE', #22634 ) ;
#12902=ORIENTED_EDGE ( 'NONE', *, *, #2653, .T. ) ;
#12912=ORIENTED_EDGE ( 'NONE', *, *, #32883, .F. ) ;
#12923=CIRCLE ( 'NONE', #19302, 20.00000000000000711 ) ;
#12932=CARTESIAN_POINT ( 'NONE',  ( 7.999999999999992895, 0.000000000000000000, 0.000000000000000000 ) ) ;
#12934=ORIENTED_EDGE ( 'NONE', *, *, #21354, .F. ) ;
#12937=CARTESIAN_POINT ( 'NONE',  ( 7.999999999999992895, -39.55064067543046491, -25.36340625197400200 ) ) ;
#12939=VERTEX_POINT ( 'NONE', #12209 ) ;
#12941=AXIS2_PLACEMENT_3D ( 'NONE', #14665, #5747, #1189 ) ;
#12952=DIRECTION ( 'NONE',  ( 0.000000000000000000, 0.9048270524660175784, 0.4257792915650767673 ) ) ;
#12953=CARTESIAN_POINT ( 'NONE',  ( 0.000000000000000000, 0.000000000000000000, 0.000000000000000000 ) ) ;
#12967=DIRECTION ( 'NONE',  ( -1.000000000000000000, -0.000000000000000000, -0.000000000000000000 ) ) ;
#12974=ORIENTED_EDGE ( 'NONE', *, *, #28656, .T. ) ;
#12975=EDGE_CURVE ( 'NONE', #1868, #15669, #3493, .T. ) ;
#12977=DIRECTION ( 'NONE',  ( -1.000000000000000000, 0.000000000000000000, 0.000000000000000000 ) ) ;
#12983=VERTEX_POINT ( 'NONE', #3581 ) ;
#12985=CIRCLE ( 'NONE', #2074, 20.00000000000000355 ) ;
#12998=DIRECTION ( 'NONE',  ( -1.000000000000000000, 0.000000000000000000, 0.000000000000000000 ) ) ;
#13015=DIRECTION ( 'NONE',  ( -1.000000000000000000, -0.000000000000000000, -0.000000000000000000 ) ) ;
#13022=EDGE_CURVE ( 'NONE', #574, #28112, #33455, .T. ) ;
#13027=DIRECTION ( 'NONE',  ( 0.000000000000000000, 0.9510565162951544194, -0.3090169943749448422 ) ) ;
#13031=CIRCLE ( 'NONE', #7847, 47.49900000000001654 ) ;
#13036=ORIENTED_EDGE ( 'NONE', *, *, #34637, .F. ) ;
#13041=CIRCLE ( 'NONE', #26848, 52.00000000000000711 ) ;
#13042=CARTESIAN_POINT ( 'NONE',  ( 7.999999999999992895, -44.47301969247457976, 16.68249143361895293 ) ) ;
#13043=VERTEX_POINT ( 'NONE', #20640 ) ;
#13054=FACE_OUTER_BOUND ( 'NONE', #2460, .T. ) ;
#13055=EDGE_CURVE ( 'NONE', #11602, #26957, #4298, .T. ) ;
#13062=DIRECTION ( 'NONE',  ( -1.000000000000000000, 0.000000000000000000, 0.000000000000000000 ) ) ;
#13065=ORIENTED_EDGE ( 'NONE', *, *, #23388, .T. ) ;
#13072=VERTEX_POINT ( 'NONE', #26613 ) ;
#13074=DIRECTION ( 'NONE',  ( 0.000000000000000000, 0.000000000000000000, 1.000000000000000000 ) ) ;
#13079=CARTESIAN_POINT ( 'NONE',  ( 0.000000000000000000, 0.000000000000000000, 0.000000000000000000 ) ) ;
#13109=CYLINDRICAL_SURFACE ( 'NONE', #35517, 20.00000000000000355 ) ;
#13111=CIRCLE ( 'NONE', #32624, 47.49900000000000944 ) ;
#13116=CIRCLE ( 'NONE', #1612, 20.00000000000000711 ) ;
#13118=AXIS2_PLACEMENT_3D ( 'NONE', #23565, #10427, #1791 ) ;
#13122=CYLINDRICAL_SURFACE ( 'NONE', #25308, 52.00000000000000711 ) ;
#13130=DIRECTION ( 'NONE',  ( -1.000000000000000000, 0.000000000000000000, -0.000000000000000000 ) ) ;
#13131=CYLINDRICAL_SURFACE ( 'NONE', #8862, 20.00000000000000711 ) ;
#13132=ORIENTED_EDGE ( 'NONE', *, *, #31733, .F. ) ;
#13135=DIRECTION ( 'NONE',  ( 0.000000000000000000, 0.000000000000000000, 1.000000000000000000 ) ) ;
#13143=AXIS2_PLACEMENT_3D ( 'NONE', #7136, #31801, #5128 ) ;
#13150=CARTESIAN_POINT ( 'NONE',  ( 0.000000000000000000, 15.49408907645234734, -44.90087086784577508 ) ) ;
#13158=CARTESIAN_POINT ( 'NONE',  ( 7.999999999999992895, 11.46872990052444408, -45.56340405422432127 ) ) ;
#13161=CARTESIAN_POINT ( 'NONE',  ( 7.999999999999992895, 0.000000000000000000, 0.000000000000000000 ) ) ;
#13167=AXIS2_PLACEMENT_3D ( 'NONE', #2224, #18925, #27585 ) ;
#13168=CARTESIAN_POINT ( 'NONE',  ( 4.000000000000003553, -39.64889472655756464, 33.64468972902493960 ) ) ;
#13175=DIRECTION ( 'NONE',  ( 1.000000000000000000, -0.000000000000000000, -0.000000000000000000 ) ) ;
#13178=ORIENTED_EDGE ( 'NONE', *, *, #4919, .T. ) ;
#13186=AXIS2_PLACEMENT_3D ( 'NONE', #31051, #20045, #22401 ) ;
#13187=ADVANCED_FACE ( 'NONE', ( #9685 ), #10037, .T. ) ;
#13191=CIRCLE ( 'NONE', #3425, 52.00000000000000711 ) ;
#13205=CARTESIAN_POINT ( 'NONE',  ( 0.000000000000000000, 0.000000000000000000, 0.000000000000000000 ) ) ;
#13211=EDGE_LOOP ( 'NONE', ( #13369, #4555, #15620, #3914 ) ) ;
#13214=ADVANCED_FACE ( 'NONE', ( #6976 ), #18492, .T. ) ;
#13236=CIRCLE ( 'NONE', #20676, 52.00000000000000711 ) ;
#13250=CARTESIAN_POINT ( 'NONE',  ( 0.000000000000000000, -13.85708833600000744, 45.43276465116660745 ) ) ;
#13257=ORIENTED_EDGE ( 'NONE', *, *, #23440, .F. ) ;
#13260=CARTESIAN_POINT ( 'NONE',  ( 7.999999999999992895, 39.78933988720114456, 24.98727647985016276 ) ) ;
#13262=ORIENTED_EDGE ( 'NONE', *, *, #22014, .T. ) ;
#13266=ADVANCED_FACE ( 'NONE', ( #24966 ), #290, .T. ) ;
#13267=ORIENTED_EDGE ( 'NONE', *, *, #15244, .F. ) ;
#13289=DIRECTION ( 'NONE',  ( 0.000000000000000000, 0.000000000000000000, 1.000000000000000000 ) ) ;
#13293=ORIENTED_EDGE ( 'NONE', *, *, #20765, .T. ) ;
#13294=CIRCLE ( 'NONE', #4102, 20.00000000000001421 ) ;
#13298=DIRECTION ( 'NONE',  ( -1.000000000000000000, 0.000000000000000000, -0.000000000000000000 ) ) ;
#13303=DIRECTION ( 'NONE',  ( 0.000000000000000000, 0.000000000000000000, 1.000000000000000000 ) ) ;
#13304=ORIENTED_EDGE ( 'NONE', *, *, #14514, .T. ) ;
#13308=CARTESIAN_POINT ( 'NONE',  ( -9.999999999999994671, 0.000000000000000000, 0.000000000000000000 ) ) ;
#13309=DIRECTION ( 'NONE',  ( 0.000000000000000000, 0.000000000000000000, 1.000000000000000000 ) ) ;
#13311=FACE_OUTER_BOUND ( 'NONE', #33437, .T. ) ;
#13318=ORIENTED_EDGE ( 'NONE', *, *, #32639, .F. ) ;
#13319=DIRECTION ( 'NONE',  ( -1.000000000000000000, -0.000000000000000000, -0.000000000000000000 ) ) ;
#13326=FACE_OUTER_BOUND ( 'NONE', #18286, .T. ) ;
#13331=DIRECTION ( 'NONE',  ( 0.000000000000000000, 0.000000000000000000, 1.000000000000000000 ) ) ;
#13336=VERTEX_POINT ( 'NONE', #14667 ) ;
#13338=CYLINDRICAL_SURFACE ( 'NONE', #14059, 20.00000000000000355 ) ;
#13339=ORIENTED_EDGE ( 'NONE', *, *, #1421, .T. ) ;
#13341=CARTESIAN_POINT ( 'NONE',  ( 0.000000000000000000, 0.000000000000000000, 0.000000000000000000 ) ) ;
#13354=VERTEX_POINT ( 'NONE', #14316 ) ;
#13362=DIRECTION ( 'NONE',  ( 0.000000000000000000, -0.3681245526846654292, -0.9297764858882563432 ) ) ;
#13369=ORIENTED_EDGE ( 'NONE', *, *, #28860, .F. ) ;
#13371=DIRECTION ( 'NONE',  ( -1.000000000000000000, 0.000000000000000000, 0.000000000000000000 ) ) ;
#13372=CARTESIAN_POINT ( 'NONE',  ( 4.000000000000003553, -24.47917365149914914, -45.87777302070961127 ) ) ;
#13378=DIRECTION ( 'NONE',  ( 0.000000000000000000, 0.4817536741017163782, -0.8763066800438630288 ) ) ;
#13382=ORIENTED_EDGE ( 'NONE', *, *, #18756, .T. ) ;
#13385=AXIS2_PLACEMENT_3D ( 'NONE', #21443, #8118, #32440 ) ;
#13390=CYLINDRICAL_SURFACE ( 'NONE', #34230, 52.00000000000000711 ) ;
#13391=ORIENTED_EDGE ( 'NONE', *, *, #17830, .T. ) ;
#13394=CARTESIAN_POINT ( 'NONE',  ( 7.999999999999992895, 0.000000000000000000, 0.000000000000000000 ) ) ;
#13397=CIRCLE ( 'NONE', #734, 47.49900000000001654 ) ;
#13400=CARTESIAN_POINT ( 'NONE',  ( 0.000000000000000000, -3.840921266750157326, 47.34345070675169609 ) ) ;
#13416=EDGE_LOOP ( 'NONE', ( #27002, #16952, #2298, #18204 ) ) ;
#13418=DIRECTION ( 'NONE',  ( -1.000000000000000000, -0.000000000000000000, -0.000000000000000000 ) ) ;
#13422=DIRECTION ( 'NONE',  ( -1.000000000000000000, 0.000000000000000000, 0.000000000000000000 ) ) ;
#13426=VERTEX_POINT ( 'NONE', #9106 ) ;
#13433=ORIENTED_EDGE ( 'NONE', *, *, #34467, .F. ) ;
#13435=ORIENTED_EDGE ( 'NONE', *, *, #21723, .F. ) ;
#13441=ORIENTED_EDGE ( 'NONE', *, *, #973, .T. ) ;
#13442=EDGE_LOOP ( 'NONE', ( #16057, #14556, #30729, #13939 ) ) ;
#13443=CYLINDRICAL_SURFACE ( 'NONE', #20214, 52.00000000000000711 ) ;
#13457=CYLINDRICAL_SURFACE ( 'NONE', #30742, 47.49900000000001654 ) ;
#13458=AXIS2_PLACEMENT_3D ( 'NONE', #4173, #3810, #25779 ) ;
#13466=DIRECTION ( 'NONE',  ( -1.000000000000000000, 0.000000000000000000, 0.000000000000000000 ) ) ;
#13467=EDGE_CURVE ( 'NONE', #22983, #3168, #19357, .T. ) ;
#13474=LINE ( 'NONE', #2864, #16557 ) ;
#13483=AXIS2_PLACEMENT_3D ( 'NONE', #23227, #12254, #34220 ) ;
#13484=EDGE_CURVE ( 'NONE', #33840, #7659, #3865, .T. ) ;
#13486=CARTESIAN_POINT ( 'NONE',  ( 7.999999999999992895, 0.000000000000000000, 0.000000000000000000 ) ) ;
#13488=VERTEX_POINT ( 'NONE', #25497 ) ;
#13498=DIRECTION ( 'NONE',  ( 0.000000000000000000, -0.9510565162951565288, 0.3090169943749382919 ) ) ;
#13501=ORIENTED_EDGE ( 'NONE', *, *, #6564, .T. ) ;
#13509=EDGE_CURVE ( 'NONE', #7270, #29218, #15887, .T. ) ;
#13516=ORIENTED_EDGE ( 'NONE', *, *, #4009, .F. ) ;
#13518=VECTOR ( 'NONE', #7162, 1000.000000000000000 ) ;
#13531=DIRECTION ( 'NONE',  ( 0.000000000000000000, 0.000000000000000000, 1.000000000000000000 ) ) ;
#13532=ORIENTED_EDGE ( 'NONE', *, *, #12831, .T. ) ;
#13536=EDGE_CURVE ( 'NONE', #26957, #9355, #6131, .T. ) ;
#13537=CYLINDRICAL_SURFACE ( 'NONE', #32343, 47.49900000000001654 ) ;
#13542=FACE_OUTER_BOUND ( 'NONE', #23420, .T. ) ;
#13548=CARTESIAN_POINT ( 'NONE',  ( 7.999999999999992895, -39.64889472655708857, -33.64468972902551513 ) ) ;
#13559=VERTEX_POINT ( 'NONE', #26031 ) ;
#13564=DIRECTION ( 'NONE',  ( 0.000000000000000000, 0.000000000000000000, 1.000000000000000000 ) ) ;
#13568=CARTESIAN_POINT ( 'NONE',  ( 7.999999999999992895, -32.00046193115124282, -34.40241257139719977 ) ) ;
#13578=CIRCLE ( 'NONE', #11843, 47.49900000000001654 ) ;
#13579=CARTESIAN_POINT ( 'NONE',  ( 7.999999999999992895, -15.49408907645140943, -44.90087086784610904 ) ) ;
#13582=FACE_OUTER_BOUND ( 'NONE', #2123, .T. ) ;
#13587=ORIENTED_EDGE ( 'NONE', *, *, #2777, .T. ) ;
#13591=CARTESIAN_POINT ( 'NONE',  ( 7.999999999999992895, -19.44205635905572649, 43.33776004284603545 ) ) ;
#13592=DIRECTION ( 'NONE',  ( 0.000000000000000000, -6.938893903907226800E-15, 1.000000000000000000 ) ) ;
#13598=CARTESIAN_POINT ( 'NONE',  ( 7.999999999999992895, 0.000000000000000000, 0.000000000000000000 ) ) ;
#13599=DIRECTION ( 'NONE',  ( -1.000000000000000000, -0.000000000000000000, -0.000000000000000000 ) ) ;
#13601=ORIENTED_EDGE ( 'NONE', *, *, #20357, .F. ) ;
#13604=EDGE_LOOP ( 'NONE', ( #29671, #26588, #29152, #13501 ) ) ;
#13607=EDGE_CURVE ( 'NONE', #8021, #7666, #9812, .T. ) ;
#13614=DIRECTION ( 'NONE',  ( -1.000000000000000000, 0.000000000000000000, 0.000000000000000000 ) ) ;
#13620=AXIS2_PLACEMENT_3D ( 'NONE', #23865, #9643, #23681 ) ;
#13623=DIRECTION ( 'NONE',  ( -1.000000000000000000, 0.000000000000000000, 0.000000000000000000 ) ) ;
#13625=LINE ( 'NONE', #16486, #24589 ) ;
#13627=AXIS2_PLACEMENT_3D ( 'NONE', #15422, #12746, #20999 ) ;
#13636=DIRECTION ( 'NONE',  ( -1.000000000000000000, -0.000000000000000000, 0.000000000000000000 ) ) ;
#13639=CIRCLE ( 'NONE', #33173, 20.00000000000000000 ) ;
#13649=VECTOR ( 'NONE', #17923, 1000.000000000000000 ) ;
#13650=ORIENTED_EDGE ( 'NONE', *, *, #5305, .F. ) ;
#13653=DIRECTION ( 'NONE',  ( -1.000000000000000000, -0.000000000000000000, 0.000000000000000000 ) ) ;
#13656=EDGE_CURVE ( 'NONE', #10641, #6851, #23863, .T. ) ;
#13661=VERTEX_POINT ( 'NONE', #4618 ) ;
#13662=AXIS2_PLACEMENT_3D ( 'NONE', #10396, #12559, #23714 ) ;
#13665=CARTESIAN_POINT ( 'NONE',  ( 0.000000000000000000, -36.05989434073592292, -30.12041790338657066 ) ) ;
#13681=CYLINDRICAL_SURFACE ( 'NONE', #11167, 52.00000000000000711 ) ;
#13683=CYLINDRICAL_SURFACE ( 'NONE', #12425, 20.00000000000000711 ) ;
#13684=EDGE_LOOP ( 'NONE', ( #29759, #7269, #22534, #34604 ) ) ;
#13690=ORIENTED_EDGE ( 'NONE', *, *, #33770, .T. ) ;
#13695=CIRCLE ( 'NONE', #30374, 11.00000000000000000 ) ;
#13697=CIRCLE ( 'NONE', #22286, 20.00000000000000355 ) ;
#13699=DIRECTION ( 'NONE',  ( 0.000000000000000000, 0.000000000000000000, 1.000000000000000000 ) ) ;
#13700=VERTEX_POINT ( 'NONE', #8173 ) ;
#13701=ORIENTED_EDGE ( 'NONE', *, *, #11285, .T. ) ;
#13718=DIRECTION ( 'NONE',  ( -1.000000000000000000, -0.000000000000000000, 0.000000000000000000 ) ) ;
#13743=ORIENTED_EDGE ( 'NONE', *, *, #11299, .F. ) ;
#13748=ADVANCED_FACE ( 'NONE', ( #27105 ), #22038, .T. ) ;
#13749=DIRECTION ( 'NONE',  ( -1.000000000000000000, 0.000000000000000000, 0.000000000000000000 ) ) ;
#13751=ORIENTED_EDGE ( 'NONE', *, *, #30713, .F. ) ;
#13764=ORIENTED_EDGE ( 'NONE', *, *, #22660, .T. ) ;
#13774=DIRECTION ( 'NONE',  ( -1.000000000000000000, -0.000000000000000000, -0.000000000000000000 ) ) ;
#13778=AXIS2_PLACEMENT_3D ( 'NONE', #4667, #23729, #32187 ) ;
#13779=CARTESIAN_POINT ( 'NONE',  ( 4.000000000000003553, 19.74581912682842244, 48.10512059033400334 ) ) ;
#13787=VERTEX_POINT ( 'NONE', #18626 ) ;
#13795=CYLINDRICAL_SURFACE ( 'NONE', #16049, 20.00000000000000355 ) ;
#13800=CARTESIAN_POINT ( 'NONE',  ( 7.999999999999992895, -7.162210897276087174, 51.50439529848826936 ) ) ;
#13821=ORIENTED_EDGE ( 'NONE', *, *, #28864, .T. ) ;
#13822=EDGE_CURVE ( 'NONE', #7838, #27467, #5023, .T. ) ;
#13823=EDGE_LOOP ( 'NONE', ( #28479, #4134, #8143, #22307 ) ) ;
#13825=CIRCLE ( 'NONE', #16134, 20.00000000000000355 ) ;
#13827=DIRECTION ( 'NONE',  ( 0.000000000000000000, 0.000000000000000000, -1.000000000000000000 ) ) ;
#13842=VECTOR ( 'NONE', #35178, 1000.000000000000000 ) ;
#13850=CARTESIAN_POINT ( 'NONE',  ( 0.000000000000000000, -27.43636312076347394, 38.14186064215141414 ) ) ;
#13853=ADVANCED_FACE ( 'NONE', ( #27157 ), #5199, .T. ) ;
#13862=EDGE_CURVE ( 'NONE', #8656, #31607, #7321, .T. ) ;
#13866=CARTESIAN_POINT ( 'NONE',  ( 7.999999999999992895, 39.55064067543098361, -25.36340625197317067 ) ) ;
#13867=FACE_OUTER_BOUND ( 'NONE', #22395, .T. ) ;
#13868=EDGE_LOOP ( 'NONE', ( #19600, #7088, #14634, #33647 ) ) ;
#13870=DIRECTION ( 'NONE',  ( -1.000000000000000000, 0.000000000000000000, -0.000000000000000000 ) ) ;
#13876=DIRECTION ( 'NONE',  ( 0.000000000000000000, -0.2486898871648622333, 0.9685831611286292997 ) ) ;
#13886=DIRECTION ( 'NONE',  ( 0.000000000000000000, 0.000000000000000000, -1.000000000000000000 ) ) ;
#13888=EDGE_CURVE ( 'NONE', #28224, #13661, #6719, .T. ) ;
#13891=ORIENTED_EDGE ( 'NONE', *, *, #18479, .F. ) ;
#13894=DIRECTION ( 'NONE',  ( -1.000000000000000000, -0.000000000000000000, 0.000000000000000000 ) ) ;
#13904=LINE ( 'NONE', #24891, #16473 ) ;
#13905=EDGE_CURVE ( 'NONE', #5721, #8621, #11916, .T. ) ;
#13906=ORIENTED_EDGE ( 'NONE', *, *, #2737, .T. ) ;
#13936=CYLINDRICAL_SURFACE ( 'NONE', #2760, 20.00000000000000355 ) ;
#13939=ORIENTED_EDGE ( 'NONE', *, *, #23028, .T. ) ;
#13940=CARTESIAN_POINT ( 'NONE',  ( 4.000000000000003553, -40.47821179127737423, 32.64221760512746329 ) ) ;
#13942=CIRCLE ( 'NONE', #15076, 47.49900000000001654 ) ;
#13943=DIRECTION ( 'NONE',  ( -1.000000000000000000, 0.000000000000000000, 0.000000000000000000 ) ) ;
#13952=DIRECTION ( 'NONE',  ( -1.000000000000000000, -0.000000000000000000, 0.000000000000000000 ) ) ;
#13955=ORIENTED_EDGE ( 'NONE', *, *, #2897, .F. ) ;
#13959=CARTESIAN_POINT ( 'NONE',  ( 7.999999999999992895, -46.21320724403641833, -10.97699764142004497 ) ) ;
#13965=CIRCLE ( 'NONE', #30649, 20.00000000000000711 ) ;
#13967=CIRCLE ( 'NONE', #30653, 20.00000000000000711 ) ;
#13969=CARTESIAN_POINT ( 'NONE',  ( 7.999999999999992895, -20.99948489194393275, -42.60488980472803888 ) ) ;
#13970=DIRECTION ( 'NONE',  ( 0.000000000000000000, -0.5877852522924624790, -0.8090169943749551118 ) ) ;
#13982=LINE ( 'NONE', #32722, #23876 ) ;
#13984=CARTESIAN_POINT ( 'NONE',  ( 7.999999999999992895, 0.000000000000000000, 0.000000000000000000 ) ) ;
#13985=VERTEX_POINT ( 'NONE', #5370 ) ;
#13987=AXIS2_PLACEMENT_3D ( 'NONE', #2237, #35521, #5107 ) ;
#13988=CARTESIAN_POINT ( 'NONE',  ( 0.000000000000000000, 46.19362259308833529, 8.585149169758651055 ) ) ;
#13989=AXIS2_PLACEMENT_3D ( 'NONE', #22290, #16345, #24829 ) ;
#13998=EDGE_LOOP ( 'NONE', ( #6730, #34726, #989, #30920, #20650, #2855, #22424, #23796, #12732, #25039, #27715, #1237, #22643, #7170, #31957, #31795, #19279, #26684, #7370, #21346, #3352, #26805, #15785, #32988, #20195, #29098, #14793, #17577, #6514, #22268, #295, #2931, #14503, #14581, #5511, #28841, #29284, #19548, #33083, #24119, #1915, #26836, #23612, #32325, #12280, #22972, #604, #24173, #25181, #27213, #24356, #24367, #21697, #23804, #17826, #28743, #19407, #1921, #4261, #20568, #16155, #23269, #28965, #3214, #3878, #18635, #23622, #24232, #34161, #27991, #22657, #13391, #3390, #25932, #35063, #4427, #28667, #10608, #2806, #5679, #556, #19243, #16590, #15760, #19771, #17206, #19174, #23935, #5583, #15757, #30658, #34961, #20583, #34816, #20329, #3608, #3457, #24245, #1463, #32909, #18425, #12456, #34829, #6318, #28286, #28998, #29375, #14833, #9736, #15566, #6516, #10381, #6206, #34224, #10986, #14770, #25550, #28435, #26277, #33865, #16561, #3473, #585, #29415, #22883, #22930, #20866, #28060, #34376, #26224, #10145, #30833, #26403, #10391, #13382, #8197, #16366, #29198, #34290, #10911, #30810, #3083, #19635, #15487, #33295, #7411, #6096, #868, #4139, #8790, #12394, #744, #10648, #15676, #25730, #24137, #615, #3930, #15069, #11562, #23742, #5557, #3233, #1078, #10272, #5777, #1294, #29509, #6446, #15885, #14469, #26087, #8941, #25401, #17964, #11530, #5760, #27387, #25328, #8435, #33139, #15187, #31402, #23225, #34908, #18690, #8718, #7609, #26116, #16413, #3961, #22088, #9864, #24449, #28934, #25975, #12449, #12934, #32958, #13293, #24847, #29252, #26367 ) ) ;
#13999=AXIS2_PLACEMENT_3D ( 'NONE', #17407, #14187, #19572 ) ;
#14003=ORIENTED_EDGE ( 'NONE', *, *, #2033, .F. ) ;
#14016=DIRECTION ( 'NONE',  ( 1.000000000000000000, 0.000000000000000000, 0.000000000000000000 ) ) ;
#14018=EDGE_LOOP ( 'NONE', ( #32162, #9771, #7246, #76 ) ) ;
#14019=CARTESIAN_POINT ( 'NONE',  ( 0.000000000000000000, -44.25018368420724357, -27.31155879685229237 ) ) ;
#14033=ORIENTED_EDGE ( 'NONE', *, *, #29013, .F. ) ;
#14037=ORIENTED_EDGE ( 'NONE', *, *, #32838, .T. ) ;
#14042=VERTEX_POINT ( 'NONE', #11806 ) ;
#14045=FACE_OUTER_BOUND ( 'NONE', #14204, .T. ) ;
#14047=EDGE_CURVE ( 'NONE', #29687, #31732, #14139, .T. ) ;
#14057=FACE_OUTER_BOUND ( 'NONE', #16420, .T. ) ;
#14059=AXIS2_PLACEMENT_3D ( 'NONE', #2002, #12977, #34765 ) ;
#14076=CARTESIAN_POINT ( 'NONE',  ( 7.999999999999992895, 9.744342220504046637, -46.48873837489789196 ) ) ;
#14082=AXIS2_PLACEMENT_3D ( 'NONE', #6572, #20240, #3541 ) ;
#14087=AXIS2_PLACEMENT_3D ( 'NONE', #27326, #6237, #25688 ) ;
#14095=AXIS2_PLACEMENT_3D ( 'NONE', #26300, #18176, #23770 ) ;
#14100=LINE ( 'NONE', #11415, #8166 ) ;
#14102=ORIENTED_EDGE ( 'NONE', *, *, #11537, .T. ) ;
#14105=AXIS2_PLACEMENT_3D ( 'NONE', #27814, #19331, #25101 ) ;
#14106=DIRECTION ( 'NONE',  ( 0.000000000000000000, 0.000000000000000000, -1.000000000000000000 ) ) ;
#14112=EDGE_LOOP ( 'NONE', ( #30300, #24662, #693, #24806 ) ) ;
#14113=CYLINDRICAL_SURFACE ( 'NONE', #349, 52.00000000000000711 ) ;
#14116=DIRECTION ( 'NONE',  ( -1.000000000000000000, 0.000000000000000000, 0.000000000000000000 ) ) ;
#14120=EDGE_CURVE ( 'NONE', #6500, #5335, #19874, .T. ) ;
#14122=CIRCLE ( 'NONE', #34259, 20.00000000000000355 ) ;
#14123=ORIENTED_EDGE ( 'NONE', *, *, #10593, .T. ) ;
#14125=LINE ( 'NONE', #3000, #5142 ) ;
#14127=EDGE_CURVE ( 'NONE', #14555, #33603, #2095, .T. ) ;
#14130=CIRCLE ( 'NONE', #29674, 52.00000000000000711 ) ;
#14131=CARTESIAN_POINT ( 'NONE',  ( 7.999999999999992895, 15.49408907645171851, 44.90087086784599535 ) ) ;
#14133=DIRECTION ( 'NONE',  ( 0.000000000000000000, -0.9980267284282722251, 0.06279051952930256308 ) ) ;
#14134=CIRCLE ( 'NONE', #338, 20.00000000000000711 ) ;
#14139=CIRCLE ( 'NONE', #33127, 47.49900000000001654 ) ;
#14158=EDGE_CURVE ( 'NONE', #16904, #32383, #20610, .T. ) ;
#14159=CARTESIAN_POINT ( 'NONE',  ( 0.000000000000000000, -44.47301969247433817, -16.68249143361957820 ) ) ;
#14162=DIRECTION ( 'NONE',  ( 1.000000000000000000, 0.000000000000000000, 0.000000000000000000 ) ) ;
#14164=VERTEX_POINT ( 'NONE', #23146 ) ;
#14168=CARTESIAN_POINT ( 'NONE',  ( 0.000000000000000000, -12.30077720129132679, 50.52416135122078344 ) ) ;
#14187=DIRECTION ( 'NONE',  ( -1.000000000000000000, 0.000000000000000000, 0.000000000000000000 ) ) ;
#14191=VECTOR ( 'NONE', #34676, 1000.000000000000000 ) ;
#14192=CARTESIAN_POINT ( 'NONE',  ( 7.999999999999992895, 0.000000000000000000, 0.000000000000000000 ) ) ;
#14194=CARTESIAN_POINT ( 'NONE',  ( 0.000000000000000000, -22.43957647427129842, -41.27978878573651400 ) ) ;
#14196=VERTEX_POINT ( 'NONE', #26213 ) ;
#14199=ORIENTED_EDGE ( 'NONE', *, *, #6449, .F. ) ;
#14204=EDGE_LOOP ( 'NONE', ( #28826, #19513, #1891, #32864 ) ) ;
#14211=CARTESIAN_POINT ( 'NONE',  ( 4.000000000000003553, -51.93417535146740960, -2.615612846549736581 ) ) ;
#14214=DIRECTION ( 'NONE',  ( 0.000000000000000000, 0.000000000000000000, 1.000000000000000000 ) ) ;
#14226=CARTESIAN_POINT ( 'NONE',  ( 7.999999999999992895, 46.90537658765334328, -2.727856614653800804 ) ) ;
#14232=CARTESIAN_POINT ( 'NONE',  ( 7.999999999999992895, 35.11945359308165138, -38.34871548465979174 ) ) ;
#14237=CARTESIAN_POINT ( 'NONE',  ( 7.999999999999992895, -0.2227391519119825691, 46.98410307550729215 ) ) ;
#14243=ADVANCED_FACE ( 'NONE', ( #26398 ), #7302, .T. ) ;
#14245=DIRECTION ( 'NONE',  ( 0.000000000000000000, 0.9510565162951521989, 0.3090169943749515036 ) ) ;
#14247=VERTEX_POINT ( 'NONE', #31610 ) ;
#14249=CARTESIAN_POINT ( 'NONE',  ( 7.999999999999992895, -20.99948489194452250, 42.60488980472776177 ) ) ;
#14264=CIRCLE ( 'NONE', #16584, 52.00000000000000711 ) ;
#14277=CARTESIAN_POINT ( 'NONE',  ( -9.999999999999994671, 0.000000000000000000, 0.000000000000000000 ) ) ;
#14280=DIRECTION ( 'NONE',  ( -1.000000000000000000, -0.000000000000000000, -0.000000000000000000 ) ) ;
#14286=AXIS2_PLACEMENT_3D ( 'NONE', #23124, #31412, #4743 ) ;
#14292=DIRECTION ( 'NONE',  ( -1.000000000000000000, -0.000000000000000000, -0.000000000000000000 ) ) ;
#14293=DIRECTION ( 'NONE',  ( 0.000000000000000000, -0.2486898871648415832, -0.9685831611286344067 ) ) ;
#14310=CARTESIAN_POINT ( 'NONE',  ( 7.999999999999992895, -39.55064067543080597, 25.36340625197344778 ) ) ;
#14316=CARTESIAN_POINT ( 'NONE',  ( 0.000000000000000000, 40.47821179127763003, -32.64221760512714354 ) ) ;
#14320=CARTESIAN_POINT ( 'NONE',  ( 7.999999999999992895, 0.2227391519116599106, 46.98410307550729215 ) ) ;
#14326=CARTESIAN_POINT ( 'NONE',  ( 7.999999999999992895, -46.19362259308826424, -8.585149169758999221 ) ) ;
#14331=CARTESIAN_POINT ( 'NONE',  ( 7.999999999999992895, -22.82995208772716467, 41.06517797613655318 ) ) ;
#14332=CARTESIAN_POINT ( 'NONE',  ( 7.999999999999992895, 0.000000000000000000, 0.000000000000000000 ) ) ;
#14336=AXIS2_PLACEMENT_3D ( 'NONE', #15627, #16163, #18697 ) ;
#14338=CARTESIAN_POINT ( 'NONE',  ( 4.000000000000003553, -47.32430374665916872, -21.55018039121578255 ) ) ;
#14340=AXIS2_PLACEMENT_3D ( 'NONE', #12953, #10607, #5036 ) ;
#14348=ORIENTED_EDGE ( 'NONE', *, *, #6558, .T. ) ;
#14353=CYLINDRICAL_SURFACE ( 'NONE', #2373, 52.00000000000000711 ) ;
#14355=EDGE_CURVE ( 'NONE', #12939, #34112, #11358, .T. ) ;
#14374=EDGE_LOOP ( 'NONE', ( #3252, #6563, #1700, #16772 ) ) ;
#14379=EDGE_LOOP ( 'NONE', ( #16602, #31646, #15094, #5149 ) ) ;
#14383=DIRECTION ( 'NONE',  ( 0.000000000000000000, 0.000000000000000000, 1.000000000000000000 ) ) ;
#14387=ORIENTED_EDGE ( 'NONE', *, *, #1805, .F. ) ;
#14396=EDGE_CURVE ( 'NONE', #20157, #4114, #13031, .T. ) ;
#14401=CARTESIAN_POINT ( 'NONE',  ( 0.000000000000000000, 20.99948489194482448, -42.60488980472762677 ) ) ;
#14417=EDGE_CURVE ( 'NONE', #28739, #33531, #8412, .T. ) ;
#14419=EDGE_LOOP ( 'NONE', ( #941, #19939, #4720, #33046 ) ) ;
#14435=CARTESIAN_POINT ( 'NONE',  ( 7.999999999999992895, 0.000000000000000000, 0.000000000000000000 ) ) ;
#14439=DIRECTION ( 'NONE',  ( -1.000000000000000000, -0.000000000000000000, -0.000000000000000000 ) ) ;
#14440=AXIS2_PLACEMENT_3D ( 'NONE', #18190, #29201, #1829 ) ;
#14441=CIRCLE ( 'NONE', #28832, 20.00000000000000711 ) ;
#14444=CARTESIAN_POINT ( 'NONE',  ( 7.999999999999992895, -36.34385289850609979, 29.77717097092063980 ) ) ;
#14445=DIRECTION ( 'NONE',  ( 1.000000000000000000, 0.000000000000000000, 0.000000000000000000 ) ) ;
#14447=DIRECTION ( 'NONE',  ( -1.000000000000000000, -0.000000000000000000, -0.000000000000000000 ) ) ;
#14452=DIRECTION ( 'NONE',  ( -1.000000000000000000, 0.000000000000000000, 0.000000000000000000 ) ) ;
#14454=LINE ( 'NONE', #3505, #29356 ) ;
#14456=CARTESIAN_POINT ( 'NONE',  ( 4.000000000000003553, -44.25018368420762016, 27.31155879685168131 ) ) ;
#14465=CIRCLE ( 'NONE', #28289, 47.49900000000002365 ) ;
#14469=ORIENTED_EDGE ( 'NONE', *, *, #28860, .T. ) ;
#14476=DIRECTION ( 'NONE',  ( -1.000000000000000000, 0.000000000000000000, -0.000000000000000000 ) ) ;
#14481=CIRCLE ( 'NONE', #136, 47.49900000000000944 ) ;
#14489=FACE_OUTER_BOUND ( 'NONE', #8676, .T. ) ;
#14491=LINE ( 'NONE', #25503, #576 ) ;
#14496=ORIENTED_EDGE ( 'NONE', *, *, #18323, .F. ) ;
#14498=ORIENTED_EDGE ( 'NONE', *, *, #11007, .F. ) ;
#14501=VERTEX_POINT ( 'NONE', #29281 ) ;
#14503=ORIENTED_EDGE ( 'NONE', *, *, #33522, .T. ) ;
#14509=CARTESIAN_POINT ( 'NONE',  ( 7.999999999999992895, 11.90021268425617329, -45.45261810511203038 ) ) ;
#14514=EDGE_CURVE ( 'NONE', #22481, #8656, #30515, .T. ) ;
#14515=EDGE_CURVE ( 'NONE', #4091, #33531, #2715, .T. ) ;
#14517=DIRECTION ( 'NONE',  ( -1.000000000000000000, -0.000000000000000000, -0.000000000000000000 ) ) ;
#14531=CARTESIAN_POINT ( 'NONE',  ( 0.000000000000000000, -46.77034588191288833, -22.72740077717277885 ) ) ;
#14536=EDGE_LOOP ( 'NONE', ( #12760, #12096, #11815, #13178 ) ) ;
#14541=ORIENTED_EDGE ( 'NONE', *, *, #15624, .F. ) ;
#14547=AXIS2_PLACEMENT_3D ( 'NONE', #17397, #8943, #22279 ) ;
#14549=ORIENTED_EDGE ( 'NONE', *, *, #4071, .T. ) ;
#14555=VERTEX_POINT ( 'NONE', #27818 ) ;
#14556=ORIENTED_EDGE ( 'NONE', *, *, #32854, .F. ) ;
#14568=CARTESIAN_POINT ( 'NONE',  ( 7.999999999999992895, 22.82995208772746665, -41.06517797613640397 ) ) ;
#14579=VERTEX_POINT ( 'NONE', #16979 ) ;
#14581=ORIENTED_EDGE ( 'NONE', *, *, #34139, .T. ) ;
#14590=DIRECTION ( 'NONE',  ( -1.000000000000000000, 0.000000000000000000, -0.000000000000000000 ) ) ;
#14594=ADVANCED_FACE ( 'NONE', ( #3336 ), #19163, .T. ) ;
#14607=EDGE_CURVE ( 'NONE', #23898, #9389, #6693, .T. ) ;
#14610=EDGE_CURVE ( 'NONE', #19467, #7819, #25672, .T. ) ;
#14612=AXIS2_PLACEMENT_3D ( 'NONE', #29462, #23695, #18822 ) ;
#14616=CARTESIAN_POINT ( 'NONE',  ( 7.999999999999992895, 0.000000000000000000, 0.000000000000000000 ) ) ;
#14623=DIRECTION ( 'NONE',  ( 0.000000000000000000, 0.3681245526846785854, -0.9297764858882511252 ) ) ;
#14624=CYLINDRICAL_SURFACE ( 'NONE', #26018, 20.00000000000000711 ) ;
#14625=CYLINDRICAL_SURFACE ( 'NONE', #11095, 20.00000000000000711 ) ;
#14629=CARTESIAN_POINT ( 'NONE',  ( 0.000000000000000000, 0.000000000000000000, 0.000000000000000000 ) ) ;
#14634=ORIENTED_EDGE ( 'NONE', *, *, #14514, .F. ) ;
#14660=DIRECTION ( 'NONE',  ( -1.000000000000000000, 0.000000000000000000, -0.000000000000000000 ) ) ;
#14661=ORIENTED_EDGE ( 'NONE', *, *, #12787, .F. ) ;
#14663=CYLINDRICAL_SURFACE ( 'NONE', #27475, 20.00000000000000711 ) ;
#14665=CARTESIAN_POINT ( 'NONE',  ( 7.999999999999992895, 39.55064067543098361, -25.36340625197317067 ) ) ;
#14666=CIRCLE ( 'NONE', #25624, 20.00000000000000711 ) ;
#14667=CARTESIAN_POINT ( 'NONE',  ( 7.999999999999992895, 43.83938735307295076, -18.28286404005752175 ) ) ;
#14669=DIRECTION ( 'NONE',  ( 0.000000000000000000, 0.000000000000000000, 1.000000000000000000 ) ) ;
#14671=CARTESIAN_POINT ( 'NONE',  ( -9.999999999999994671, 0.000000000000000000, 0.000000000000000000 ) ) ;
#14674=DIRECTION ( 'NONE',  ( 0.000000000000000000, -0.5877852522924802425, 0.8090169943749421222 ) ) ;
#14682=EDGE_LOOP ( 'NONE', ( #10327, #20690, #35541, #35034 ) ) ;
#14691=CIRCLE ( 'NONE', #34851, 20.00000000000000711 ) ;
#14693=ORIENTED_EDGE ( 'NONE', *, *, #33010, .T. ) ;
#14708=DIRECTION ( 'NONE',  ( 1.000000000000000000, 0.000000000000000000, 0.000000000000000000 ) ) ;
#14713=FACE_OUTER_BOUND ( 'NONE', #24030, .T. ) ;
#14722=AXIS2_PLACEMENT_3D ( 'NONE', #6979, #6447, #28954 ) ;
#14726=AXIS2_PLACEMENT_3D ( 'NONE', #5848, #25108, #6197 ) ;
#14727=ADVANCED_FACE ( 'NONE', ( #1155 ), #978, .T. ) ;
#14732=EDGE_CURVE ( 'NONE', #29371, #29366, #21047, .T. ) ;
#14741=FACE_OUTER_BOUND ( 'NONE', #15742, .T. ) ;
#14743=VERTEX_POINT ( 'NONE', #34464 ) ;
#14744=ORIENTED_EDGE ( 'NONE', *, *, #29725, .T. ) ;
#14747=ORIENTED_EDGE ( 'NONE', *, *, #23894, .T. ) ;
#14753=CARTESIAN_POINT ( 'NONE',  ( 7.999999999999992895, -41.20225022064655462, 23.63323037071389621 ) ) ;
#14759=AXIS2_PLACEMENT_3D ( 'NONE', #15920, #30340, #8175 ) ;
#14762=DIRECTION ( 'NONE',  ( -1.000000000000000000, 0.000000000000000000, -0.000000000000000000 ) ) ;
#14764=EDGE_LOOP ( 'NONE', ( #21420, #15656, #10547, #15296 ) ) ;
#14769=CIRCLE ( 'NONE', #30317, 20.00000000000000711 ) ;
#14770=ORIENTED_EDGE ( 'NONE', *, *, #23019, .T. ) ;
#14776=DIRECTION ( 'NONE',  ( -1.000000000000000000, 0.000000000000000000, 0.000000000000000000 ) ) ;
#14780=ORIENTED_EDGE ( 'NONE', *, *, #31705, .T. ) ;
#14782=CIRCLE ( 'NONE', #21699, 47.49900000000001654 ) ;
#14787=EDGE_LOOP ( 'NONE', ( #33459, #13906, #27888, #18205 ) ) ;
#14789=DIRECTION ( 'NONE',  ( 0.000000000000000000, -0.5877852522924624790, -0.8090169943749551118 ) ) ;
#14792=DIRECTION ( 'NONE',  ( -1.000000000000000000, 0.000000000000000000, -0.000000000000000000 ) ) ;
#14793=ORIENTED_EDGE ( 'NONE', *, *, #10323, .T. ) ;
#14794=VERTEX_POINT ( 'NONE', #34274 ) ;
#14801=AXIS2_PLACEMENT_3D ( 'NONE', #15024, #32480, #5486 ) ;
#14807=VECTOR ( 'NONE', #19442, 1000.000000000000000 ) ;
#14811=VECTOR ( 'NONE', #22442, 1000.000000000000000 ) ;
#14817=CIRCLE ( 'NONE', #34974, 20.00000000000000355 ) ;
#14828=ORIENTED_EDGE ( 'NONE', *, *, #16909, .T. ) ;
#14833=ORIENTED_EDGE ( 'NONE', *, *, #11448, .T. ) ;
#14844=DIRECTION ( 'NONE',  ( -1.000000000000000000, 0.000000000000000000, 0.000000000000000000 ) ) ;
#14848=EDGE_CURVE ( 'NONE', #3935, #12448, #18946, .T. ) ;
#14849=CYLINDRICAL_SURFACE ( 'NONE', #8250, 20.00000000000000355 ) ;
#14857=CYLINDRICAL_SURFACE ( 'NONE', #31427, 47.49900000000001654 ) ;
#14863=DIRECTION ( 'NONE',  ( -1.000000000000000000, 0.000000000000000000, 0.000000000000000000 ) ) ;
#14866=ORIENTED_EDGE ( 'NONE', *, *, #26258, .F. ) ;
#14878=ORIENTED_EDGE ( 'NONE', *, *, #19363, .T. ) ;
#14887=ADVANCED_FACE ( 'NONE', ( #7604 ), #7437, .T. ) ;
#14893=DIRECTION ( 'NONE',  ( -1.000000000000000000, -0.000000000000000000, -0.000000000000000000 ) ) ;
#14903=ORIENTED_EDGE ( 'NONE', *, *, #6598, .F. ) ;
#14904=AXIS2_PLACEMENT_3D ( 'NONE', #14435, #9225, #22717 ) ;
#14905=EDGE_LOOP ( 'NONE', ( #8339, #3148, #9583, #31789 ) ) ;
#14907=DIRECTION ( 'NONE',  ( 0.000000000000000000, 0.000000000000000000, 1.000000000000000000 ) ) ;
#14908=ORIENTED_EDGE ( 'NONE', *, *, #29189, .F. ) ;
#14909=ORIENTED_EDGE ( 'NONE', *, *, #30443, .T. ) ;
#14911=AXIS2_PLACEMENT_3D ( 'NONE', #12412, #7182, #9354 ) ;
#14912=DIRECTION ( 'NONE',  ( -1.000000000000000000, 0.000000000000000000, 0.000000000000000000 ) ) ;
#14915=CARTESIAN_POINT ( 'NONE',  ( 7.999999999999992895, -30.03615769709763583, 42.44795908868979950 ) ) ;
#14927=DIRECTION ( 'NONE',  ( 0.000000000000000000, -0.6845471059286950544, 0.7289686274214053352 ) ) ;
#14940=EDGE_CURVE ( 'NONE', #33784, #28703, #23983, .T. ) ;
#14968=ORIENTED_EDGE ( 'NONE', *, *, #19604, .T. ) ;
#14973=CARTESIAN_POINT ( 'NONE',  ( 7.999999999999992895, 0.000000000000000000, 0.000000000000000000 ) ) ;
#14985=CIRCLE ( 'NONE', #9240, 20.00000000000000711 ) ;
#14995=VERTEX_POINT ( 'NONE', #24719 ) ;
#15007=EDGE_CURVE ( 'NONE', #24147, #4250, #13904, .T. ) ;
#15017=CYLINDRICAL_SURFACE ( 'NONE', #4542, 47.49900000000001654 ) ;
#15020=DIRECTION ( 'NONE',  ( 1.000000000000000000, 0.000000000000000000, 0.000000000000000000 ) ) ;
#15021=LINE ( 'NONE', #31066, #7126 ) ;
#15024=CARTESIAN_POINT ( 'NONE',  ( 7.999999999999992895, 11.46872990052444408, -45.56340405422432127 ) ) ;
#15029=CYLINDRICAL_SURFACE ( 'NONE', #27898, 20.00000000000000355 ) ;
#15030=LINE ( 'NONE', #28737, #390 ) ;
#15031=CARTESIAN_POINT ( 'NONE',  ( 0.000000000000000000, 10.58300524425836109, 3.000000000000002665 ) ) ;
#15033=CIRCLE ( 'NONE', #28854, 47.49900000000001654 ) ;
#15040=DIRECTION ( 'NONE',  ( 1.000000000000000000, 0.000000000000000000, -0.000000000000000000 ) ) ;
#15044=EDGE_CURVE ( 'NONE', #31746, #28247, #28574, .T. ) ;
#15045=LINE ( 'NONE', #23334, #15408 ) ;
#15046=EDGE_CURVE ( 'NONE', #29853, #22200, #30120, .T. ) ;
#15047=DIRECTION ( 'NONE',  ( 0.000000000000000000, -0.9822872507286903865, 0.1873813145857150808 ) ) ;
#15050=EDGE_LOOP ( 'NONE', ( #3472, #3551, #21390, #16753 ) ) ;
#15055=CIRCLE ( 'NONE', #23112, 20.00000000000000355 ) ;
#15062=DIRECTION ( 'NONE',  ( 0.000000000000000000, 0.000000000000000000, -1.000000000000000000 ) ) ;
#15064=DIRECTION ( 'NONE',  ( 0.000000000000000000, 0.8443279255020125218, 0.5358267949790005424 ) ) ;
#15068=CARTESIAN_POINT ( 'NONE',  ( 0.000000000000000000, 32.32520163883582853, 34.09746168776048592 ) ) ;
#15069=ORIENTED_EDGE ( 'NONE', *, *, #13484, .T. ) ;
#15073=ORIENTED_EDGE ( 'NONE', *, *, #24883, .T. ) ;
#15075=CARTESIAN_POINT ( 'NONE',  ( 0.000000000000000000, -47.00885577955417460, 6.806061952192132836 ) ) ;
#15076=AXIS2_PLACEMENT_3D ( 'NONE', #8290, #8818, #30793 ) ;
#15078=VERTEX_POINT ( 'NONE', #3116 ) ;
#15079=VERTEX_POINT ( 'NONE', #388 ) ;
#15086=DIRECTION ( 'NONE',  ( -1.000000000000000000, 0.000000000000000000, 0.000000000000000000 ) ) ;
#15092=EDGE_CURVE ( 'NONE', #16713, #11969, #5019, .T. ) ;
#15093=DIRECTION ( 'NONE',  ( -1.000000000000000000, 0.000000000000000000, 0.000000000000000000 ) ) ;
#15094=ORIENTED_EDGE ( 'NONE', *, *, #7549, .T. ) ;
#15096=AXIS2_PLACEMENT_3D ( 'NONE', #14277, #16799, #11235 ) ;
#15098=CIRCLE ( 'NONE', #29505, 20.00000000000000711 ) ;
#15099=CARTESIAN_POINT ( 'NONE',  ( 7.999999999999992895, 0.000000000000000000, 0.000000000000000000 ) ) ;
#15102=AXIS2_PLACEMENT_3D ( 'NONE', #6729, #3688, #17705 ) ;
#15107=VERTEX_POINT ( 'NONE', #14249 ) ;
#15110=ORIENTED_EDGE ( 'NONE', *, *, #26516, .F. ) ;
#15112=ORIENTED_EDGE ( 'NONE', *, *, #2697, .T. ) ;
#15130=CARTESIAN_POINT ( 'NONE',  ( 7.999999999999992895, 0.000000000000000000, 0.000000000000000000 ) ) ;
#15134=EDGE_LOOP ( 'NONE', ( #14102, #4023, #34499, #3199 ) ) ;
#15142=DIRECTION ( 'NONE',  ( -1.000000000000000000, -0.000000000000000000, 0.000000000000000000 ) ) ;
#15149=CARTESIAN_POINT ( 'NONE',  ( 7.999999999999992895, 46.11014828289842882, -9.022736828080857308 ) ) ;
#15150=CYLINDRICAL_SURFACE ( 'NONE', #7185, 20.00000000000000355 ) ;
#15154=DIRECTION ( 'NONE',  ( -1.000000000000000000, 0.000000000000000000, 0.000000000000000000 ) ) ;
#15159=DIRECTION ( 'NONE',  ( 1.000000000000000000, 0.000000000000000000, 0.000000000000000000 ) ) ;
#15171=EDGE_CURVE ( 'NONE', #9761, #17170, #5986, .T. ) ;
#15181=PLANE ( 'NONE',  #25445 ) ;
#15187=ORIENTED_EDGE ( 'NONE', *, *, #9512, .F. ) ;
#15192=ADVANCED_FACE ( 'NONE', ( #12275 ), #15309, .T. ) ;
#15194=CARTESIAN_POINT ( 'NONE',  ( 4.000000000000003553, -7.162210897276083621, 51.50439529848826936 ) ) ;
#15200=ORIENTED_EDGE ( 'NONE', *, *, #10525, .F. ) ;
#15203=CYLINDRICAL_SURFACE ( 'NONE', #7202, 20.00000000000000355 ) ;
#15205=AXIS2_PLACEMENT_3D ( 'NONE', #11115, #13636, #19379 ) ;
#15206=EDGE_LOOP ( 'NONE', ( #8422, #22121, #25784, #12902 ) ) ;
#15213=EDGE_CURVE ( 'NONE', #10641, #21218, #392, .T. ) ;
#15216=ORIENTED_EDGE ( 'NONE', *, *, #29832, .T. ) ;
#15226=CYLINDRICAL_SURFACE ( 'NONE', #2861, 20.00000000000000355 ) ;
#15227=EDGE_LOOP ( 'NONE', ( #353, #3689, #15247, #24843 ) ) ;
#15229=CIRCLE ( 'NONE', #35368, 20.00000000000000355 ) ;
#15230=CARTESIAN_POINT ( 'NONE',  ( 7.999999999999992895, -42.60732521687556584, -19.80331771201704427 ) ) ;
#15235=LINE ( 'NONE', #9681, #30676 ) ;
#15244=EDGE_CURVE ( 'NONE', #27298, #4328, #5042, .T. ) ;
#15247=ORIENTED_EDGE ( 'NONE', *, *, #12370, .T. ) ;
#15254=CARTESIAN_POINT ( 'NONE',  ( 0.000000000000000000, 24.72041153920790180, -40.55929306992661765 ) ) ;
#15255=CIRCLE ( 'NONE', #21579, 52.00000000000000711 ) ;
#15256=DIRECTION ( 'NONE',  ( -1.000000000000000000, 0.000000000000000000, 0.000000000000000000 ) ) ;
#15269=ORIENTED_EDGE ( 'NONE', *, *, #7218, .T. ) ;
#15276=CIRCLE ( 'NONE', #12418, 20.00000000000000711 ) ;
#15277=DIRECTION ( 'NONE',  ( -1.000000000000000000, 0.000000000000000000, 0.000000000000000000 ) ) ;
#15282=VECTOR ( 'NONE', #28336, 1000.000000000000000 ) ;
#15284=DIRECTION ( 'NONE',  ( -1.000000000000000000, -0.000000000000000000, 0.000000000000000000 ) ) ;
#15288=CYLINDRICAL_SURFACE ( 'NONE', #29002, 20.00000000000000355 ) ;
#15292=ORIENTED_EDGE ( 'NONE', *, *, #26992, .T. ) ;
#15296=ORIENTED_EDGE ( 'NONE', *, *, #35040, .T. ) ;
#15300=LINE ( 'NONE', #18006, #8126 ) ;
#15309=CYLINDRICAL_SURFACE ( 'NONE', #26868, 20.00000000000000355 ) ;
#15318=CARTESIAN_POINT ( 'NONE',  ( 0.000000000000000000, 41.20225022064637699, 23.63323037071417332 ) ) ;
#15322=CARTESIAN_POINT ( 'NONE',  ( 7.999999999999992895, -50.95304419620833158, 10.38206564895643957 ) ) ;
#15327=AXIS2_PLACEMENT_3D ( 'NONE', #11662, #4125, #9502 ) ;
#15332=ORIENTED_EDGE ( 'NONE', *, *, #24109, .F. ) ;
#15333=LINE ( 'NONE', #12839, #27497 ) ;
#15334=CARTESIAN_POINT ( 'NONE',  ( 0.000000000000000000, 46.21320724403665281, -10.97699764141904488 ) ) ;
#15336=AXIS2_PLACEMENT_3D ( 'NONE', #18088, #4967, #1913 ) ;
#15340=DIRECTION ( 'NONE',  ( -1.000000000000000000, -0.000000000000000000, -0.000000000000000000 ) ) ;
#15345=CARTESIAN_POINT ( 'NONE',  ( 7.999999999999992895, -27.43636312076347394, 38.14186064215141414 ) ) ;
#15346=ORIENTED_EDGE ( 'NONE', *, *, #17609, .F. ) ;
#15353=AXIS2_PLACEMENT_3D ( 'NONE', #23859, #10173, #7636 ) ;
#15355=ORIENTED_EDGE ( 'NONE', *, *, #11299, .T. ) ;
#15360=CARTESIAN_POINT ( 'NONE',  ( 0.000000000000000000, -38.92705108641712286, -27.21837053747841395 ) ) ;
#15367=EDGE_CURVE ( 'NONE', #2175, #1839, #33792, .T. ) ;
#15370=ORIENTED_EDGE ( 'NONE', *, *, #35407, .F. ) ;
#15377=DIRECTION ( 'NONE',  ( 0.000000000000000000, 0.000000000000000000, -1.000000000000000000 ) ) ;
#15383=EDGE_CURVE ( 'NONE', #32804, #31713, #3321, .T. ) ;
#15386=CIRCLE ( 'NONE', #19979, 47.49900000000001654 ) ;
#15389=EDGE_LOOP ( 'NONE', ( #23654, #19487, #17666, #26817 ) ) ;
#15393=CARTESIAN_POINT ( 'NONE',  ( 7.999999999999992895, 5.667686777402359155, -46.64153600743598105 ) ) ;
#15398=CARTESIAN_POINT ( 'NONE',  ( 0.000000000000000000, -47.32430374665916872, -21.55018039121578255 ) ) ;
#15400=CARTESIAN_POINT ( 'NONE',  ( 7.999999999999992895, 49.65209126885763879, 15.44894276735568539 ) ) ;
#15401=CARTESIAN_POINT ( 'NONE',  ( 7.999999999999992895, 0.000000000000000000, 0.000000000000000000 ) ) ;
#15403=DIRECTION ( 'NONE',  ( 1.000000000000000000, 0.000000000000000000, 0.000000000000000000 ) ) ;
#15408=VECTOR ( 'NONE', #29110, 1000.000000000000000 ) ;
#15411=AXIS2_PLACEMENT_3D ( 'NONE', #27307, #22068, #30182 ) ;
#15412=DIRECTION ( 'NONE',  ( 0.000000000000000000, 0.000000000000000000, 1.000000000000000000 ) ) ;
#15416=ADVANCED_FACE ( 'NONE', ( #10470 ), #23977, .T. ) ;
#15417=EDGE_CURVE ( 'NONE', #16883, #688, #15939, .T. ) ;
#15422=CARTESIAN_POINT ( 'NONE',  ( 7.999999999999992895, 0.000000000000000000, 0.000000000000000000 ) ) ;
#15424=DIRECTION ( 'NONE',  ( -1.000000000000000000, 0.000000000000000000, 0.000000000000000000 ) ) ;
#15431=EDGE_CURVE ( 'NONE', #7438, #32535, #24602, .T. ) ;
#15433=ORIENTED_EDGE ( 'NONE', *, *, #8269, .T. ) ;
#15435=DIRECTION ( 'NONE',  ( -1.000000000000000000, -0.000000000000000000, 0.000000000000000000 ) ) ;
#15436=ORIENTED_EDGE ( 'NONE', *, *, #21195, .F. ) ;
#15439=ORIENTED_EDGE ( 'NONE', *, *, #34749, .T. ) ;
#15442=CARTESIAN_POINT ( 'NONE',  ( 0.000000000000000000, 47.22458491092828581, -5.098390039073752433 ) ) ;
#15449=EDGE_CURVE ( 'NONE', #33861, #423, #33199, .T. ) ;
#15458=CIRCLE ( 'NONE', #21227, 11.00000000000000000 ) ;
#15460=CARTESIAN_POINT ( 'NONE',  ( 4.000000000000003553, 44.25018368420781911, -27.31155879685134735 ) ) ;
#15466=AXIS2_PLACEMENT_3D ( 'NONE', #20896, #15142, #20554 ) ;
#15471=ORIENTED_EDGE ( 'NONE', *, *, #6213, .F. ) ;
#15474=AXIS2_PLACEMENT_3D ( 'NONE', #4152, #32037, #17447 ) ;
#15475=CARTESIAN_POINT ( 'NONE',  ( 0.000000000000000000, -13.56094713063537327, -50.20060470671755581 ) ) ;
#15487=ORIENTED_EDGE ( 'NONE', *, *, #18141, .T. ) ;
#15493=VERTEX_POINT ( 'NONE', #181 ) ;
#15497=FACE_OUTER_BOUND ( 'NONE', #20674, .T. ) ;
#15499=ORIENTED_EDGE ( 'NONE', *, *, #9054, .F. ) ;
#15501=AXIS2_PLACEMENT_3D ( 'NONE', #24410, #4976, #29639 ) ;
#15502=FACE_OUTER_BOUND ( 'NONE', #987, .T. ) ;
#15510=CIRCLE ( 'NONE', #6325, 20.00000000000000000 ) ;
#15512=CARTESIAN_POINT ( 'NONE',  ( 0.000000000000000000, 0.000000000000000000, 0.000000000000000000 ) ) ;
#15516=DIRECTION ( 'NONE',  ( -1.000000000000000000, 0.000000000000000000, 0.000000000000000000 ) ) ;
#15524=CARTESIAN_POINT ( 'NONE',  ( 0.000000000000000000, 51.93417535146742381, 2.615612846549361770 ) ) ;
#15526=LINE ( 'NONE', #1880, #28957 ) ;
#15527=ORIENTED_EDGE ( 'NONE', *, *, #32670, .F. ) ;
#15532=ORIENTED_EDGE ( 'NONE', *, *, #10478, .F. ) ;
#15541=EDGE_CURVE ( 'NONE', #1868, #19467, #30442, .T. ) ;
#15546=CYLINDRICAL_SURFACE ( 'NONE', #11718, 20.00000000000000355 ) ;
#15556=CYLINDRICAL_SURFACE ( 'NONE', #15336, 20.00000000000000355 ) ;
#15566=ORIENTED_EDGE ( 'NONE', *, *, #10478, .T. ) ;
#15571=VERTEX_POINT ( 'NONE', #8102 ) ;
#15574=EDGE_CURVE ( 'NONE', #22574, #13336, #10792, .T. ) ;
#15575=ADVANCED_FACE ( 'NONE', ( #5601 ), #28092, .T. ) ;
#15579=DIRECTION ( 'NONE',  ( 0.000000000000000000, 0.000000000000000000, 1.000000000000000000 ) ) ;
#15594=CARTESIAN_POINT ( 'NONE',  ( -9.999999999999994671, 0.000000000000000000, 0.000000000000000000 ) ) ;
#15605=LINE ( 'NONE', #34374, #24044 ) ;
#15607=VERTEX_POINT ( 'NONE', #27572 ) ;
#15611=CARTESIAN_POINT ( 'NONE',  ( 7.999999999999992895, 10.58300524425836109, -3.000000000000002665 ) ) ;
#15614=ADVANCED_FACE ( 'NONE', ( #3435 ), #19086, .T. ) ;
#15619=ORIENTED_EDGE ( 'NONE', *, *, #13022, .F. ) ;
#15620=ORIENTED_EDGE ( 'NONE', *, *, #29873, .T. ) ;
#15624=EDGE_CURVE ( 'NONE', #24598, #2557, #17662, .T. ) ;
#15625=DIRECTION ( 'NONE',  ( -1.000000000000000000, -0.000000000000000000, -0.000000000000000000 ) ) ;
#15627=CARTESIAN_POINT ( 'NONE',  ( 7.999999999999992895, 36.05989434073656241, -30.12041790338579261 ) ) ;
#15634=DIRECTION ( 'NONE',  ( 0.000000000000000000, -0.5877852522924803536, 0.8090169943749422332 ) ) ;
#15641=DIRECTION ( 'NONE',  ( -1.000000000000000000, -0.000000000000000000, -0.000000000000000000 ) ) ;
#15643=AXIS2_PLACEMENT_3D ( 'NONE', #23995, #27406, #16205 ) ;
#15650=EDGE_CURVE ( 'NONE', #4059, #966, #32960, .T. ) ;
#15653=EDGE_CURVE ( 'NONE', #31530, #10826, #2180, .T. ) ;
#15655=ADVANCED_FACE ( 'NONE', ( #16373 ), #10995, .T. ) ;
#15656=ORIENTED_EDGE ( 'NONE', *, *, #10617, .F. ) ;
#15659=AXIS2_PLACEMENT_3D ( 'NONE', #11787, #19532, #13970 ) ;
#15669=VERTEX_POINT ( 'NONE', #7175 ) ;
#15673=AXIS2_PLACEMENT_3D ( 'NONE', #29355, #24305, #5228 ) ;
#15674=CARTESIAN_POINT ( 'NONE',  ( 7.999999999999992895, -42.03146605346771025, -22.12489237027362421 ) ) ;
#15675=EDGE_LOOP ( 'NONE', ( #5502, #3284, #11710, #321 ) ) ;
#15676=ORIENTED_EDGE ( 'NONE', *, *, #25683, .T. ) ;
#15680=LINE ( 'NONE', #17721, #30398 ) ;
#15688=ORIENTED_EDGE ( 'NONE', *, *, #3341, .T. ) ;
#15694=DIRECTION ( 'NONE',  ( 0.000000000000000000, 0.000000000000000000, -1.000000000000000000 ) ) ;
#15697=AXIS2_PLACEMENT_3D ( 'NONE', #8383, #286, #33242 ) ;
#15701=CARTESIAN_POINT ( 'NONE',  ( 7.999999999999992895, -26.17370628620627215, -39.63700417846191471 ) ) ;
#15707=VERTEX_POINT ( 'NONE', #29160 ) ;
#15709=ADVANCED_FACE ( 'NONE', ( #32206 ), #18338, .T. ) ;
#15717=DIRECTION ( 'NONE',  ( 0.000000000000000000, 0.8443279255020161855, -0.5358267949789946583 ) ) ;
#15718=CARTESIAN_POINT ( 'NONE',  ( 0.000000000000000000, 27.43636312076321104, 38.14186064215159888 ) ) ;
#15728=ORIENTED_EDGE ( 'NONE', *, *, #11627, .F. ) ;
#15735=CYLINDRICAL_SURFACE ( 'NONE', #30790, 47.49900000000001654 ) ;
#15737=DIRECTION ( 'NONE',  ( -1.000000000000000000, 0.000000000000000000, 0.000000000000000000 ) ) ;
#15742=EDGE_LOOP ( 'NONE', ( #1928, #8408, #2682, #17796 ) ) ;
#15748=CYLINDRICAL_SURFACE ( 'NONE', #14612, 52.00000000000000711 ) ;
#15756=VERTEX_POINT ( 'NONE', #15442 ) ;
#15757=ORIENTED_EDGE ( 'NONE', *, *, #20259, .T. ) ;
#15760=ORIENTED_EDGE ( 'NONE', *, *, #11126, .T. ) ;
#15762=DIRECTION ( 'NONE',  ( -1.000000000000000000, -0.000000000000000000, 0.000000000000000000 ) ) ;
#15763=DIRECTION ( 'NONE',  ( 0.000000000000000000, 0.000000000000000000, 1.000000000000000000 ) ) ;
#15764=CIRCLE ( 'NONE', #20356, 20.00000000000000355 ) ;
#15765=CIRCLE ( 'NONE', #23868, 20.00000000000000711 ) ;
#15772=DIRECTION ( 'NONE',  ( -1.000000000000000000, -0.000000000000000000, -0.000000000000000000 ) ) ;
#15773=DIRECTION ( 'NONE',  ( 0.000000000000000000, 0.8443279255020164076, -0.5358267949789945472 ) ) ;
#15774=EDGE_CURVE ( 'NONE', #540, #20427, #29336, .T. ) ;
#15780=DIRECTION ( 'NONE',  ( 0.000000000000000000, 0.000000000000000000, 1.000000000000000000 ) ) ;
#15784=FACE_OUTER_BOUND ( 'NONE', #2386, .T. ) ;
#15785=ORIENTED_EDGE ( 'NONE', *, *, #12015, .T. ) ;
#15787=ORIENTED_EDGE ( 'NONE', *, *, #29757, .T. ) ;
#15790=DIRECTION ( 'NONE',  ( -1.000000000000000000, 0.000000000000000000, 0.000000000000000000 ) ) ;
#15796=VERTEX_POINT ( 'NONE', #26811 ) ;
#15799=CIRCLE ( 'NONE', #881, 11.00000000000000000 ) ;
#15801=CARTESIAN_POINT ( 'NONE',  ( 0.000000000000000000, 5.667686777402359155, -46.64153600743598105 ) ) ;
#15817=EDGE_CURVE ( 'NONE', #21198, #28224, #20562, .T. ) ;
#15819=EDGE_LOOP ( 'NONE', ( #24240, #7937, #11482, #29526 ) ) ;
#15826=CIRCLE ( 'NONE', #3211, 20.00000000000000355 ) ;
#15827=ORIENTED_EDGE ( 'NONE', *, *, #6641, .T. ) ;
#15829=DIRECTION ( 'NONE',  ( -1.000000000000000000, 0.000000000000000000, 0.000000000000000000 ) ) ;
#15831=ORIENTED_EDGE ( 'NONE', *, *, #19560, .F. ) ;
#15833=ADVANCED_FACE ( 'NONE', ( #8756 ), #2688, .T. ) ;
#15834=CIRCLE ( 'NONE', #323, 52.00000000000000711 ) ;
#15840=CARTESIAN_POINT ( 'NONE',  ( 7.999999999999992895, 46.19362259308833529, 8.585149169758651055 ) ) ;
#15847=CARTESIAN_POINT ( 'NONE',  ( 7.999999999999992895, -30.93515269692138503, 36.04401931830242489 ) ) ;
#15851=EDGE_CURVE ( 'NONE', #8283, #11310, #13697, .T. ) ;
#15852=AXIS2_PLACEMENT_3D ( 'NONE', #5923, #3234, #12386 ) ;
#15853=AXIS2_PLACEMENT_3D ( 'NONE', #6580, #23692, #28561 ) ;
#15857=LINE ( 'NONE', #27228, #18540 ) ;
#15859=CIRCLE ( 'NONE', #22187, 52.00000000000000711 ) ;
#15861=AXIS2_PLACEMENT_3D ( 'NONE', #33627, #23001, #4127 ) ;
#15872=DIRECTION ( 'NONE',  ( 0.000000000000000000, 0.9510565162951545304, -0.3090169943749447867 ) ) ;
#15885=ORIENTED_EDGE ( 'NONE', *, *, #14417, .F. ) ;
#15887=CIRCLE ( 'NONE', #25104, 20.00000000000000355 ) ;
#15891=CARTESIAN_POINT ( 'NONE',  ( 7.999999999999992895, -46.87740477351715640, 16.82754413119429415 ) ) ;
#15892=ORIENTED_EDGE ( 'NONE', *, *, #19777, .F. ) ;
#15895=DIRECTION ( 'NONE',  ( -1.000000000000000000, -0.000000000000000000, -0.000000000000000000 ) ) ;
#15896=EDGE_CURVE ( 'NONE', #27135, #5839, #24457, .T. ) ;
#15898=AXIS2_PLACEMENT_3D ( 'NONE', #22632, #25370, #6091 ) ;
#15899=VECTOR ( 'NONE', #30809, 1000.000000000000000 ) ;
#15902=CARTESIAN_POINT ( 'NONE',  ( 0.000000000000000000, 0.000000000000000000, 0.000000000000000000 ) ) ;
#15903=DIRECTION ( 'NONE',  ( -1.000000000000000000, 0.000000000000000000, -0.000000000000000000 ) ) ;
#15906=CIRCLE ( 'NONE', #17059, 52.00000000000000711 ) ;
#15907=DIRECTION ( 'NONE',  ( 0.000000000000000000, 0.000000000000000000, 1.000000000000000000 ) ) ;
#15920=CARTESIAN_POINT ( 'NONE',  ( 7.999999999999992895, 0.000000000000000000, 0.000000000000000000 ) ) ;
#15923=DIRECTION ( 'NONE',  ( 1.000000000000000000, 0.000000000000000000, 0.000000000000000000 ) ) ;
#15924=CARTESIAN_POINT ( 'NONE',  ( 7.999999999999992895, 44.61570720899095477, -14.73072383765580717 ) ) ;
#15927=AXIS2_PLACEMENT_3D ( 'NONE', #24265, #2843, #5188 ) ;
#15928=VERTEX_POINT ( 'NONE', #32733 ) ;
#15929=CARTESIAN_POINT ( 'NONE',  ( 50.00005079999998969, 0.000000000000000000, 0.000000000000000000 ) ) ;
#15933=ORIENTED_EDGE ( 'NONE', *, *, #19377, .F. ) ;
#15938=ORIENTED_EDGE ( 'NONE', *, *, #26013, .T. ) ;
#15939=CIRCLE ( 'NONE', #3884, 52.00000000000000711 ) ;
#15948=DIRECTION ( 'NONE',  ( 0.000000000000000000, 0.9510565162951521989, 0.3090169943749515036 ) ) ;
#15960=AXIS2_PLACEMENT_3D ( 'NONE', #6592, #1384, #22977 ) ;
#15969=DIRECTION ( 'NONE',  ( -1.000000000000000000, 0.000000000000000000, 0.000000000000000000 ) ) ;
#15970=VERTEX_POINT ( 'NONE', #494 ) ;
#15973=CARTESIAN_POINT ( 'NONE',  ( 7.999999999999992895, -46.87740477351715640, -3.172455868805712509 ) ) ;
#15975=ORIENTED_EDGE ( 'NONE', *, *, #32911, .T. ) ;
#15976=CARTESIAN_POINT ( 'NONE',  ( 0.000000000000000000, -41.20225022064621356, -23.63323037071446464 ) ) ;
#15980=DIRECTION ( 'NONE',  ( -1.000000000000000000, 0.000000000000000000, 0.000000000000000000 ) ) ;
#15982=ORIENTED_EDGE ( 'NONE', *, *, #23790, .T. ) ;
#15986=DIRECTION ( 'NONE',  ( 0.000000000000000000, 0.000000000000000000, 1.000000000000000000 ) ) ;
#16002=DIRECTION ( 'NONE',  ( -1.000000000000000000, 0.000000000000000000, -0.000000000000000000 ) ) ;
#16005=ORIENTED_EDGE ( 'NONE', *, *, #4307, .F. ) ;
#16007=CARTESIAN_POINT ( 'NONE',  ( 7.999999999999992895, -5.667686777401384823, -46.64153600743608763 ) ) ;
#16010=VERTEX_POINT ( 'NONE', #28576 ) ;
#16011=CARTESIAN_POINT ( 'NONE',  ( 7.999999999999992895, 0.000000000000000000, 3.000000000000002665 ) ) ;
#16015=DIRECTION ( 'NONE',  ( -1.000000000000000000, 0.000000000000000000, -0.000000000000000000 ) ) ;
#16016=DIRECTION ( 'NONE',  ( -1.000000000000000000, -0.000000000000000000, 0.000000000000000000 ) ) ;
#16025=EDGE_CURVE ( 'NONE', #5335, #35590, #31505, .T. ) ;
#16026=EDGE_CURVE ( 'NONE', #8613, #933, #454, .T. ) ;
#16028=CARTESIAN_POINT ( 'NONE',  ( -9.999999999999994671, 0.000000000000000000, 0.000000000000000000 ) ) ;
#16035=ADVANCED_FACE ( 'NONE', ( #23336 ), #25521, .T. ) ;
#16039=FACE_OUTER_BOUND ( 'NONE', #404, .T. ) ;
#16040=EDGE_LOOP ( 'NONE', ( #6814, #9382, #1731, #24544 ) ) ;
#16044=EDGE_LOOP ( 'NONE', ( #2379, #23076, #4314, #12214 ) ) ;
#16045=CARTESIAN_POINT ( 'NONE',  ( 7.999999999999992895, 0.000000000000000000, 0.000000000000000000 ) ) ;
#16049=AXIS2_PLACEMENT_3D ( 'NONE', #27306, #18478, #26965 ) ;
#16057=ORIENTED_EDGE ( 'NONE', *, *, #9242, .F. ) ;
#16061=DIRECTION ( 'NONE',  ( -1.000000000000000000, 0.000000000000000000, 0.000000000000000000 ) ) ;
#16062=VERTEX_POINT ( 'NONE', #20085 ) ;
#16065=DIRECTION ( 'NONE',  ( -1.000000000000000000, 0.000000000000000000, -0.000000000000000000 ) ) ;
#16067=EDGE_CURVE ( 'NONE', #33383, #2175, #11818, .T. ) ;
#16068=EDGE_CURVE ( 'NONE', #35590, #19983, #34337, .T. ) ;
#16073=CARTESIAN_POINT ( 'NONE',  ( 7.999999999999992895, 26.17370628620710349, -39.63700417846138890 ) ) ;
#16077=CARTESIAN_POINT ( 'NONE',  ( 4.000000000000003553, 13.56094713063641777, -50.20060470671727870 ) ) ;
#16078=VECTOR ( 'NONE', #24783, 1000.000000000000000 ) ;
#16080=VERTEX_POINT ( 'NONE', #12360 ) ;
#16081=AXIS2_PLACEMENT_3D ( 'NONE', #28203, #6761, #3543 ) ;
#16091=CARTESIAN_POINT ( 'NONE',  ( -9.999999999999994671, 0.000000000000000000, 0.000000000000000000 ) ) ;
#16095=EDGE_CURVE ( 'NONE', #13700, #2418, #8516, .T. ) ;
#16107=EDGE_CURVE ( 'NONE', #2044, #2939, #11047, .T. ) ;
#16115=DIRECTION ( 'NONE',  ( 0.000000000000000000, 0.000000000000000000, 1.000000000000000000 ) ) ;
#16119=CARTESIAN_POINT ( 'NONE',  ( 7.999999999999992895, 29.60891106212789126, 37.14118181634776050 ) ) ;
#16120=DIRECTION ( 'NONE',  ( 0.000000000000000000, 0.1253332335642974860, 0.9921147013144787641 ) ) ;
#16121=EDGE_CURVE ( 'NONE', #4059, #5839, #14264, .T. ) ;
#16129=DIRECTION ( 'NONE',  ( -1.000000000000000000, 0.000000000000000000, 0.000000000000000000 ) ) ;
#16133=CIRCLE ( 'NONE', #9236, 20.00000000000000355 ) ;
#16134=AXIS2_PLACEMENT_3D ( 'NONE', #31796, #31447, #28749 ) ;
#16136=CIRCLE ( 'NONE', #7519, 20.00000000000000711 ) ;
#16137=CARTESIAN_POINT ( 'NONE',  ( 7.999999999999992895, 22.43957647427220081, -41.27978878573601662 ) ) ;
#16145=CARTESIAN_POINT ( 'NONE',  ( 7.999999999999992895, -19.44205635905512608, -43.33776004284631256 ) ) ;
#16146=DIRECTION ( 'NONE',  ( -1.000000000000000000, 0.000000000000000000, 0.000000000000000000 ) ) ;
#16151=EDGE_CURVE ( 'NONE', #19983, #7838, #34992, .T. ) ;
#16155=ORIENTED_EDGE ( 'NONE', *, *, #27271, .F. ) ;
#16158=DIRECTION ( 'NONE',  ( 0.000000000000000000, 0.000000000000000000, 1.000000000000000000 ) ) ;
#16162=AXIS2_PLACEMENT_3D ( 'NONE', #26276, #15086, #31141 ) ;
#16163=DIRECTION ( 'NONE',  ( -1.000000000000000000, 0.000000000000000000, -0.000000000000000000 ) ) ;
#16174=DIRECTION ( 'NONE',  ( 0.000000000000000000, 0.000000000000000000, 1.000000000000000000 ) ) ;
#16176=ORIENTED_EDGE ( 'NONE', *, *, #28205, .F. ) ;
#16184=DIRECTION ( 'NONE',  ( 0.000000000000000000, 0.000000000000000000, 1.000000000000000000 ) ) ;
#16204=DIRECTION ( 'NONE',  ( -1.000000000000000000, 0.000000000000000000, 0.000000000000000000 ) ) ;
#16205=DIRECTION ( 'NONE',  ( 0.000000000000000000, 0.000000000000000000, 1.000000000000000000 ) ) ;
#16213=CARTESIAN_POINT ( 'NONE',  ( 0.000000000000000000, 0.000000000000000000, 0.000000000000000000 ) ) ;
#16223=ADVANCED_FACE ( 'NONE', ( #1746 ), #34515, .T. ) ;
#16224=AXIS2_PLACEMENT_3D ( 'NONE', #8038, #19020, #5354 ) ;
#16227=ORIENTED_EDGE ( 'NONE', *, *, #16268, .F. ) ;
#16231=ORIENTED_EDGE ( 'NONE', *, *, #21194, .F. ) ;
#16237=ORIENTED_EDGE ( 'NONE', *, *, #29725, .F. ) ;
#16238=ORIENTED_EDGE ( 'NONE', *, *, #17174, .F. ) ;
#16239=EDGE_CURVE ( 'NONE', #28676, #32250, #18107, .T. ) ;
#16250=EDGE_CURVE ( 'NONE', #24147, #14794, #33248, .T. ) ;
#16257=DIRECTION ( 'NONE',  ( 0.000000000000000000, 0.000000000000000000, 1.000000000000000000 ) ) ;
#16265=LINE ( 'NONE', #13591, #32013 ) ;
#16268=EDGE_CURVE ( 'NONE', #35594, #34977, #471, .T. ) ;
#16273=EDGE_LOOP ( 'NONE', ( #21419, #32463, #23836, #25805 ) ) ;
#16276=CARTESIAN_POINT ( 'NONE',  ( -9.999999999999994671, 0.000000000000000000, 0.000000000000000000 ) ) ;
#16282=EDGE_CURVE ( 'NONE', #20113, #14995, #21185, .T. ) ;
#16284=ORIENTED_EDGE ( 'NONE', *, *, #24342, .F. ) ;
#16286=CIRCLE ( 'NONE', #773, 20.00000000000000711 ) ;
#16295=CIRCLE ( 'NONE', #20897, 47.49900000000001654 ) ;
#16308=AXIS2_PLACEMENT_3D ( 'NONE', #4609, #4956, #23674 ) ;
#16311=ORIENTED_EDGE ( 'NONE', *, *, #587, .F. ) ;
#16315=CYLINDRICAL_SURFACE ( 'NONE', #15205, 20.00000000000000355 ) ;
#16325=CYLINDRICAL_SURFACE ( 'NONE', #19825, 20.00000000000000355 ) ;
#16334=DIRECTION ( 'NONE',  ( 0.000000000000000000, -0.8443279255020087470, -0.5358267949790065376 ) ) ;
#16337=EDGE_CURVE ( 'NONE', #15107, #11039, #16780, .T. ) ;
#16345=DIRECTION ( 'NONE',  ( -1.000000000000000000, -0.000000000000000000, 0.000000000000000000 ) ) ;
#16348=FACE_OUTER_BOUND ( 'NONE', #24233, .T. ) ;
#16350=DIRECTION ( 'NONE',  ( -1.000000000000000000, 0.000000000000000000, 0.000000000000000000 ) ) ;
#16355=ORIENTED_EDGE ( 'NONE', *, *, #21648, .T. ) ;
#16358=EDGE_CURVE ( 'NONE', #10989, #29853, #6229, .T. ) ;
#16366=ORIENTED_EDGE ( 'NONE', *, *, #10550, .F. ) ;
#16368=AXIS2_PLACEMENT_3D ( 'NONE', #12932, #34545, #23916 ) ;
#16370=DIRECTION ( 'NONE',  ( -1.000000000000000000, -0.000000000000000000, -0.000000000000000000 ) ) ;
#16373=FACE_OUTER_BOUND ( 'NONE', #6141, .T. ) ;
#16374=CARTESIAN_POINT ( 'NONE',  ( 0.000000000000000000, 51.85248208264518155, 3.914090171286368935 ) ) ;
#16382=EDGE_CURVE ( 'NONE', #30241, #6690, #30831, .T. ) ;
#16386=CIRCLE ( 'NONE', #17538, 20.00000000000000711 ) ;
#16399=CARTESIAN_POINT ( 'NONE',  ( 7.999999999999992895, -12.30077720129063934, -50.52416135122095397 ) ) ;
#16413=ORIENTED_EDGE ( 'NONE', *, *, #8140, .F. ) ;
#16414=ORIENTED_EDGE ( 'NONE', *, *, #3294, .F. ) ;
#16416=AXIS2_PLACEMENT_3D ( 'NONE', #28501, #26343, #34260 ) ;
#16420=EDGE_LOOP ( 'NONE', ( #27486, #9655, #29977, #16510 ) ) ;
#16424=DIRECTION ( 'NONE',  ( -1.000000000000000000, 0.000000000000000000, 0.000000000000000000 ) ) ;
#16426=AXIS2_PLACEMENT_3D ( 'NONE', #5405, #16881, #21942 ) ;
#16435=CARTESIAN_POINT ( 'NONE',  ( 7.999999999999992895, -43.55304910509386218, -28.41006711800031326 ) ) ;
#16442=CARTESIAN_POINT ( 'NONE',  ( 7.999999999999992895, 22.82995208772687334, 41.06517797613670950 ) ) ;
#16443=CARTESIAN_POINT ( 'NONE',  ( 7.999999999999992895, -36.05989434073592292, -30.12041790338657066 ) ) ;
#16458=EDGE_LOOP ( 'NONE', ( #28260, #35393, #21061, #26895 ) ) ;
#16473=VECTOR ( 'NONE', #5457, 1000.000000000000000 ) ;
#16475=LINE ( 'NONE', #35595, #16078 ) ;
#16478=CARTESIAN_POINT ( 'NONE',  ( 0.000000000000000000, 50.95304419620839553, -10.38206564895607897 ) ) ;
#16481=CARTESIAN_POINT ( 'NONE',  ( 0.000000000000000000, 7.162210897275723021, 51.50439529848832620 ) ) ;
#16486=CARTESIAN_POINT ( 'NONE',  ( 4.000000000000003553, 49.65209126885763169, 15.44894276735568539 ) ) ;
#16498=DIRECTION ( 'NONE',  ( -1.000000000000000000, 0.000000000000000000, 0.000000000000000000 ) ) ;
#16507=ORIENTED_EDGE ( 'NONE', *, *, #24763, .T. ) ;
#16510=ORIENTED_EDGE ( 'NONE', *, *, #6696, .T. ) ;
#16517=AXIS2_PLACEMENT_3D ( 'NONE', #35567, #10528, #16257 ) ;
#16530=AXIS2_PLACEMENT_3D ( 'NONE', #22140, #24681, #14383 ) ;
#16538=ADVANCED_FACE ( 'NONE', ( #31054 ), #30706, .T. ) ;
#16546=EDGE_LOOP ( 'NONE', ( #26351, #22609, #13257, #2643 ) ) ;
#16549=AXIS2_PLACEMENT_3D ( 'NONE', #12663, #20564, #34627 ) ;
#16552=DIRECTION ( 'NONE',  ( -1.000000000000000000, -0.000000000000000000, 0.000000000000000000 ) ) ;
#16554=EDGE_LOOP ( 'NONE', ( #35145, #33144, #1512, #26414 ) ) ;
#16556=CIRCLE ( 'NONE', #30953, 52.00000000000000711 ) ;
#16557=VECTOR ( 'NONE', #16685, 1000.000000000000000 ) ;
#16561=ORIENTED_EDGE ( 'NONE', *, *, #33902, .F. ) ;
#16567=DIRECTION ( 'NONE',  ( -1.000000000000000000, 0.000000000000000000, -0.000000000000000000 ) ) ;
#16572=DIRECTION ( 'NONE',  ( 0.000000000000000000, 0.000000000000000000, 1.000000000000000000 ) ) ;
#16577=CARTESIAN_POINT ( 'NONE',  ( 0.000000000000000000, -8.053585752061602321, -46.81126742072033409 ) ) ;
#16578=VECTOR ( 'NONE', #20432, 1000.000000000000000 ) ;
#16584=AXIS2_PLACEMENT_3D ( 'NONE', #13394, #31620, #23704 ) ;
#16590=ORIENTED_EDGE ( 'NONE', *, *, #24958, .T. ) ;
#16591=DIRECTION ( 'NONE',  ( 0.000000000000000000, -0.9980267284282723361, 0.06279051952930260472 ) ) ;
#16596=CARTESIAN_POINT ( 'NONE',  ( 0.000000000000000000, 0.000000000000000000, 0.000000000000000000 ) ) ;
#16599=EDGE_CURVE ( 'NONE', #8972, #20300, #1098, .T. ) ;
#16602=ORIENTED_EDGE ( 'NONE', *, *, #15044, .F. ) ;
#16608=ORIENTED_EDGE ( 'NONE', *, *, #27778, .F. ) ;
#16622=DIRECTION ( 'NONE',  ( 0.000000000000000000, 0.000000000000000000, 1.000000000000000000 ) ) ;
#16626=FACE_OUTER_BOUND ( 'NONE', #28458, .T. ) ;
#16629=VECTOR ( 'NONE', #8156, 1000.000000000000000 ) ;
#16636=DIRECTION ( 'NONE',  ( -1.000000000000000000, 0.000000000000000000, 0.000000000000000000 ) ) ;
#16640=DIRECTION ( 'NONE',  ( -1.000000000000000000, -0.000000000000000000, 0.000000000000000000 ) ) ;
#16642=DIRECTION ( 'NONE',  ( -1.000000000000000000, -0.000000000000000000, 0.000000000000000000 ) ) ;
#16646=ORIENTED_EDGE ( 'NONE', *, *, #1285, .F. ) ;
#16649=CIRCLE ( 'NONE', #27038, 52.00000000000000711 ) ;
#16653=CARTESIAN_POINT ( 'NONE',  ( 7.999999999999992895, 0.000000000000000000, 0.000000000000000000 ) ) ;
#16657=AXIS2_PLACEMENT_3D ( 'NONE', #26647, #1978, #7542 ) ;
#16660=CARTESIAN_POINT ( 'NONE',  ( 0.000000000000000000, -2.123073309834833111, -47.45152853935339010 ) ) ;
#16662=CARTESIAN_POINT ( 'NONE',  ( 0.000000000000000000, 0.000000000000000000, 0.000000000000000000 ) ) ;
#16667=DIRECTION ( 'NONE',  ( 0.000000000000000000, 0.000000000000000000, 1.000000000000000000 ) ) ;
#16668=ORIENTED_EDGE ( 'NONE', *, *, #27778, .T. ) ;
#16671=FACE_OUTER_BOUND ( 'NONE', #33928, .T. ) ;
#16685=DIRECTION ( 'NONE',  ( -1.000000000000000000, 0.000000000000000000, 0.000000000000000000 ) ) ;
#16687=EDGE_CURVE ( 'NONE', #19047, #11680, #23501, .T. ) ;
#16692=CARTESIAN_POINT ( 'NONE',  ( 7.999999999999992895, 0.000000000000000000, 0.000000000000000000 ) ) ;
#16705=EDGE_CURVE ( 'NONE', #19242, #31652, #34833, .T. ) ;
#16708=CARTESIAN_POINT ( 'NONE',  ( 7.999999999999992895, 11.90021268425554624, 45.45261810511217959 ) ) ;
#16713=VERTEX_POINT ( 'NONE', #32123 ) ;
#16727=EDGE_LOOP ( 'NONE', ( #13441, #16284, #4981, #30471 ) ) ;
#16729=DIRECTION ( 'NONE',  ( 0.000000000000000000, 0.000000000000000000, 1.000000000000000000 ) ) ;
#16753=ORIENTED_EDGE ( 'NONE', *, *, #27515, .T. ) ;
#16757=AXIS2_PLACEMENT_3D ( 'NONE', #1387, #17219, #12011 ) ;
#16760=DIRECTION ( 'NONE',  ( -1.000000000000000000, -0.000000000000000000, 0.000000000000000000 ) ) ;
#16763=DIRECTION ( 'NONE',  ( 0.000000000000000000, -0.6845471059286951654, 0.7289686274214054462 ) ) ;
#16772=ORIENTED_EDGE ( 'NONE', *, *, #21195, .T. ) ;
#16780=LINE ( 'NONE', #33187, #23481 ) ;
#16784=DIRECTION ( 'NONE',  ( 0.000000000000000000, 0.000000000000000000, 1.000000000000000000 ) ) ;
#16789=EDGE_CURVE ( 'NONE', #32720, #35265, #18336, .T. ) ;
#16791=CARTESIAN_POINT ( 'NONE',  ( 0.000000000000000000, 9.744342220504046637, -46.48873837489789196 ) ) ;
#16792=AXIS2_PLACEMENT_3D ( 'NONE', #10358, #35380, #24926 ) ;
#16797=CYLINDRICAL_SURFACE ( 'NONE', #12523, 52.00000000000000711 ) ;
#16798=FACE_OUTER_BOUND ( 'NONE', #1517, .T. ) ;
#16799=DIRECTION ( 'NONE',  ( -1.000000000000000000, -0.000000000000000000, -0.000000000000000000 ) ) ;
#16802=CYLINDRICAL_SURFACE ( 'NONE', #14105, 20.00000000000000355 ) ;
#16805=CARTESIAN_POINT ( 'NONE',  ( 7.999999999999992895, 35.20873326984081331, 31.88259874184044662 ) ) ;
#16811=ORIENTED_EDGE ( 'NONE', *, *, #8709, .T. ) ;
#16820=ORIENTED_EDGE ( 'NONE', *, *, #21344, .T. ) ;
#16822=CIRCLE ( 'NONE', #5908, 20.00000000000000355 ) ;
#16824=DIRECTION ( 'NONE',  ( 0.000000000000000000, 0.000000000000000000, 1.000000000000000000 ) ) ;
#16828=CIRCLE ( 'NONE', #27222, 52.00000000000000711 ) ;
#16831=LINE ( 'NONE', #27668, #11378 ) ;
#16833=CARTESIAN_POINT ( 'NONE',  ( 7.999999999999992895, 8.053585752062575764, -46.81126742072014224 ) ) ;
#16843=VECTOR ( 'NONE', #29887, 1000.000000000000000 ) ;
#16844=CARTESIAN_POINT ( 'NONE',  ( 0.000000000000000000, 39.78933988720149273, -24.98727647984960853 ) ) ;
#16847=CARTESIAN_POINT ( 'NONE',  ( 7.999999999999992895, -38.92705108641712286, -27.21837053747841395 ) ) ;
#16851=ORIENTED_EDGE ( 'NONE', *, *, #24109, .T. ) ;
#16856=DIRECTION ( 'NONE',  ( 0.000000000000000000, 0.000000000000000000, 1.000000000000000000 ) ) ;
#16862=ORIENTED_EDGE ( 'NONE', *, *, #25355, .T. ) ;
#16863=ORIENTED_EDGE ( 'NONE', *, *, #24154, .F. ) ;
#16870=CARTESIAN_POINT ( 'NONE',  ( 7.999999999999992895, 0.000000000000000000, 0.000000000000000000 ) ) ;
#16875=FACE_OUTER_BOUND ( 'NONE', #28791, .T. ) ;
#16881=DIRECTION ( 'NONE',  ( -1.000000000000000000, 0.000000000000000000, 0.000000000000000000 ) ) ;
#16883=VERTEX_POINT ( 'NONE', #4946 ) ;
#16895=DIRECTION ( 'NONE',  ( 1.000000000000000000, 0.000000000000000000, 0.000000000000000000 ) ) ;
#16896=AXIS2_PLACEMENT_3D ( 'NONE', #34728, #31490, #14907 ) ;
#16901=DIRECTION ( 'NONE',  ( -1.000000000000000000, 0.000000000000000000, 0.000000000000000000 ) ) ;
#16904=VERTEX_POINT ( 'NONE', #62 ) ;
#16909=EDGE_CURVE ( 'NONE', #9660, #13354, #10878, .T. ) ;
#16913=CARTESIAN_POINT ( 'NONE',  ( 7.999999999999992895, 47.49120266317496686, -0.8606222198176971538 ) ) ;
#16919=DIRECTION ( 'NONE',  ( 0.000000000000000000, 0.000000000000000000, 1.000000000000000000 ) ) ;
#16924=EDGE_CURVE ( 'NONE', #32382, #6142, #30455, .T. ) ;
#16926=DIRECTION ( 'NONE',  ( -1.000000000000000000, -0.000000000000000000, -0.000000000000000000 ) ) ;
#16934=VERTEX_POINT ( 'NONE', #25623 ) ;
#16952=ORIENTED_EDGE ( 'NONE', *, *, #10440, .T. ) ;
#16953=DIRECTION ( 'NONE',  ( -1.000000000000000000, 0.000000000000000000, 0.000000000000000000 ) ) ;
#16959=ADVANCED_FACE ( 'NONE', ( #6173 ), #31189, .T. ) ;
#16966=DIRECTION ( 'NONE',  ( -1.000000000000000000, 0.000000000000000000, 0.000000000000000000 ) ) ;
#16967=ORIENTED_EDGE ( 'NONE', *, *, #29728, .T. ) ;
#16979=CARTESIAN_POINT ( 'NONE',  ( 0.000000000000000000, 19.44205635905602847, -43.33776004284589334 ) ) ;
#16982=VERTEX_POINT ( 'NONE', #33360 ) ;
#16983=CIRCLE ( 'NONE', #3215, 20.00000000000000711 ) ;
#16984=CARTESIAN_POINT ( 'NONE',  ( 7.999999999999992895, 47.32430374665963058, -21.55018039121478424 ) ) ;
#16986=DIRECTION ( 'NONE',  ( 0.000000000000000000, 0.000000000000000000, 1.000000000000000000 ) ) ;
#16996=EDGE_CURVE ( 'NONE', #25438, #33987, #28137, .T. ) ;
#16997=CARTESIAN_POINT ( 'NONE',  ( 7.999999999999992895, 0.000000000000000000, 0.000000000000000000 ) ) ;
#16999=CIRCLE ( 'NONE', #7809, 47.49900000000001654 ) ;
#17003=DIRECTION ( 'NONE',  ( -1.000000000000000000, 0.000000000000000000, 0.000000000000000000 ) ) ;
#17004=ADVANCED_FACE ( 'NONE', ( #33896 ), #5994, .T. ) ;
#17005=CIRCLE ( 'NONE', #1506, 20.00000000000000711 ) ;
#17007=DIRECTION ( 'NONE',  ( -1.000000000000000000, 0.000000000000000000, -0.000000000000000000 ) ) ;
#17017=CARTESIAN_POINT ( 'NONE',  ( 0.000000000000000000, -46.87740477351715640, 16.82754413119429415 ) ) ;
#17019=ORIENTED_EDGE ( 'NONE', *, *, #13822, .T. ) ;
#17033=ADVANCED_FACE ( 'NONE', ( #19653 ), #9046, .T. ) ;
#17036=FACE_OUTER_BOUND ( 'NONE', #25446, .T. ) ;
#17038=DIRECTION ( 'NONE',  ( 0.000000000000000000, 0.000000000000000000, 1.000000000000000000 ) ) ;
#17046=DIRECTION ( 'NONE',  ( 0.000000000000000000, 0.000000000000000000, -1.000000000000000000 ) ) ;
#17059=AXIS2_PLACEMENT_3D ( 'NONE', #25502, #6575, #34317 ) ;
#17074=DIRECTION ( 'NONE',  ( -1.000000000000000000, -0.000000000000000000, 0.000000000000000000 ) ) ;
#17075=CARTESIAN_POINT ( 'NONE',  ( 7.999999999999992895, 39.64889472655782043, -33.64468972902464827 ) ) ;
#17077=ADVANCED_FACE ( 'NONE', ( #22542 ), #30494, .T. ) ;
#17084=FACE_OUTER_BOUND ( 'NONE', #20581, .T. ) ;
#17090=CARTESIAN_POINT ( 'NONE',  ( 4.000000000000003553, 50.95304419620839553, -10.38206564895607897 ) ) ;
#17112=DIRECTION ( 'NONE',  ( -1.000000000000000000, 0.000000000000000000, -0.000000000000000000 ) ) ;
#17115=DIRECTION ( 'NONE',  ( -1.000000000000000000, -0.000000000000000000, -0.000000000000000000 ) ) ;
#17130=EDGE_LOOP ( 'NONE', ( #20152, #34062, #21950, #24822 ) ) ;
#17137=CARTESIAN_POINT ( 'NONE',  ( 7.999999999999992895, 6.109652351742432153, -46.58570277113502556 ) ) ;
#17142=AXIS2_PLACEMENT_3D ( 'NONE', #21914, #30208, #18863 ) ;
#17145=DIRECTION ( 'NONE',  ( 0.000000000000000000, -0.5877852522924624790, -0.8090169943749551118 ) ) ;
#17156=AXIS2_PLACEMENT_3D ( 'NONE', #23, #18745, #7587 ) ;
#17157=FACE_OUTER_BOUND ( 'NONE', #31553, .T. ) ;
#17161=DIRECTION ( 'NONE',  ( -1.000000000000000000, 0.000000000000000000, -0.000000000000000000 ) ) ;
#17162=ADVANCED_FACE ( 'NONE', ( #15502 ), #4375, .T. ) ;
#17164=DIRECTION ( 'NONE',  ( -1.000000000000000000, -0.000000000000000000, -0.000000000000000000 ) ) ;
#17165=ORIENTED_EDGE ( 'NONE', *, *, #11527, .T. ) ;
#17170=VERTEX_POINT ( 'NONE', #15322 ) ;
#17174=EDGE_CURVE ( 'NONE', #26508, #17425, #13191, .T. ) ;
#17194=CARTESIAN_POINT ( 'NONE',  ( 0.000000000000000000, -19.74581912682874929, 48.10512059033386834 ) ) ;
#17199=LINE ( 'NONE', #648, #27901 ) ;
#17205=DIRECTION ( 'NONE',  ( -1.000000000000000000, 0.000000000000000000, -0.000000000000000000 ) ) ;
#17206=ORIENTED_EDGE ( 'NONE', *, *, #24184, .T. ) ;
#17210=EDGE_CURVE ( 'NONE', #33795, #9689, #26334, .T. ) ;
#17214=CIRCLE ( 'NONE', #6305, 52.00000000000000711 ) ;
#17219=DIRECTION ( 'NONE',  ( -1.000000000000000000, -0.000000000000000000, -0.000000000000000000 ) ) ;
#17221=ORIENTED_EDGE ( 'NONE', *, *, #3178, .T. ) ;
#17231=CARTESIAN_POINT ( 'NONE',  ( 7.999999999999992895, 13.85708833599969303, 45.43276465116672114 ) ) ;
#17233=DIRECTION ( 'NONE',  ( -1.000000000000000000, -0.000000000000000000, 0.000000000000000000 ) ) ;
#17240=DIRECTION ( 'NONE',  ( -1.000000000000000000, 0.000000000000000000, -0.000000000000000000 ) ) ;
#17243=AXIS2_PLACEMENT_3D ( 'NONE', #30602, #16895, #5937 ) ;
#17245=CARTESIAN_POINT ( 'NONE',  ( 0.000000000000000000, -0.2227391519113268437, -46.98410307550732057 ) ) ;
#17248=VERTEX_POINT ( 'NONE', #23077 ) ;
#17252=ORIENTED_EDGE ( 'NONE', *, *, #29587, .F. ) ;
#17253=EDGE_CURVE ( 'NONE', #33486, #29368, #31369, .T. ) ;
#17254=ORIENTED_EDGE ( 'NONE', *, *, #18094, .F. ) ;
#17256=VERTEX_POINT ( 'NONE', #11006 ) ;
#17259=AXIS2_PLACEMENT_3D ( 'NONE', #10881, #35028, #32303 ) ;
#17261=CYLINDRICAL_SURFACE ( 'NONE', #25369, 47.49900000000001654 ) ;
#17262=ORIENTED_EDGE ( 'NONE', *, *, #26167, .F. ) ;
#17278=ORIENTED_EDGE ( 'NONE', *, *, #698, .F. ) ;
#17285=AXIS2_PLACEMENT_3D ( 'NONE', #21224, #25626, #17496 ) ;
#17287=CARTESIAN_POINT ( 'NONE',  ( -9.999999999999994671, 0.000000000000000000, 0.000000000000000000 ) ) ;
#17289=CARTESIAN_POINT ( 'NONE',  ( 0.000000000000000000, -17.50309955389642269, 43.60271849949356948 ) ) ;
#17295=MECHANICAL_DESIGN_GEOMETRIC_PRESENTATION_REPRESENTATION('',(#23666),#27682);
#17301=ORIENTED_EDGE ( 'NONE', *, *, #31642, .T. ) ;
#17318=DIRECTION ( 'NONE',  ( -1.000000000000000000, -0.000000000000000000, 0.000000000000000000 ) ) ;
#17322=FACE_OUTER_BOUND ( 'NONE', #3780, .T. ) ;
#17323=CARTESIAN_POINT ( 'NONE',  ( 7.999999999999992895, 42.41764978026606059, -20.20639853260303198 ) ) ;
#17327=DIRECTION ( 'NONE',  ( 0.000000000000000000, 0.000000000000000000, -1.000000000000000000 ) ) ;
#17331=EDGE_CURVE ( 'NONE', #28676, #30827, #32168, .T. ) ;
#17333=DIRECTION ( 'NONE',  ( -1.000000000000000000, 0.000000000000000000, 0.000000000000000000 ) ) ;
#17337=FACE_OUTER_BOUND ( 'NONE', #11190, .T. ) ;
#17338=DIRECTION ( 'NONE',  ( -1.000000000000000000, -0.000000000000000000, 0.000000000000000000 ) ) ;
#17343=AXIS2_PLACEMENT_3D ( 'NONE', #11004, #32787, #13876 ) ;
#17351=FACE_BOUND ( 'NONE', #30572, .T. ) ;
#17361=DIRECTION ( 'NONE',  ( 0.000000000000000000, 0.000000000000000000, 1.000000000000000000 ) ) ;
#17369=CARTESIAN_POINT ( 'NONE',  ( 0.000000000000000000, 0.000000000000000000, 0.000000000000000000 ) ) ;
#17370=FACE_OUTER_BOUND ( 'NONE', #226, .T. ) ;
#17371=CYLINDRICAL_SURFACE ( 'NONE', #7280, 20.00000000000000355 ) ;
#17376=DIRECTION ( 'NONE',  ( -1.000000000000000000, 0.000000000000000000, 0.000000000000000000 ) ) ;
#17387=AXIS2_PLACEMENT_3D ( 'NONE', #30508, #30850, #22379 ) ;
#17388=DIRECTION ( 'NONE',  ( -1.000000000000000000, 0.000000000000000000, 0.000000000000000000 ) ) ;
#17391=ADVANCED_FACE ( 'NONE', ( #23756 ), #29693, .T. ) ;
#17394=ORIENTED_EDGE ( 'NONE', *, *, #30836, .F. ) ;
#17397=CARTESIAN_POINT ( 'NONE',  ( -9.999999999999994671, 0.000000000000000000, 0.000000000000000000 ) ) ;
#17407=CARTESIAN_POINT ( 'NONE',  ( 7.999999999999992895, -46.19362259308839214, 8.585149169758333088 ) ) ;
#17409=EDGE_CURVE ( 'NONE', #19596, #29784, #29326, .T. ) ;
#17416=ORIENTED_EDGE ( 'NONE', *, *, #11458, .F. ) ;
#17420=AXIS2_PLACEMENT_3D ( 'NONE', #8892, #19340, #24769 ) ;
#17422=CARTESIAN_POINT ( 'NONE',  ( 7.999999999999992895, -43.55304910509426719, 28.41006711799970574 ) ) ;
#17425=VERTEX_POINT ( 'NONE', #35458 ) ;
#17428=CARTESIAN_POINT ( 'NONE',  ( 7.999999999999992895, -32.32520163883559405, -34.09746168776067776 ) ) ;
#17430=VERTEX_POINT ( 'NONE', #7713 ) ;
#17432=CARTESIAN_POINT ( 'NONE',  ( 7.999999999999992895, 41.20225022064637699, 23.63323037071417332 ) ) ;
#17442=ADVANCED_FACE ( 'NONE', ( #23942 ), #18347, .T. ) ;
#17447=DIRECTION ( 'NONE',  ( 0.000000000000000000, 0.3681245526846787519, -0.9297764858882511252 ) ) ;
#17448=ORIENTED_EDGE ( 'NONE', *, *, #30690, .F. ) ;
#17451=LINE ( 'NONE', #5786, #26917 ) ;
#17452=EDGE_CURVE ( 'NONE', #27872, #7481, #7377, .T. ) ;
#17460=VERTEX_POINT ( 'NONE', #24124 ) ;
#17461=LINE ( 'NONE', #25944, #26770 ) ;
#17463=EDGE_LOOP ( 'NONE', ( #10014, #23981, #23104, #101 ) ) ;
#17473=CARTESIAN_POINT ( 'NONE',  ( 0.000000000000000000, 0.000000000000000000, 0.000000000000000000 ) ) ;
#17492=ORIENTED_EDGE ( 'NONE', *, *, #4523, .T. ) ;
#17496=DIRECTION ( 'NONE',  ( 0.000000000000000000, 0.000000000000000000, 1.000000000000000000 ) ) ;
#17501=DIRECTION ( 'NONE',  ( 0.000000000000000000, 0.000000000000000000, 1.000000000000000000 ) ) ;
#17502=CARTESIAN_POINT ( 'NONE',  ( 0.000000000000000000, -36.34385289850568057, -29.77717097092114074 ) ) ;
#17508=ORIENTED_EDGE ( 'NONE', *, *, #6007, .F. ) ;
#17510=CARTESIAN_POINT ( 'NONE',  ( 0.000000000000000000, -32.00046193115173310, 34.40241257139674502 ) ) ;
#17511=CARTESIAN_POINT ( 'NONE',  ( 7.999999999999992895, 0.000000000000000000, 0.000000000000000000 ) ) ;
#17526=ORIENTED_EDGE ( 'NONE', *, *, #26013, .F. ) ;
#17530=DIRECTION ( 'NONE',  ( 0.000000000000000000, -0.1253332335642905471, -0.9921147013144795412 ) ) ;
#17532=DIRECTION ( 'NONE',  ( -1.000000000000000000, -0.000000000000000000, -0.000000000000000000 ) ) ;
#17538=AXIS2_PLACEMENT_3D ( 'NONE', #4831, #23725, #15773 ) ;
#17545=VECTOR ( 'NONE', #18092, 1000.000000000000000 ) ;
#17553=DIRECTION ( 'NONE',  ( 0.000000000000000000, 0.000000000000000000, -1.000000000000000000 ) ) ;
#17556=CIRCLE ( 'NONE', #11808, 52.00000000000000711 ) ;
#17565=CIRCLE ( 'NONE', #25640, 20.00000000000000355 ) ;
#17577=ORIENTED_EDGE ( 'NONE', *, *, #33010, .F. ) ;
#17585=CARTESIAN_POINT ( 'NONE',  ( 0.000000000000000000, 32.00046193115148441, 34.40241257139697950 ) ) ;
#17592=DIRECTION ( 'NONE',  ( 0.000000000000000000, 0.9510565162951544194, -0.3090169943749447867 ) ) ;
#17593=ORIENTED_EDGE ( 'NONE', *, *, #6641, .F. ) ;
#17609=EDGE_CURVE ( 'NONE', #33387, #18497, #22282, .T. ) ;
#17610=DIRECTION ( 'NONE',  ( -1.000000000000000000, -0.000000000000000000, -0.000000000000000000 ) ) ;
#17622=VECTOR ( 'NONE', #31694, 1000.000000000000000 ) ;
#17624=CYLINDRICAL_SURFACE ( 'NONE', #24699, 20.00000000000000355 ) ;
#17637=CIRCLE ( 'NONE', #11919, 47.49900000000000944 ) ;
#17645=VERTEX_POINT ( 'NONE', #17809 ) ;
#17646=CARTESIAN_POINT ( 'NONE',  ( 4.000000000000003553, 51.19683565102445044, 9.104066087303658961 ) ) ;
#17649=ORIENTED_EDGE ( 'NONE', *, *, #13509, .T. ) ;
#17657=EDGE_CURVE ( 'NONE', #2418, #7438, #6873, .T. ) ;
#17658=EDGE_LOOP ( 'NONE', ( #14968, #9028, #35352, #18904 ) ) ;
#17662=CIRCLE ( 'NONE', #32070, 20.00000000000001421 ) ;
#17666=ORIENTED_EDGE ( 'NONE', *, *, #3395, .F. ) ;
#17668=ADVANCED_FACE ( 'NONE', ( #30225 ), #5564, .T. ) ;
#17669=DIRECTION ( 'NONE',  ( -1.000000000000000000, -0.000000000000000000, -0.000000000000000000 ) ) ;
#17670=ADVANCED_FACE ( 'NONE', ( #18118 ), #34525, .T. ) ;
#17671=AXIS2_PLACEMENT_3D ( 'NONE', #13260, #8358, #18821 ) ;
#17672=DIRECTION ( 'NONE',  ( 0.000000000000000000, 0.000000000000000000, 1.000000000000000000 ) ) ;
#17677=ORIENTED_EDGE ( 'NONE', *, *, #32309, .F. ) ;
#17681=CIRCLE ( 'NONE', #11368, 52.00000000000000711 ) ;
#17688=DIRECTION ( 'NONE',  ( 0.000000000000000000, 0.3681245526846720906, 0.9297764858882537897 ) ) ;
#17691=CARTESIAN_POINT ( 'NONE',  ( -9.999999999999994671, 0.000000000000000000, 0.000000000000000000 ) ) ;
#17693=DIRECTION ( 'NONE',  ( -1.000000000000000000, 0.000000000000000000, 0.000000000000000000 ) ) ;
#17696=DIRECTION ( 'NONE',  ( -1.000000000000000000, -0.000000000000000000, 0.000000000000000000 ) ) ;
#17705=DIRECTION ( 'NONE',  ( 0.000000000000000000, -0.6845471059286791782, -0.7289686274214204342 ) ) ;
#17707=ORIENTED_EDGE ( 'NONE', *, *, #15213, .F. ) ;
#17711=VECTOR ( 'NONE', #5352, 1000.000000000000000 ) ;
#17721=CARTESIAN_POINT ( 'NONE',  ( 4.000000000000003553, 7.162210897275723021, 51.50439529848832620 ) ) ;
#17724=DIRECTION ( 'NONE',  ( -1.000000000000000000, 0.000000000000000000, -0.000000000000000000 ) ) ;
#17725=ORIENTED_EDGE ( 'NONE', *, *, #33446, .F. ) ;
#17729=CYLINDRICAL_SURFACE ( 'NONE', #2436, 20.00000000000000355 ) ;
#17731=CARTESIAN_POINT ( 'NONE',  ( 7.999999999999992895, -20.99948489194393275, -42.60488980472803888 ) ) ;
#17736=DIRECTION ( 'NONE',  ( -1.000000000000000000, -0.000000000000000000, -0.000000000000000000 ) ) ;
#17740=DIRECTION ( 'NONE',  ( -1.000000000000000000, -0.000000000000000000, 0.000000000000000000 ) ) ;
#17755=ORIENTED_EDGE ( 'NONE', *, *, #29324, .F. ) ;
#17757=AXIS2_PLACEMENT_3D ( 'NONE', #17137, #25265, #31014 ) ;
#17759=DIRECTION ( 'NONE',  ( 0.000000000000000000, 0.000000000000000000, 1.000000000000000000 ) ) ;
#17764=DIRECTION ( 'NONE',  ( 0.000000000000000000, 0.000000000000000000, 1.000000000000000000 ) ) ;
#17771=CYLINDRICAL_SURFACE ( 'NONE', #2105, 20.00000000000000355 ) ;
#17773=ADVANCED_FACE ( 'NONE', ( #20449 ), #31462, .T. ) ;
#17778=DIRECTION ( 'NONE',  ( -1.000000000000000000, -0.000000000000000000, 0.000000000000000000 ) ) ;
#17780=ORIENTED_EDGE ( 'NONE', *, *, #7618, .F. ) ;
#17784=LINE ( 'NONE', #6458, #18064 ) ;
#17791=CARTESIAN_POINT ( 'NONE',  ( 7.999999999999992895, -46.21320724403657465, 10.97699764141937884 ) ) ;
#17796=ORIENTED_EDGE ( 'NONE', *, *, #19383, .T. ) ;
#17802=CARTESIAN_POINT ( 'NONE',  ( 7.999999999999992895, 27.43636312076375461, -38.14186064215119387 ) ) ;
#17808=AXIS2_PLACEMENT_3D ( 'NONE', #12342, #3376, #9460 ) ;
#17809=CARTESIAN_POINT ( 'NONE',  ( 0.000000000000000000, 18.53613841426857789, -48.58406706613882875 ) ) ;
#17812=CARTESIAN_POINT ( 'NONE',  ( 50.00005079999998969, 14.30000000000000071, -3.000000000000002665 ) ) ;
#17815=CARTESIAN_POINT ( 'NONE',  ( 4.000000000000003553, -24.47917365149978508, 45.87777302070926311 ) ) ;
#17825=CARTESIAN_POINT ( 'NONE',  ( 7.999999999999992895, 0.000000000000000000, 0.000000000000000000 ) ) ;
#17826=ORIENTED_EDGE ( 'NONE', *, *, #31733, .T. ) ;
#17828=LINE ( 'NONE', #7031, #2401 ) ;
#17830=EDGE_CURVE ( 'NONE', #35186, #11728, #994, .T. ) ;
#17831=ORIENTED_EDGE ( 'NONE', *, *, #12730, .F. ) ;
#17835=DIRECTION ( 'NONE',  ( -1.000000000000000000, -0.000000000000000000, -0.000000000000000000 ) ) ;
#17843=DIRECTION ( 'NONE',  ( 0.000000000000000000, 0.1253332335643045359, -0.9921147013144778759 ) ) ;
#17850=EDGE_LOOP ( 'NONE', ( #1786, #20956, #357, #14693 ) ) ;
#17855=VECTOR ( 'NONE', #25267, 1000.000000000000000 ) ;
#17856=CARTESIAN_POINT ( 'NONE',  ( 0.000000000000000000, -7.162210897276083621, 51.50439529848826936 ) ) ;
#17861=CARTESIAN_POINT ( 'NONE',  ( 7.999999999999992895, -27.43636312076294814, -38.14186064215180494 ) ) ;
#17870=DIRECTION ( 'NONE',  ( 0.000000000000000000, 0.3681245526846719240, 0.9297764858882537897 ) ) ;
#17872=DIRECTION ( 'NONE',  ( -1.000000000000000000, 0.000000000000000000, -0.000000000000000000 ) ) ;
#17878=CYLINDRICAL_SURFACE ( 'NONE', #28527, 20.00000000000000355 ) ;
#17881=ORIENTED_EDGE ( 'NONE', *, *, #23388, .F. ) ;
#17882=VERTEX_POINT ( 'NONE', #10027 ) ;
#17885=ORIENTED_EDGE ( 'NONE', *, *, #31358, .F. ) ;
#17889=AXIS2_PLACEMENT_3D ( 'NONE', #33685, #14590, #25603 ) ;
#17898=DIRECTION ( 'NONE',  ( -1.000000000000000000, -0.000000000000000000, -0.000000000000000000 ) ) ;
#17914=CARTESIAN_POINT ( 'NONE',  ( 0.000000000000000000, -22.82995208772657492, -41.06517797613687293 ) ) ;
#17915=ORIENTED_EDGE ( 'NONE', *, *, #21344, .F. ) ;
#17922=ORIENTED_EDGE ( 'NONE', *, *, #16282, .F. ) ;
#17923=DIRECTION ( 'NONE',  ( -1.000000000000000000, 0.000000000000000000, 0.000000000000000000 ) ) ;
#17927=ORIENTED_EDGE ( 'NONE', *, *, #30141, .F. ) ;
#17932=DIRECTION ( 'NONE',  ( 0.000000000000000000, -0.9822872507286903865, 0.1873813145857150253 ) ) ;
#17933=ORIENTED_EDGE ( 'NONE', *, *, #11285, .F. ) ;
#17934=EDGE_LOOP ( 'NONE', ( #5119, #21422, #5347, #6827 ) ) ;
#17944=CARTESIAN_POINT ( 'NONE',  ( 0.000000000000000000, -38.92705108641750655, 27.21837053747785973 ) ) ;
#17956=CARTESIAN_POINT ( 'NONE',  ( 4.000000000000003553, 31.08872492059957793, 41.68322423723111569 ) ) ;
#17964=ORIENTED_EDGE ( 'NONE', *, *, #14607, .T. ) ;
#17972=ORIENTED_EDGE ( 'NONE', *, *, #28778, .F. ) ;
#17990=DIRECTION ( 'NONE',  ( 1.000000000000000000, 0.000000000000000000, -0.000000000000000000 ) ) ;
#17993=ORIENTED_EDGE ( 'NONE', *, *, #13888, .F. ) ;
#17994=CARTESIAN_POINT ( 'NONE',  ( 7.999999999999992895, 0.000000000000000000, 0.000000000000000000 ) ) ;
#17998=VERTEX_POINT ( 'NONE', #31993 ) ;
#18001=CIRCLE ( 'NONE', #3663, 47.49900000000001654 ) ;
#18003=ORIENTED_EDGE ( 'NONE', *, *, #28864, .F. ) ;
#18004=VECTOR ( 'NONE', #18075, 1000.000000000000000 ) ;
#18006=CARTESIAN_POINT ( 'NONE',  ( 4.000000000000003553, 51.85248208264518155, 3.914090171286383146 ) ) ;
#18008=ORIENTED_EDGE ( 'NONE', *, *, #11448, .F. ) ;
#18010=EDGE_CURVE ( 'NONE', #29619, #24892, #1022, .T. ) ;
#18019=CARTESIAN_POINT ( 'NONE',  ( 0.000000000000000000, 40.47821179127715396, 32.64221760512774040 ) ) ;
#18025=EDGE_CURVE ( 'NONE', #9, #33840, #26317, .T. ) ;
#18026=CARTESIAN_POINT ( 'NONE',  ( 0.000000000000000000, -9.744342220503076746, -46.48873837489808380 ) ) ;
#18030=AXIS2_PLACEMENT_3D ( 'NONE', #29128, #34531, #31634 ) ;
#18035=EDGE_CURVE ( 'NONE', #22481, #26780, #19949, .T. ) ;
#18038=CARTESIAN_POINT ( 'NONE',  ( 7.999999999999992895, -42.41764978026620270, 20.20639853260275487 ) ) ;
#18043=DIRECTION ( 'NONE',  ( 0.000000000000000000, 0.000000000000000000, 1.000000000000000000 ) ) ;
#18044=DIRECTION ( 'NONE',  ( 0.000000000000000000, 0.5877852522924685852, 0.8090169943749506709 ) ) ;
#18045=VERTEX_POINT ( 'NONE', #16478 ) ;
#18046=CARTESIAN_POINT ( 'NONE',  ( 7.999999999999992895, 0.000000000000000000, 0.000000000000000000 ) ) ;
#18048=CARTESIAN_POINT ( 'NONE',  ( 7.999999999999992895, -13.56094713063537327, -50.20060470671755581 ) ) ;
#18060=ORIENTED_EDGE ( 'NONE', *, *, #2042, .F. ) ;
#18064=VECTOR ( 'NONE', #15435, 1000.000000000000000 ) ;
#18066=AXIS2_PLACEMENT_3D ( 'NONE', #19066, #29711, #5057 ) ;
#18067=EDGE_CURVE ( 'NONE', #23561, #14501, #16831, .T. ) ;
#18068=EDGE_CURVE ( 'NONE', #4435, #34390, #9650, .T. ) ;
#18075=DIRECTION ( 'NONE',  ( -1.000000000000000000, 0.000000000000000000, 0.000000000000000000 ) ) ;
#18085=DIRECTION ( 'NONE',  ( 0.000000000000000000, 0.000000000000000000, 1.000000000000000000 ) ) ;
#18088=CARTESIAN_POINT ( 'NONE',  ( 7.999999999999992895, 46.19362259308833529, 8.585149169758651055 ) ) ;
#18092=DIRECTION ( 'NONE',  ( -1.000000000000000000, -0.000000000000000000, 0.000000000000000000 ) ) ;
#18094=EDGE_CURVE ( 'NONE', #10384, #7481, #27838, .T. ) ;
#18095=AXIS2_PLACEMENT_3D ( 'NONE', #35090, #32365, #1599 ) ;
#18096=ORIENTED_EDGE ( 'NONE', *, *, #28925, .F. ) ;
#18097=VERTEX_POINT ( 'NONE', #25136 ) ;
#18106=CARTESIAN_POINT ( 'NONE',  ( 0.000000000000000000, 38.92705108641732181, 27.21837053747812263 ) ) ;
#18107=LINE ( 'NONE', #4462, #1076 ) ;
#18109=EDGE_CURVE ( 'NONE', #20427, #18045, #16556, .T. ) ;
#18113=AXIS2_PLACEMENT_3D ( 'NONE', #5404, #24659, #30063 ) ;
#18116=DIRECTION ( 'NONE',  ( -1.000000000000000000, 0.000000000000000000, -0.000000000000000000 ) ) ;
#18118=FACE_OUTER_BOUND ( 'NONE', #20155, .T. ) ;
#18120=FACE_OUTER_BOUND ( 'NONE', #16546, .T. ) ;
#18130=FACE_OUTER_BOUND ( 'NONE', #3167, .T. ) ;
#18139=ORIENTED_EDGE ( 'NONE', *, *, #34186, .T. ) ;
#18141=EDGE_CURVE ( 'NONE', #7789, #13072, #28087, .T. ) ;
#18149=AXIS2_PLACEMENT_3D ( 'NONE', #27803, #17318, #17145 ) ;
#18151=DIRECTION ( 'NONE',  ( -1.000000000000000000, 0.000000000000000000, 0.000000000000000000 ) ) ;
#18160=CARTESIAN_POINT ( 'NONE',  ( 7.999999999999992895, 0.000000000000000000, 0.000000000000000000 ) ) ;
#18161=ADVANCED_FACE ( 'NONE', ( #2654 ), #11266, .T. ) ;
#18163=ORIENTED_EDGE ( 'NONE', *, *, #21166, .T. ) ;
#18172=VECTOR ( 'NONE', #26979, 1000.000000000000000 ) ;
#18176=DIRECTION ( 'NONE',  ( -1.000000000000000000, -0.000000000000000000, 0.000000000000000000 ) ) ;
#18187=ORIENTED_EDGE ( 'NONE', *, *, #10138, .F. ) ;
#18190=CARTESIAN_POINT ( 'NONE',  ( 0.000000000000000000, -11.90021268425586953, 45.45261810511210143 ) ) ;
#18195=CARTESIAN_POINT ( 'NONE',  ( 7.999999999999992895, 34.03046037009305280, -33.13733193845769165 ) ) ;
#18198=ORIENTED_EDGE ( 'NONE', *, *, #8796, .F. ) ;
#18202=VECTOR ( 'NONE', #15737, 1000.000000000000000 ) ;
#18204=ORIENTED_EDGE ( 'NONE', *, *, #9885, .F. ) ;
#18205=ORIENTED_EDGE ( 'NONE', *, *, #15383, .T. ) ;
#18211=ORIENTED_EDGE ( 'NONE', *, *, #32543, .F. ) ;
#18219=CYLINDRICAL_SURFACE ( 'NONE', #27923, 20.00000000000000355 ) ;
#18223=CARTESIAN_POINT ( 'NONE',  ( 7.999999999999992895, -11.46872990052349550, -45.56340405422456996 ) ) ;
#18224=DIRECTION ( 'NONE',  ( -1.000000000000000000, -0.000000000000000000, -0.000000000000000000 ) ) ;
#18232=EDGE_CURVE ( 'NONE', #15796, #14501, #13695, .T. ) ;
#18242=ORIENTED_EDGE ( 'NONE', *, *, #32147, .F. ) ;
#18246=CARTESIAN_POINT ( 'NONE',  ( 0.000000000000000000, 0.000000000000000000, 0.000000000000000000 ) ) ;
#18250=AXIS2_PLACEMENT_3D ( 'NONE', #3666, #19311, #27799 ) ;
#18255=CIRCLE ( 'NONE', #2775, 52.00000000000000711 ) ;
#18265=DIRECTION ( 'NONE',  ( -1.000000000000000000, 0.000000000000000000, -0.000000000000000000 ) ) ;
#18266=AXIS2_PLACEMENT_3D ( 'NONE', #16213, #24530, #18757 ) ;
#18271=DIRECTION ( 'NONE',  ( 0.000000000000000000, -0.7705132427757817037, -0.6374239897486988493 ) ) ;
#18273=ORIENTED_EDGE ( 'NONE', *, *, #1824, .F. ) ;
#18275=AXIS2_PLACEMENT_3D ( 'NONE', #23403, #15277, #10071 ) ;
#18286=EDGE_LOOP ( 'NONE', ( #4711, #16005, #4013, #4000 ) ) ;
#18292=DIRECTION ( 'NONE',  ( 1.000000000000000000, 0.000000000000000000, 0.000000000000000000 ) ) ;
#18293=ORIENTED_EDGE ( 'NONE', *, *, #2737, .F. ) ;
#18306=CARTESIAN_POINT ( 'NONE',  ( 0.000000000000000000, 11.90021268425554624, 45.45261810511217959 ) ) ;
#18323=EDGE_CURVE ( 'NONE', #8621, #32451, #28680, .T. ) ;
#18324=CARTESIAN_POINT ( 'NONE',  ( -9.999999999999994671, 0.000000000000000000, 0.000000000000000000 ) ) ;
#18326=ORIENTED_EDGE ( 'NONE', *, *, #22451, .T. ) ;
#18331=CIRCLE ( 'NONE', #23494, 47.49900000000000944 ) ;
#18336=CIRCLE ( 'NONE', #35600, 47.49900000000000944 ) ;
#18337=FACE_OUTER_BOUND ( 'NONE', #13604, .T. ) ;
#18338=CYLINDRICAL_SURFACE ( 'NONE', #13118, 20.00000000000000355 ) ;
#18342=ORIENTED_EDGE ( 'NONE', *, *, #3146, .T. ) ;
#18347=CYLINDRICAL_SURFACE ( 'NONE', #6301, 52.00000000000000711 ) ;
#18348=EDGE_CURVE ( 'NONE', #25018, #10010, #20007, .T. ) ;
#18350=EDGE_CURVE ( 'NONE', #21046, #19596, #15680, .T. ) ;
#18359=DIRECTION ( 'NONE',  ( 0.000000000000000000, 0.6845471059286846183, 0.7289686274214153272 ) ) ;
#18360=ORIENTED_EDGE ( 'NONE', *, *, #3374, .T. ) ;
#18362=DIRECTION ( 'NONE',  ( -1.000000000000000000, -0.000000000000000000, 0.000000000000000000 ) ) ;
#18367=ADVANCED_FACE ( 'NONE', ( #26698 ), #15017, .T. ) ;
#18369=ADVANCED_FACE ( 'NONE', ( #19098 ), #21615, .T. ) ;
#18373=DIRECTION ( 'NONE',  ( 0.000000000000000000, -0.9048270524660235736, 0.4257792915650641663 ) ) ;
#18388=AXIS2_PLACEMENT_3D ( 'NONE', #25327, #33589, #6234 ) ;
#18390=ORIENTED_EDGE ( 'NONE', *, *, #29324, .T. ) ;
#18391=VERTEX_POINT ( 'NONE', #27227 ) ;
#18392=CIRCLE ( 'NONE', #22412, 52.00000000000000711 ) ;
#18402=ORIENTED_EDGE ( 'NONE', *, *, #30173, .F. ) ;
#18407=ORIENTED_EDGE ( 'NONE', *, *, #4026, .F. ) ;
#18425=ORIENTED_EDGE ( 'NONE', *, *, #27515, .F. ) ;
#18427=AXIS2_PLACEMENT_3D ( 'NONE', #6967, #2134, #17764 ) ;
#18441=DIRECTION ( 'NONE',  ( -1.000000000000000000, -0.000000000000000000, 0.000000000000000000 ) ) ;
#18442=ORIENTED_EDGE ( 'NONE', *, *, #3561, .T. ) ;
#18453=CARTESIAN_POINT ( 'NONE',  ( 7.999999999999992895, -47.00885577955408223, -6.806061952192771436 ) ) ;
#18464=EDGE_LOOP ( 'NONE', ( #24634, #19111, #24198, #25035 ) ) ;
#18465=AXIS2_PLACEMENT_3D ( 'NONE', #8838, #17115, #28121 ) ;
#18474=ORIENTED_EDGE ( 'NONE', *, *, #23274, .T. ) ;
#18476=EDGE_CURVE ( 'NONE', #12864, #26214, #35016, .T. ) ;
#18478=DIRECTION ( 'NONE',  ( -1.000000000000000000, 0.000000000000000000, 0.000000000000000000 ) ) ;
#18479=EDGE_CURVE ( 'NONE', #27299, #11684, #22900, .T. ) ;
#18480=EDGE_CURVE ( 'NONE', #33000, #29366, #32796, .T. ) ;
#18492=CYLINDRICAL_SURFACE ( 'NONE', #29377, 20.00000000000000355 ) ;
#18495=LINE ( 'NONE', #1952, #10139 ) ;
#18496=CARTESIAN_POINT ( 'NONE',  ( 0.000000000000000000, 30.03615769709793426, -42.44795908868959344 ) ) ;
#18497=VERTEX_POINT ( 'NONE', #16577 ) ;
#18502=ORIENTED_EDGE ( 'NONE', *, *, #8430, .F. ) ;
#18504=DIRECTION ( 'NONE',  ( -1.000000000000000000, -0.000000000000000000, 0.000000000000000000 ) ) ;
#18508=EDGE_CURVE ( 'NONE', #4978, #4101, #10840, .T. ) ;
#18509=DIRECTION ( 'NONE',  ( 0.000000000000000000, -0.9510565162951565288, 0.3090169943749382919 ) ) ;
#18513=AXIS2_PLACEMENT_3D ( 'NONE', #27491, #2833, #33058 ) ;
#18515=DIRECTION ( 'NONE',  ( 0.000000000000000000, 0.000000000000000000, 1.000000000000000000 ) ) ;
#18523=CARTESIAN_POINT ( 'NONE',  ( 0.000000000000000000, -0.6505223195686569149, 51.99593080916758936 ) ) ;
#18535=DIRECTION ( 'NONE',  ( 0.000000000000000000, 0.000000000000000000, 1.000000000000000000 ) ) ;
#18540=VECTOR ( 'NONE', #2570, 1000.000000000000000 ) ;
#18542=ORIENTED_EDGE ( 'NONE', *, *, #35040, .F. ) ;
#18544=AXIS2_PLACEMENT_3D ( 'NONE', #27262, #5306, #3442 ) ;
#18559=EDGE_CURVE ( 'NONE', #3119, #403, #27482, .T. ) ;
#18560=ORIENTED_EDGE ( 'NONE', *, *, #21550, .F. ) ;
#18568=EDGE_CURVE ( 'NONE', #25018, #892, #17451, .T. ) ;
#18588=CARTESIAN_POINT ( 'NONE',  ( 7.999999999999992895, -47.49120266317495975, -0.8606222198180163430 ) ) ;
#18601=ORIENTED_EDGE ( 'NONE', *, *, #4997, .T. ) ;
#18604=FACE_OUTER_BOUND ( 'NONE', #7575, .T. ) ;
#18607=EDGE_LOOP ( 'NONE', ( #9188, #29246, #21789, #1008 ) ) ;
#18614=VECTOR ( 'NONE', #17724, 1000.000000000000000 ) ;
#18626=CARTESIAN_POINT ( 'NONE',  ( 7.999999999999992895, -29.60891106212813995, 37.14118181634756866 ) ) ;
#18628=CYLINDRICAL_SURFACE ( 'NONE', #7624, 52.00000000000000711 ) ;
#18629=CARTESIAN_POINT ( 'NONE',  ( 7.999999999999992895, 0.000000000000000000, 0.000000000000000000 ) ) ;
#18631=DIRECTION ( 'NONE',  ( -1.000000000000000000, 0.000000000000000000, 0.000000000000000000 ) ) ;
#18635=ORIENTED_EDGE ( 'NONE', *, *, #3294, .T. ) ;
#18638=ADVANCED_FACE ( 'NONE', ( #25226 ), #30792, .T. ) ;
#18650=DIRECTION ( 'NONE',  ( -1.000000000000000000, 0.000000000000000000, -0.000000000000000000 ) ) ;
#18656=DIRECTION ( 'NONE',  ( 0.000000000000000000, -0.8443279255020201823, 0.5358267949789887741 ) ) ;
#18662=FACE_OUTER_BOUND ( 'NONE', #8452, .T. ) ;
#18663=CIRCLE ( 'NONE', #4891, 47.49900000000001654 ) ;
#18666=DIRECTION ( 'NONE',  ( -1.000000000000000000, 0.000000000000000000, -0.000000000000000000 ) ) ;
#18684=CARTESIAN_POINT ( 'NONE',  ( 7.999999999999992895, 0.000000000000000000, 0.000000000000000000 ) ) ;
#18690=ORIENTED_EDGE ( 'NONE', *, *, #6564, .F. ) ;
#18697=DIRECTION ( 'NONE',  ( 0.000000000000000000, 0.000000000000000000, 1.000000000000000000 ) ) ;
#18705=ADVANCED_FACE ( 'NONE', ( #14045 ), #11363, .T. ) ;
#18712=ORIENTED_EDGE ( 'NONE', *, *, #28412, .F. ) ;
#18720=CARTESIAN_POINT ( 'NONE',  ( 0.000000000000000000, -22.82995208772716467, 41.06517797613655318 ) ) ;
#18726=CIRCLE ( 'NONE', #3220, 52.00000000000000711 ) ;
#18731=DIRECTION ( 'NONE',  ( -1.000000000000000000, 0.000000000000000000, -0.000000000000000000 ) ) ;
#18734=CARTESIAN_POINT ( 'NONE',  ( 7.999999999999992895, 44.25018368420782622, -27.31155879685134735 ) ) ;
#18736=EDGE_LOOP ( 'NONE', ( #35182, #17252, #14348, #3690 ) ) ;
#18745=DIRECTION ( 'NONE',  ( -1.000000000000000000, 0.000000000000000000, 0.000000000000000000 ) ) ;
#18748=AXIS2_PLACEMENT_3D ( 'NONE', #6907, #4227, #12679 ) ;
#18749=ADVANCED_FACE ( 'NONE', ( #34401 ), #12419, .T. ) ;
#18751=AXIS2_PLACEMENT_3D ( 'NONE', #10406, #9686, #4664 ) ;
#18756=EDGE_CURVE ( 'NONE', #32280, #4250, #28650, .T. ) ;
#18757=DIRECTION ( 'NONE',  ( 0.000000000000000000, 0.000000000000000000, 1.000000000000000000 ) ) ;
#18759=CARTESIAN_POINT ( 'NONE',  ( 0.000000000000000000, 51.93417535146742381, -2.615612846549375536 ) ) ;
#18765=CARTESIAN_POINT ( 'NONE',  ( 7.999999999999992895, 27.43636312076321104, 38.14186064215159888 ) ) ;
#18781=CARTESIAN_POINT ( 'NONE',  ( -9.999999999999994671, 0.000000000000000000, 0.000000000000000000 ) ) ;
#18793=LINE ( 'NONE', #32304, #22815 ) ;
#18795=AXIS2_PLACEMENT_3D ( 'NONE', #16844, #27848, #3191 ) ;
#18801=DIRECTION ( 'NONE',  ( -1.000000000000000000, 0.000000000000000000, 0.000000000000000000 ) ) ;
#18806=CARTESIAN_POINT ( 'NONE',  ( 7.999999999999992895, 0.000000000000000000, 0.000000000000000000 ) ) ;
#18811=FACE_OUTER_BOUND ( 'NONE', #13211, .T. ) ;
#18820=AXIS2_PLACEMENT_3D ( 'NONE', #3096, #369, #22332 ) ;
#18821=DIRECTION ( 'NONE',  ( 0.000000000000000000, 0.000000000000000000, 1.000000000000000000 ) ) ;
#18822=DIRECTION ( 'NONE',  ( 0.000000000000000000, 0.000000000000000000, 1.000000000000000000 ) ) ;
#18828=ORIENTED_EDGE ( 'NONE', *, *, #20973, .T. ) ;
#18833=DIRECTION ( 'NONE',  ( 0.000000000000000000, 0.000000000000000000, -1.000000000000000000 ) ) ;
#18836=CARTESIAN_POINT ( 'NONE',  ( 7.999999999999992895, 0.000000000000000000, 0.000000000000000000 ) ) ;
#18843=AXIS2_PLACEMENT_3D ( 'NONE', #22673, #25584, #9185 ) ;
#18852=FACE_OUTER_BOUND ( 'NONE', #9430, .T. ) ;
#18863=DIRECTION ( 'NONE',  ( 0.000000000000000000, -0.7705132427757949154, 0.6374239897486827511 ) ) ;
#18866=ORIENTED_EDGE ( 'NONE', *, *, #6321, .T. ) ;
#18867=CARTESIAN_POINT ( 'NONE',  ( 7.999999999999992895, -11.46872990052412611, 45.56340405422440654 ) ) ;
#18878=VERTEX_POINT ( 'NONE', #14753 ) ;
#18889=DIRECTION ( 'NONE',  ( -1.000000000000000000, 0.000000000000000000, 0.000000000000000000 ) ) ;
#18891=CARTESIAN_POINT ( 'NONE',  ( 4.000000000000003553, -30.03615769709705319, -42.44795908869020451 ) ) ;
#18897=ORIENTED_EDGE ( 'NONE', *, *, #6800, .F. ) ;
#18904=ORIENTED_EDGE ( 'NONE', *, *, #10156, .T. ) ;
#18910=CARTESIAN_POINT ( 'NONE',  ( 0.000000000000000000, 12.30077720129095553, 50.52416135122086871 ) ) ;
#18915=DIRECTION ( 'NONE',  ( 0.000000000000000000, 0.000000000000000000, -1.000000000000000000 ) ) ;
#18925=DIRECTION ( 'NONE',  ( -1.000000000000000000, -0.000000000000000000, -0.000000000000000000 ) ) ;
#18926=CYLINDRICAL_SURFACE ( 'NONE', #8177, 47.49900000000001654 ) ;
#18933=ORIENTED_EDGE ( 'NONE', *, *, #10237, .T. ) ;
#18937=CARTESIAN_POINT ( 'NONE',  ( 4.000000000000003553, 12.30077720129168384, -50.52416135122070528 ) ) ;
#18938=ADVANCED_FACE ( 'NONE', ( #2352 ), #32222, .T. ) ;
#18941=ORIENTED_EDGE ( 'NONE', *, *, #35277, .F. ) ;
#18946=LINE ( 'NONE', #26719, #24570 ) ;
#18957=EDGE_CURVE ( 'NONE', #29894, #3630, #29699, .T. ) ;
#18961=VERTEX_POINT ( 'NONE', #30056 ) ;
#18975=LINE ( 'NONE', #16077, #6519 ) ;
#18984=FACE_OUTER_BOUND ( 'NONE', #14419, .T. ) ;
#18989=FACE_OUTER_BOUND ( 'NONE', #21608, .T. ) ;
#18994=ORIENTED_EDGE ( 'NONE', *, *, #13509, .F. ) ;
#18999=VERTEX_POINT ( 'NONE', #21226 ) ;
#19002=EDGE_CURVE ( 'NONE', #31360, #5795, #5121, .T. ) ;
#19011=VECTOR ( 'NONE', #25572, 1000.000000000000000 ) ;
#19013=ORIENTED_EDGE ( 'NONE', *, *, #22731, .F. ) ;
#19017=DIRECTION ( 'NONE',  ( -1.000000000000000000, 0.000000000000000000, 0.000000000000000000 ) ) ;
#19020=DIRECTION ( 'NONE',  ( -1.000000000000000000, -0.000000000000000000, 0.000000000000000000 ) ) ;
#19032=CARTESIAN_POINT ( 'NONE',  ( 0.000000000000000000, -12.30077720129063756, -50.52416135122095397 ) ) ;
#19035=VERTEX_POINT ( 'NONE', #12728 ) ;
#19039=ORIENTED_EDGE ( 'NONE', *, *, #32878, .F. ) ;
#19042=DIRECTION ( 'NONE',  ( -1.000000000000000000, 0.000000000000000000, 0.000000000000000000 ) ) ;
#19047=VERTEX_POINT ( 'NONE', #15400 ) ;
#19051=AXIS2_PLACEMENT_3D ( 'NONE', #27937, #25424, #16763 ) ;
#19053=CIRCLE ( 'NONE', #33419, 52.00000000000000711 ) ;
#19059=LINE ( 'NONE', #15460, #189 ) ;
#19064=DIRECTION ( 'NONE',  ( -1.000000000000000000, 0.000000000000000000, 0.000000000000000000 ) ) ;
#19065=CYLINDRICAL_SURFACE ( 'NONE', #31969, 20.00000000000000355 ) ;
#19066=CARTESIAN_POINT ( 'NONE',  ( 0.000000000000000000, 0.000000000000000000, 0.000000000000000000 ) ) ;
#19068=LINE ( 'NONE', #30762, #33667 ) ;
#19084=ORIENTED_EDGE ( 'NONE', *, *, #8066, .F. ) ;
#19085=ORIENTED_EDGE ( 'NONE', *, *, #25553, .F. ) ;
#19086=CYLINDRICAL_SURFACE ( 'NONE', #16530, 52.00000000000000711 ) ;
#19092=EDGE_CURVE ( 'NONE', #26596, #11196, #12359, .T. ) ;
#19094=VERTEX_POINT ( 'NONE', #18106 ) ;
#19098=FACE_OUTER_BOUND ( 'NONE', #28490, .T. ) ;
#19111=ORIENTED_EDGE ( 'NONE', *, *, #20653, .T. ) ;
#19113=CARTESIAN_POINT ( 'NONE',  ( 7.999999999999992895, 5.871425383721554425, 51.66745943012285380 ) ) ;
#19121=EDGE_CURVE ( 'NONE', #10004, #20300, #15045, .T. ) ;
#19123=AXIS2_PLACEMENT_3D ( 'NONE', #12421, #34575, #900 ) ;
#19126=EDGE_CURVE ( 'NONE', #14743, #4610, #20598, .T. ) ;
#19132=DIRECTION ( 'NONE',  ( -1.000000000000000000, 0.000000000000000000, 0.000000000000000000 ) ) ;
#19133=EDGE_CURVE ( 'NONE', #9066, #11629, #4461, .T. ) ;
#19136=LINE ( 'NONE', #17090, #24316 ) ;
#19137=AXIS2_PLACEMENT_3D ( 'NONE', #18160, #29523, #21030 ) ;
#19146=AXIS2_PLACEMENT_3D ( 'NONE', #17287, #16926, #732 ) ;
#19148=DIRECTION ( 'NONE',  ( -1.000000000000000000, -0.000000000000000000, 0.000000000000000000 ) ) ;
#19149=ORIENTED_EDGE ( 'NONE', *, *, #33446, .T. ) ;
#19151=DIRECTION ( 'NONE',  ( 0.000000000000000000, 0.000000000000000000, 1.000000000000000000 ) ) ;
#19157=DIRECTION ( 'NONE',  ( -1.000000000000000000, 0.000000000000000000, 0.000000000000000000 ) ) ;
#19158=CYLINDRICAL_SURFACE ( 'NONE', #34249, 52.00000000000000711 ) ;
#19163=CYLINDRICAL_SURFACE ( 'NONE', #4989, 52.00000000000000711 ) ;
#19168=CARTESIAN_POINT ( 'NONE',  ( 0.000000000000000000, 0.000000000000000000, 0.000000000000000000 ) ) ;
#19174=ORIENTED_EDGE ( 'NONE', *, *, #32878, .T. ) ;
#19179=AXIS2_PLACEMENT_3D ( 'NONE', #11679, #3244, #22837 ) ;
#19192=CARTESIAN_POINT ( 'NONE',  ( 7.999999999999992895, -24.72041153920761758, 40.55929306992680949 ) ) ;
#19200=ORIENTED_EDGE ( 'NONE', *, *, #35497, .F. ) ;
#19202=CYLINDRICAL_SURFACE ( 'NONE', #8327, 11.00000000000000000 ) ;
#19204=CARTESIAN_POINT ( 'NONE',  ( 0.000000000000000000, 0.000000000000000000, 0.000000000000000000 ) ) ;
#19207=CARTESIAN_POINT ( 'NONE',  ( 4.000000000000003553, -36.06787431788704623, 37.45808914225476371 ) ) ;
#19210=ORIENTED_EDGE ( 'NONE', *, *, #5609, .F. ) ;
#19217=AXIS2_PLACEMENT_3D ( 'NONE', #9657, #20790, #31087 ) ;
#19223=CIRCLE ( 'NONE', #3723, 47.49900000000000944 ) ;
#19231=CYLINDRICAL_SURFACE ( 'NONE', #31618, 52.00000000000000711 ) ;
#19233=DIRECTION ( 'NONE',  ( -1.000000000000000000, 0.000000000000000000, -0.000000000000000000 ) ) ;
#19234=FACE_OUTER_BOUND ( 'NONE', #348, .T. ) ;
#19242=VERTEX_POINT ( 'NONE', #5343 ) ;
#19243=ORIENTED_EDGE ( 'NONE', *, *, #25928, .T. ) ;
#19245=CARTESIAN_POINT ( 'NONE',  ( 7.999999999999992895, 17.50309955389674954, -43.60271849949345579 ) ) ;
#19256=CARTESIAN_POINT ( 'NONE',  ( 7.999999999999992895, 2.123073309835863842, -47.45152853935333326 ) ) ;
#19266=CIRCLE ( 'NONE', #7760, 20.00000000000000000 ) ;
#19270=DIRECTION ( 'NONE',  ( 1.000000000000000000, -0.000000000000000000, -0.000000000000000000 ) ) ;
#19279=ORIENTED_EDGE ( 'NONE', *, *, #35310, .T. ) ;
#19297=CIRCLE ( 'NONE', #27374, 20.00000000000000711 ) ;
#19302=AXIS2_PLACEMENT_3D ( 'NONE', #17245, #17778, #28251 ) ;
#19306=DIRECTION ( 'NONE',  ( -1.000000000000000000, 0.000000000000000000, 0.000000000000000000 ) ) ;
#19311=DIRECTION ( 'NONE',  ( -1.000000000000000000, -0.000000000000000000, 0.000000000000000000 ) ) ;
#19314=CARTESIAN_POINT ( 'NONE',  ( 7.999999999999992895, 0.000000000000000000, 0.000000000000000000 ) ) ;
#19317=AXIS2_PLACEMENT_3D ( 'NONE', #21991, #10672, #8496 ) ;
#19329=VECTOR ( 'NONE', #33039, 1000.000000000000000 ) ;
#19331=DIRECTION ( 'NONE',  ( -1.000000000000000000, 0.000000000000000000, 0.000000000000000000 ) ) ;
#19337=DIRECTION ( 'NONE',  ( -1.000000000000000000, -0.000000000000000000, -0.000000000000000000 ) ) ;
#19340=DIRECTION ( 'NONE',  ( -1.000000000000000000, 0.000000000000000000, 0.000000000000000000 ) ) ;
#19341=ORIENTED_EDGE ( 'NONE', *, *, #10593, .F. ) ;
#19343=ORIENTED_EDGE ( 'NONE', *, *, #18350, .T. ) ;
#19349=AXIS2_PLACEMENT_3D ( 'NONE', #17289, #22517, #34049 ) ;
#19356=LINE ( 'NONE', #33060, #21820 ) ;
#19357=CIRCLE ( 'NONE', #31418, 47.49900000000001654 ) ;
#19363=EDGE_CURVE ( 'NONE', #423, #17460, #22937, .T. ) ;
#19366=ADVANCED_FACE ( 'NONE', ( #33934 ), #11604, .T. ) ;
#19373=VECTOR ( 'NONE', #15903, 1000.000000000000000 ) ;
#19377=EDGE_CURVE ( 'NONE', #17248, #7480, #14125, .T. ) ;
#19379=DIRECTION ( 'NONE',  ( 0.000000000000000000, 0.000000000000000000, 1.000000000000000000 ) ) ;
#19381=CIRCLE ( 'NONE', #5040, 20.00000000000000355 ) ;
#19383=EDGE_CURVE ( 'NONE', #6413, #15079, #33853, .T. ) ;
#19384=ORIENTED_EDGE ( 'NONE', *, *, #31450, .F. ) ;
#19387=AXIS2_PLACEMENT_3D ( 'NONE', #8804, #27388, #16729 ) ;
#19390=VERTEX_POINT ( 'NONE', #13959 ) ;
#19401=CIRCLE ( 'NONE', #2202, 52.00000000000000711 ) ;
#19402=EDGE_CURVE ( 'NONE', #3377, #32945, #6212, .T. ) ;
#19406=EDGE_CURVE ( 'NONE', #16080, #25525, #18331, .T. ) ;
#19407=ORIENTED_EDGE ( 'NONE', *, *, #6529, .F. ) ;
#19410=VECTOR ( 'NONE', #14912, 1000.000000000000000 ) ;
#19423=CYLINDRICAL_SURFACE ( 'NONE', #30213, 47.49900000000001654 ) ;
#19424=DIRECTION ( 'NONE',  ( 1.000000000000000000, -0.000000000000000000, -0.000000000000000000 ) ) ;
#19427=DIRECTION ( 'NONE',  ( -1.000000000000000000, -0.000000000000000000, 0.000000000000000000 ) ) ;
#19428=ORIENTED_EDGE ( 'NONE', *, *, #107, .F. ) ;
#19437=CARTESIAN_POINT ( 'NONE',  ( 7.999999999999992895, 9.744342220503382279, 46.48873837489803407 ) ) ;
#19439=VERTEX_POINT ( 'NONE', #9086 ) ;
#19440=AXIS2_PLACEMENT_3D ( 'NONE', #15401, #4279, #27084 ) ;
#19442=DIRECTION ( 'NONE',  ( 1.000000000000000000, 0.000000000000000000, -0.000000000000000000 ) ) ;
#19445=DIRECTION ( 'NONE',  ( -1.000000000000000000, -0.000000000000000000, 0.000000000000000000 ) ) ;
#19453=ORIENTED_EDGE ( 'NONE', *, *, #16705, .T. ) ;
#19465=AXIS2_PLACEMENT_3D ( 'NONE', #7092, #12502, #34292 ) ;
#19467=VERTEX_POINT ( 'NONE', #32170 ) ;
#19471=VERTEX_POINT ( 'NONE', #12196 ) ;
#19473=ORIENTED_EDGE ( 'NONE', *, *, #10240, .T. ) ;
#19477=CARTESIAN_POINT ( 'NONE',  ( 7.999999999999992895, 0.000000000000000000, 0.000000000000000000 ) ) ;
#19478=VERTEX_POINT ( 'NONE', #23528 ) ;
#19479=CARTESIAN_POINT ( 'NONE',  ( 7.999999999999992895, 47.49120266317496686, 0.8606222198176832761 ) ) ;
#19482=VERTEX_POINT ( 'NONE', #12554 ) ;
#19484=VECTOR ( 'NONE', #33230, 1000.000000000000000 ) ;
#19487=ORIENTED_EDGE ( 'NONE', *, *, #5094, .T. ) ;
#19513=ORIENTED_EDGE ( 'NONE', *, *, #27912, .F. ) ;
#19515=FACE_OUTER_BOUND ( 'NONE', #21057, .T. ) ;
#19529=DIRECTION ( 'NONE',  ( -1.000000000000000000, -0.000000000000000000, -0.000000000000000000 ) ) ;
#19530=DIRECTION ( 'NONE',  ( -1.000000000000000000, 0.000000000000000000, 0.000000000000000000 ) ) ;
#19532=DIRECTION ( 'NONE',  ( -1.000000000000000000, -0.000000000000000000, 0.000000000000000000 ) ) ;
#19548=ORIENTED_EDGE ( 'NONE', *, *, #11056, .T. ) ;
#19552=ORIENTED_EDGE ( 'NONE', *, *, #32795, .F. ) ;
#19555=VECTOR ( 'NONE', #30257, 1000.000000000000000 ) ;
#19557=CARTESIAN_POINT ( 'NONE',  ( 7.999999999999992895, -46.19362259308826424, -8.585149169758999221 ) ) ;
#19560=EDGE_CURVE ( 'NONE', #34584, #17460, #27578, .T. ) ;
#19563=ORIENTED_EDGE ( 'NONE', *, *, #10563, .T. ) ;
#19572=DIRECTION ( 'NONE',  ( 0.000000000000000000, 0.000000000000000000, 1.000000000000000000 ) ) ;
#19576=VECTOR ( 'NONE', #24334, 1000.000000000000000 ) ;
#19578=DIRECTION ( 'NONE',  ( -1.000000000000000000, -0.000000000000000000, -0.000000000000000000 ) ) ;
#19584=CARTESIAN_POINT ( 'NONE',  ( 0.000000000000000000, 0.000000000000000000, 11.00000000000000000 ) ) ;
#19587=DIRECTION ( 'NONE',  ( -1.000000000000000000, 0.000000000000000000, -0.000000000000000000 ) ) ;
#19588=ADVANCED_FACE ( 'NONE', ( #4286 ), #15226, .T. ) ;
#19591=ORIENTED_EDGE ( 'NONE', *, *, #11371, .T. ) ;
#19596=VERTEX_POINT ( 'NONE', #20445 ) ;
#19600=ORIENTED_EDGE ( 'NONE', *, *, #25166, .F. ) ;
#19604=EDGE_CURVE ( 'NONE', #30986, #1640, #4991, .T. ) ;
#19615=DIRECTION ( 'NONE',  ( -1.000000000000000000, 0.000000000000000000, 0.000000000000000000 ) ) ;
#19623=VERTEX_POINT ( 'NONE', #16119 ) ;
#19624=AXIS2_PLACEMENT_3D ( 'NONE', #26693, #31893, #9931 ) ;
#19635=ORIENTED_EDGE ( 'NONE', *, *, #6021, .T. ) ;
#19637=VERTEX_POINT ( 'NONE', #35413 ) ;
#19638=AXIS2_PLACEMENT_3D ( 'NONE', #5232, #8082, #18359 ) ;
#19642=ORIENTED_EDGE ( 'NONE', *, *, #8200, .T. ) ;
#19645=ADVANCED_FACE ( 'NONE', ( #32706 ), #13795, .T. ) ;
#19651=ORIENTED_EDGE ( 'NONE', *, *, #7348, .T. ) ;
#19653=FACE_OUTER_BOUND ( 'NONE', #9577, .T. ) ;
#19655=CARTESIAN_POINT ( 'NONE',  ( 0.000000000000000000, 0.000000000000000000, 0.000000000000000000 ) ) ;
#19663=CARTESIAN_POINT ( 'NONE',  ( 7.999999999999992895, 0.000000000000000000, 0.000000000000000000 ) ) ;
#19664=DIRECTION ( 'NONE',  ( 0.000000000000000000, 0.000000000000000000, -1.000000000000000000 ) ) ;
#19667=ORIENTED_EDGE ( 'NONE', *, *, #8110, .T. ) ;
#19668=DIRECTION ( 'NONE',  ( 1.000000000000000000, -0.000000000000000000, -0.000000000000000000 ) ) ;
#19680=CARTESIAN_POINT ( 'NONE',  ( 7.999999999999992895, -44.75336757549789013, 14.30704879393590545 ) ) ;
#19684=VECTOR ( 'NONE', #12840, 1000.000000000000000 ) ;
#19692=AXIS2_PLACEMENT_3D ( 'NONE', #20509, #3983, #14927 ) ;
#19693=CARTESIAN_POINT ( 'NONE',  ( 7.999999999999992895, 35.20873326984081331, 31.88259874184044662 ) ) ;
#19697=CARTESIAN_POINT ( 'NONE',  ( 0.000000000000000000, 42.60732521687570795, 19.80331771201672453 ) ) ;
#19715=ORIENTED_EDGE ( 'NONE', *, *, #26955, .T. ) ;
#19720=AXIS2_PLACEMENT_3D ( 'NONE', #31289, #14708, #15062 ) ;
#19725=DIRECTION ( 'NONE',  ( -1.000000000000000000, -0.000000000000000000, -0.000000000000000000 ) ) ;
#19728=VERTEX_POINT ( 'NONE', #30013 ) ;
#19742=CARTESIAN_POINT ( 'NONE',  ( 0.000000000000000000, 0.000000000000000000, 0.000000000000000000 ) ) ;
#19744=CARTESIAN_POINT ( 'NONE',  ( 7.999999999999992895, 36.34385289850631295, -29.77717097092039111 ) ) ;
#19749=ORIENTED_EDGE ( 'NONE', *, *, #35217, .T. ) ;
#19766=AXIS2_PLACEMENT_3D ( 'NONE', #10702, #27273, #16622 ) ;
#19771=ORIENTED_EDGE ( 'NONE', *, *, #28656, .F. ) ;
#19777=EDGE_CURVE ( 'NONE', #574, #23561, #15458, .T. ) ;
#19785=CARTESIAN_POINT ( 'NONE',  ( 7.999999999999992895, -13.85708833600001277, 45.43276465116660745 ) ) ;
#19786=CIRCLE ( 'NONE', #29607, 20.00000000000000711 ) ;
#19787=ADVANCED_FACE ( 'NONE', ( #24784 ), #9093, .T. ) ;
#19790=EDGE_CURVE ( 'NONE', #5839, #9669, #10324, .T. ) ;
#19795=VECTOR ( 'NONE', #6765, 1000.000000000000000 ) ;
#19796=ORIENTED_EDGE ( 'NONE', *, *, #13656, .F. ) ;
#19800=DIRECTION ( 'NONE',  ( 0.000000000000000000, 0.9980267284282713369, 0.06279051952931692659 ) ) ;
#19804=DIRECTION ( 'NONE',  ( 1.000000000000000000, 0.000000000000000000, -0.000000000000000000 ) ) ;
#19806=AXIS2_PLACEMENT_3D ( 'NONE', #34624, #9944, #26528 ) ;
#19814=CYLINDRICAL_SURFACE ( 'NONE', #27378, 47.49900000000001654 ) ;
#19815=ORIENTED_EDGE ( 'NONE', *, *, #29832, .F. ) ;
#19823=EDGE_CURVE ( 'NONE', #10826, #12629, #3005, .T. ) ;
#19825=AXIS2_PLACEMENT_3D ( 'NONE', #19557, #13653, #30735 ) ;
#19830=ADVANCED_FACE ( 'NONE', ( #804 ), #25487, .T. ) ;
#19835=CARTESIAN_POINT ( 'NONE',  ( 0.000000000000000000, 0.000000000000000000, 0.000000000000000000 ) ) ;
#19840=CARTESIAN_POINT ( 'NONE',  ( 4.000000000000003553, 46.77034588191304465, 22.72740077717247331 ) ) ;
#19849=AXIS2_PLACEMENT_3D ( 'NONE', #27632, #6005, #22910 ) ;
#19857=EDGE_LOOP ( 'NONE', ( #19932, #14199, #32542, #22099 ) ) ;
#19865=EDGE_CURVE ( 'NONE', #27467, #34112, #19356, .T. ) ;
#19866=CIRCLE ( 'NONE', #34269, 52.00000000000000711 ) ;
#19867=DIRECTION ( 'NONE',  ( -1.000000000000000000, 0.000000000000000000, 0.000000000000000000 ) ) ;
#19874=CIRCLE ( 'NONE', #6663, 20.00000000000000355 ) ;
#19882=AXIS2_PLACEMENT_3D ( 'NONE', #17369, #28371, #5874 ) ;
#19883=CARTESIAN_POINT ( 'NONE',  ( 7.999999999999992895, -15.49408907645203470, 44.90087086784588877 ) ) ;
#19885=CARTESIAN_POINT ( 'NONE',  ( -9.999999999999994671, 0.000000000000000000, 0.000000000000000000 ) ) ;
#19889=CARTESIAN_POINT ( 'NONE',  ( 4.000000000000003553, -35.11945359308084846, -38.34871548466050939 ) ) ;
#19891=ORIENTED_EDGE ( 'NONE', *, *, #26825, .T. ) ;
#19900=AXIS2_PLACEMENT_3D ( 'NONE', #25907, #23190, #3955 ) ;
#19901=DIRECTION ( 'NONE',  ( -1.000000000000000000, 0.000000000000000000, 0.000000000000000000 ) ) ;
#19903=DIRECTION ( 'NONE',  ( -1.000000000000000000, 0.000000000000000000, 0.000000000000000000 ) ) ;
#19919=CARTESIAN_POINT ( 'NONE',  ( 7.999999999999992895, 42.03146605346787368, 22.12489237027333289 ) ) ;
#19926=VECTOR ( 'NONE', #25253, 1000.000000000000000 ) ;
#19927=CARTESIAN_POINT ( 'NONE',  ( -9.999999999999994671, 0.000000000000000000, 0.000000000000000000 ) ) ;
#19928=DIRECTION ( 'NONE',  ( 0.000000000000000000, 0.4817536741017100499, 0.8763066800438663595 ) ) ;
#19929=ORIENTED_EDGE ( 'NONE', *, *, #3954, .T. ) ;
#19932=ORIENTED_EDGE ( 'NONE', *, *, #18559, .F. ) ;
#19939=ORIENTED_EDGE ( 'NONE', *, *, #26584, .T. ) ;
#19949=CIRCLE ( 'NONE', #33226, 52.00000000000000711 ) ;
#19950=CIRCLE ( 'NONE', #10199, 47.49900000000001654 ) ;
#19952=ORIENTED_EDGE ( 'NONE', *, *, #34596, .T. ) ;
#19955=AXIS2_PLACEMENT_3D ( 'NONE', #20172, #34063, #22890 ) ;
#19956=EDGE_CURVE ( 'NONE', #6860, #16883, #30881, .T. ) ;
#19960=AXIS2_PLACEMENT_3D ( 'NONE', #33385, #30350, #5683 ) ;
#19970=CARTESIAN_POINT ( 'NONE',  ( 7.999999999999992895, 39.78933988720114456, 24.98727647985016276 ) ) ;
#19979=AXIS2_PLACEMENT_3D ( 'NONE', #7532, #7173, #18509 ) ;
#19981=AXIS2_PLACEMENT_3D ( 'NONE', #25882, #19903, #15047 ) ;
#19982=DIRECTION ( 'NONE',  ( 0.000000000000000000, 0.9980267284282717810, -0.06279051952930990443 ) ) ;
#19983=VERTEX_POINT ( 'NONE', #20398 ) ;
#19987=ORIENTED_EDGE ( 'NONE', *, *, #19092, .F. ) ;
#19989=EDGE_CURVE ( 'NONE', #14995, #1331, #16649, .T. ) ;
#20006=DIRECTION ( 'NONE',  ( 0.000000000000000000, 0.000000000000000000, 1.000000000000000000 ) ) ;
#20007=CIRCLE ( 'NONE', #14286, 52.00000000000000711 ) ;
#20011=CARTESIAN_POINT ( 'NONE',  ( 7.999999999999992895, 32.32520163883631170, -34.09746168776000985 ) ) ;
#20021=CARTESIAN_POINT ( 'NONE',  ( 7.999999999999992895, 0.000000000000000000, 11.00000000000000000 ) ) ;
#20027=AXIS2_PLACEMENT_3D ( 'NONE', #27662, #9264, #33394 ) ;
#20031=DIRECTION ( 'NONE',  ( -1.000000000000000000, 0.000000000000000000, -0.000000000000000000 ) ) ;
#20035=CARTESIAN_POINT ( 'NONE',  ( 7.999999999999992895, 32.32520163883582853, 34.09746168776048592 ) ) ;
#20038=CARTESIAN_POINT ( 'NONE',  ( 7.999999999999992895, 25.61928775981044026, 45.25098998563487385 ) ) ;
#20040=VERTEX_POINT ( 'NONE', #6744 ) ;
#20045=DIRECTION ( 'NONE',  ( 1.000000000000000000, 0.000000000000000000, 0.000000000000000000 ) ) ;
#20047=EDGE_CURVE ( 'NONE', #8021, #27298, #15510, .T. ) ;
#20049=CARTESIAN_POINT ( 'NONE',  ( 0.000000000000000000, 0.000000000000000000, 0.000000000000000000 ) ) ;
#20058=UNCERTAINTY_MEASURE_WITH_UNIT (LENGTH_MEASURE( 1.000000000000000082E-05 ), #24441, 'distance_accuracy_value', 'NONE');
#20059=CARTESIAN_POINT ( 'NONE',  ( 7.999999999999992895, 0.000000000000000000, 0.000000000000000000 ) ) ;
#20060=ORIENTED_EDGE ( 'NONE', *, *, #19956, .T. ) ;
#20067=DIRECTION ( 'NONE',  ( 0.000000000000000000, 0.000000000000000000, 1.000000000000000000 ) ) ;
#20075=ORIENTED_EDGE ( 'NONE', *, *, #30871, .T. ) ;
#20076=EDGE_CURVE ( 'NONE', #27224, #4610, #23671, .T. ) ;
#20078=EDGE_CURVE ( 'NONE', #17645, #22530, #26020, .T. ) ;
#20080=VERTEX_POINT ( 'NONE', #6557 ) ;
#20083=VECTOR ( 'NONE', #22107, 1000.000000000000000 ) ;
#20084=LINE ( 'NONE', #658, #31934 ) ;
#20085=CARTESIAN_POINT ( 'NONE',  ( 0.000000000000000000, -35.20873326984057883, -31.88259874184068465 ) ) ;
#20088=DIRECTION ( 'NONE',  ( 0.000000000000000000, 0.2486898871648553222, -0.9685831611286309650 ) ) ;
#20089=EDGE_CURVE ( 'NONE', #19242, #31708, #23605, .T. ) ;
#20107=CARTESIAN_POINT ( 'NONE',  ( 7.999999999999992895, 36.34385289850589373, 29.77717097092089205 ) ) ;
#20112=LINE ( 'NONE', #10579, #2685 ) ;
#20113=VERTEX_POINT ( 'NONE', #25850 ) ;
#20123=CARTESIAN_POINT ( 'NONE',  ( 7.999999999999992895, -34.03046037009280411, 33.13733193845794034 ) ) ;
#20127=CARTESIAN_POINT ( 'NONE',  ( 7.999999999999992895, 8.053585752061906078, 46.81126742072027014 ) ) ;
#20132=CARTESIAN_POINT ( 'NONE',  ( 4.000000000000003553, -51.85248208264521708, 3.914090171286008335 ) ) ;
#20152=ORIENTED_EDGE ( 'NONE', *, *, #19092, .T. ) ;
#20155=EDGE_LOOP ( 'NONE', ( #26859, #27294, #18502, #8286 ) ) ;
#20157=VERTEX_POINT ( 'NONE', #13400 ) ;
#20158=CARTESIAN_POINT ( 'NONE',  ( 0.000000000000000000, 22.82995208772687334, 41.06517797613670950 ) ) ;
#20162=CYLINDRICAL_SURFACE ( 'NONE', #17889, 47.49900000000001654 ) ;
#20164=AXIS2_PLACEMENT_3D ( 'NONE', #386, #30640, #34054 ) ;
#20172=CARTESIAN_POINT ( 'NONE',  ( 0.000000000000000000, 0.000000000000000000, 0.000000000000000000 ) ) ;
#20174=DIRECTION ( 'NONE',  ( -1.000000000000000000, -0.000000000000000000, 0.000000000000000000 ) ) ;
#20184=CARTESIAN_POINT ( 'NONE',  ( 0.000000000000000000, 0.000000000000000000, 0.000000000000000000 ) ) ;
#20195=ORIENTED_EDGE ( 'NONE', *, *, #15044, .T. ) ;
#20209=VERTEX_POINT ( 'NONE', #21662 ) ;
#20214=AXIS2_PLACEMENT_3D ( 'NONE', #7496, #29477, #21516 ) ;
#20218=PRESENTATION_STYLE_ASSIGNMENT (( #23288 ) ) ;
#20220=EDGE_LOOP ( 'NONE', ( #23392, #10015, #11823, #16355 ) ) ;
#20231=CARTESIAN_POINT ( 'NONE',  ( 7.999999999999992895, 0.2227391519116599106, 46.98410307550729215 ) ) ;
#20240=DIRECTION ( 'NONE',  ( -1.000000000000000000, -0.000000000000000000, -0.000000000000000000 ) ) ;
#20241=ADVANCED_FACE ( 'NONE', ( #13054 ), #24041, .T. ) ;
#20249=CARTESIAN_POINT ( 'NONE',  ( 7.999999999999992895, 46.21320724403649649, 10.97699764141971102 ) ) ;
#20250=ORIENTED_EDGE ( 'NONE', *, *, #22938, .F. ) ;
#20259=EDGE_CURVE ( 'NONE', #8283, #14579, #24174, .T. ) ;
#20263=DIRECTION ( 'NONE',  ( -1.000000000000000000, 0.000000000000000000, -0.000000000000000000 ) ) ;
#20275=FACE_OUTER_BOUND ( 'NONE', #5858, .T. ) ;
#20300=VERTEX_POINT ( 'NONE', #22722 ) ;
#20302=CARTESIAN_POINT ( 'NONE',  ( 7.999999999999992895, -47.00885577955408223, -6.806061952192771436 ) ) ;
#20303=ORIENTED_EDGE ( 'NONE', *, *, #34749, .F. ) ;
#20306=CARTESIAN_POINT ( 'NONE',  ( 7.999999999999992895, -50.95304419620817526, -10.38206564895716255 ) ) ;
#20311=CIRCLE ( 'NONE', #34148, 20.00000000000000355 ) ;
#20329=ORIENTED_EDGE ( 'NONE', *, *, #11627, .T. ) ;
#20343=CARTESIAN_POINT ( 'NONE',  ( 7.999999999999992895, -51.93417535146740960, -2.615612846549736581 ) ) ;
#20345=VERTEX_POINT ( 'NONE', #24739 ) ;
#20348=DIRECTION ( 'NONE',  ( -1.000000000000000000, -0.000000000000000000, -0.000000000000000000 ) ) ;
#20356=AXIS2_PLACEMENT_3D ( 'NONE', #15393, #2459, #26765 ) ;
#20357=EDGE_CURVE ( 'NONE', #779, #15796, #8688, .T. ) ;
#20362=AXIS2_PLACEMENT_3D ( 'NONE', #27373, #33123, #8449 ) ;
#20368=EDGE_CURVE ( 'NONE', #29056, #35356, #1759, .T. ) ;
#20375=DIRECTION ( 'NONE',  ( -1.000000000000000000, 0.000000000000000000, 0.000000000000000000 ) ) ;
#20379=CIRCLE ( 'NONE', #18113, 47.49900000000001654 ) ;
#20387=ORIENTED_EDGE ( 'NONE', *, *, #7733, .T. ) ;
#20389=FILL_AREA_STYLE ('',( #9431 ) ) ;
#20398=CARTESIAN_POINT ( 'NONE',  ( 7.999999999999992895, -47.32430374665916872, -21.55018039121578255 ) ) ;
#20404=CIRCLE ( 'NONE', #5516, 52.00000000000000711 ) ;
#20413=CIRCLE ( 'NONE', #23312, 20.00000000000000355 ) ;
#20416=DIRECTION ( 'NONE',  ( -1.000000000000000000, -0.000000000000000000, -0.000000000000000000 ) ) ;
#20424=CIRCLE ( 'NONE', #3785, 20.00000000000000711 ) ;
#20427=VERTEX_POINT ( 'NONE', #6347 ) ;
#20432=DIRECTION ( 'NONE',  ( 1.000000000000000000, 0.000000000000000000, -0.000000000000000000 ) ) ;
#20437=AXIS2_PLACEMENT_3D ( 'NONE', #17861, #31561, #6887 ) ;
#20445=CARTESIAN_POINT ( 'NONE',  ( 7.999999999999992895, 7.162210897275726573, 51.50439529848831199 ) ) ;
#20446=ADVANCED_FACE ( 'NONE', ( #237 ), #34746, .T. ) ;
#20447=EDGE_CURVE ( 'NONE', #6690, #7164, #21895, .T. ) ;
#20449=FACE_OUTER_BOUND ( 'NONE', #28001, .T. ) ;
#20457=DIRECTION ( 'NONE',  ( 1.000000000000000000, 0.000000000000000000, 0.000000000000000000 ) ) ;
#20467=VERTEX_POINT ( 'NONE', #28496 ) ;
#20474=EDGE_LOOP ( 'NONE', ( #5627, #1661, #921, #31457 ) ) ;
#20492=VERTEX_POINT ( 'NONE', #13150 ) ;
#20498=ADVANCED_FACE ( 'NONE', ( #6609 ), #14353, .T. ) ;
#20500=ORIENTED_EDGE ( 'NONE', *, *, #31555, .F. ) ;
#20508=AXIS2_PLACEMENT_3D ( 'NONE', #13988, #6066, #488 ) ;
#20509=CARTESIAN_POINT ( 'NONE',  ( 7.999999999999992895, -44.75336757549767697, -14.30704879393654494 ) ) ;
#20518=DIRECTION ( 'NONE',  ( 0.000000000000000000, 0.000000000000000000, -1.000000000000000000 ) ) ;
#20521=EDGE_LOOP ( 'NONE', ( #1473, #10813, #33482, #31267 ) ) ;
#20522=CARTESIAN_POINT ( 'NONE',  ( 0.000000000000000000, -32.32520163883559405, -34.09746168776067776 ) ) ;
#20530=DIRECTION ( 'NONE',  ( 0.000000000000000000, -0.5877852522924624790, -0.8090169943749551118 ) ) ;
#20554=DIRECTION ( 'NONE',  ( 0.000000000000000000, 0.000000000000000000, 1.000000000000000000 ) ) ;
#20559=CIRCLE ( 'NONE', #4512, 20.00000000000000355 ) ;
#20561=DIRECTION ( 'NONE',  ( -1.000000000000000000, 0.000000000000000000, 0.000000000000000000 ) ) ;
#20562=CIRCLE ( 'NONE', #2207, 52.00000000000000711 ) ;
#20564=DIRECTION ( 'NONE',  ( -1.000000000000000000, -0.000000000000000000, -0.000000000000000000 ) ) ;
#20566=AXIS2_PLACEMENT_3D ( 'NONE', #6630, #31129, #11342 ) ;
#20568=ORIENTED_EDGE ( 'NONE', *, *, #18109, .T. ) ;
#20575=ORIENTED_EDGE ( 'NONE', *, *, #30449, .F. ) ;
#20579=DIRECTION ( 'NONE',  ( 0.000000000000000000, -0.8443279255020087470, -0.5358267949790064266 ) ) ;
#20581=EDGE_LOOP ( 'NONE', ( #18242, #21439, #28480, #5506 ) ) ;
#20583=ORIENTED_EDGE ( 'NONE', *, *, #33770, .F. ) ;
#20584=SHAPE_REPRESENTATION_RELATIONSHIP ( 'NONE' , 'NONE' ,  #7982, #6921 ) ;
#20585=ORIENTED_EDGE ( 'NONE', *, *, #19823, .F. ) ;
#20591=LINE ( 'NONE', #26017, #5326 ) ;
#20598=CIRCLE ( 'NONE', #7395, 20.00000000000000355 ) ;
#20603=CARTESIAN_POINT ( 'NONE',  ( 4.000000000000003553, 40.47821179127715396, 32.64221760512774040 ) ) ;
#20605=CYLINDRICAL_SURFACE ( 'NONE', #965, 52.00000000000000711 ) ;
#20610=LINE ( 'NONE', #20249, #31479 ) ;
#20611=ORIENTED_EDGE ( 'NONE', *, *, #13536, .T. ) ;
#20616=ORIENTED_EDGE ( 'NONE', *, *, #23294, .T. ) ;
#20620=CARTESIAN_POINT ( 'NONE',  ( 0.000000000000000000, -11.46872990052412611, 45.56340405422440654 ) ) ;
#20621=CARTESIAN_POINT ( 'NONE',  ( 7.999999999999992895, -32.00046193115173310, 34.40241257139674502 ) ) ;
#20624=DIRECTION ( 'NONE',  ( 0.000000000000000000, 0.000000000000000000, -1.000000000000000000 ) ) ;
#20628=DIRECTION ( 'NONE',  ( -1.000000000000000000, -0.000000000000000000, -0.000000000000000000 ) ) ;
#20631=CIRCLE ( 'NONE', #25264, 20.00000000000000711 ) ;
#20636=DIRECTION ( 'NONE',  ( -1.000000000000000000, 0.000000000000000000, 0.000000000000000000 ) ) ;
#20640=CARTESIAN_POINT ( 'NONE',  ( 7.999999999999992895, -37.91532898920900863, -28.61088654061680359 ) ) ;
#20648=CARTESIAN_POINT ( 'NONE',  ( 7.999999999999992895, 0.000000000000000000, 0.000000000000000000 ) ) ;
#20650=ORIENTED_EDGE ( 'NONE', *, *, #31158, .T. ) ;
#20653=EDGE_CURVE ( 'NONE', #17430, #12448, #6942, .T. ) ;
#20674=EDGE_LOOP ( 'NONE', ( #17927, #8489, #32373, #15982 ) ) ;
#20676=AXIS2_PLACEMENT_3D ( 'NONE', #14192, #10801, #11148 ) ;
#20680=CARTESIAN_POINT ( 'NONE',  ( 7.999999999999992895, -44.61570720899105424, 14.73072383765550164 ) ) ;
#20681=AXIS2_PLACEMENT_3D ( 'NONE', #22781, #15923, #7643 ) ;
#20683=CIRCLE ( 'NONE', #4048, 20.00000000000000355 ) ;
#20689=DIRECTION ( 'NONE',  ( 0.000000000000000000, 0.000000000000000000, 1.000000000000000000 ) ) ;
#20690=ORIENTED_EDGE ( 'NONE', *, *, #6800, .T. ) ;
#20696=ORIENTED_EDGE ( 'NONE', *, *, #31555, .T. ) ;
#20700=DIRECTION ( 'NONE',  ( -1.000000000000000000, -0.000000000000000000, -0.000000000000000000 ) ) ;
#20706=CARTESIAN_POINT ( 'NONE',  ( 7.999999999999992895, 7.162210897276456656, -51.50439529848821252 ) ) ;
#20708=ORIENTED_EDGE ( 'NONE', *, *, #32550, .F. ) ;
#20713=EDGE_CURVE ( 'NONE', #4978, #22530, #33962, .T. ) ;
#20727=DIRECTION ( 'NONE',  ( 0.000000000000000000, 0.000000000000000000, 1.000000000000000000 ) ) ;
#20733=EDGE_CURVE ( 'NONE', #27996, #13354, #7504, .T. ) ;
#20737=DIRECTION ( 'NONE',  ( 0.000000000000000000, 0.000000000000000000, 1.000000000000000000 ) ) ;
#20741=ORIENTED_EDGE ( 'NONE', *, *, #11537, .F. ) ;
#20762=CARTESIAN_POINT ( 'NONE',  ( 7.999999999999992895, -49.25004636492377585, -16.68630974939810940 ) ) ;
#20764=CARTESIAN_POINT ( 'NONE',  ( 7.999999999999992895, 0.000000000000000000, 0.000000000000000000 ) ) ;
#20765=EDGE_CURVE ( 'NONE', #2094, #3037, #24228, .T. ) ;
#20767=CYLINDRICAL_SURFACE ( 'NONE', #23783, 47.49900000000001654 ) ;
#20768=EDGE_CURVE ( 'NONE', #10384, #12895, #4824, .T. ) ;
#20770=LINE ( 'NONE', #29618, #8836 ) ;
#20778=DIRECTION ( 'NONE',  ( 0.000000000000000000, 0.000000000000000000, 1.000000000000000000 ) ) ;
#20785=CARTESIAN_POINT ( 'NONE',  ( 4.000000000000003553, -12.30077720129063756, -50.52416135122095397 ) ) ;
#20790=DIRECTION ( 'NONE',  ( -1.000000000000000000, 0.000000000000000000, 0.000000000000000000 ) ) ;
#20805=AXIS2_PLACEMENT_3D ( 'NONE', #20049, #9625, #34293 ) ;
#20814=CYLINDRICAL_SURFACE ( 'NONE', #13627, 47.49900000000001654 ) ;
#20816=AXIS2_PLACEMENT_3D ( 'NONE', #31023, #8699, #30681 ) ;
#20824=DIRECTION ( 'NONE',  ( -1.000000000000000000, 0.000000000000000000, 0.000000000000000000 ) ) ;
#20826=ORIENTED_EDGE ( 'NONE', *, *, #5932, .F. ) ;
#20828=CARTESIAN_POINT ( 'NONE',  ( 7.999999999999992895, 46.87740477351717061, 16.82754413119462455 ) ) ;
#20831=EDGE_LOOP ( 'NONE', ( #23741, #12685, #8809, #1446 ) ) ;
#20833=VECTOR ( 'NONE', #7802, 1000.000000000000000 ) ;
#20835=DIRECTION ( 'NONE',  ( 0.000000000000000000, 0.4817536741017101609, 0.8763066800438663595 ) ) ;
#20845=CARTESIAN_POINT ( 'NONE',  ( 7.999999999999992895, 0.000000000000000000, 0.000000000000000000 ) ) ;
#20860=CARTESIAN_POINT ( 'NONE',  ( 7.999999999999992895, -35.20873326984057883, -31.88259874184068465 ) ) ;
#20866=ORIENTED_EDGE ( 'NONE', *, *, #2684, .T. ) ;
#20867=ADVANCED_FACE ( 'NONE', ( #23534 ), #28765, .T. ) ;
#20869=DIRECTION ( 'NONE',  ( 0.000000000000000000, -0.8443279255020201823, 0.5358267949789886631 ) ) ;
#20876=DIRECTION ( 'NONE',  ( 0.000000000000000000, -0.9510565162951500895, -0.3090169943749581649 ) ) ;
#20888=CYLINDRICAL_SURFACE ( 'NONE', #2945, 20.00000000000000711 ) ;
#20889=ORIENTED_EDGE ( 'NONE', *, *, #12556, .T. ) ;
#20893=LINE ( 'NONE', #35156, #7567 ) ;
#20896=CARTESIAN_POINT ( 'NONE',  ( 7.999999999999992895, 0.000000000000000000, 0.000000000000000000 ) ) ;
#20897=AXIS2_PLACEMENT_3D ( 'NONE', #10400, #27634, #2804 ) ;
#20902=EDGE_CURVE ( 'NONE', #1742, #33000, #21326, .T. ) ;
#20916=DIRECTION ( 'NONE',  ( 0.000000000000000000, 0.000000000000000000, 1.000000000000000000 ) ) ;
#20920=CARTESIAN_POINT ( 'NONE',  ( 0.000000000000000000, 36.34385289850589373, 29.77717097092089205 ) ) ;
#20926=ORIENTED_EDGE ( 'NONE', *, *, #3104, .F. ) ;
#20931=ORIENTED_EDGE ( 'NONE', *, *, #11910, .F. ) ;
#20937=EDGE_CURVE ( 'NONE', #21589, #21098, #33434, .T. ) ;
#20947=DIRECTION ( 'NONE',  ( -1.000000000000000000, 0.000000000000000000, 0.000000000000000000 ) ) ;
#20956=ORIENTED_EDGE ( 'NONE', *, *, #5319, .T. ) ;
#20964=DIRECTION ( 'NONE',  ( 1.000000000000000000, 0.000000000000000000, 0.000000000000000000 ) ) ;
#20968=AXIS2_PLACEMENT_3D ( 'NONE', #3925, #17388, #31095 ) ;
#20973=EDGE_CURVE ( 'NONE', #5751, #1868, #27185, .T. ) ;
#20976=ORIENTED_EDGE ( 'NONE', *, *, #1289, .T. ) ;
#20980=CARTESIAN_POINT ( 'NONE',  ( 4.000000000000003553, 36.06787431788677623, 37.45808914225502662 ) ) ;
#20981=DIRECTION ( 'NONE',  ( 0.000000000000000000, 0.000000000000000000, 1.000000000000000000 ) ) ;
#20982=ORIENTED_EDGE ( 'NONE', *, *, #15431, .T. ) ;
#20986=CARTESIAN_POINT ( 'NONE',  ( 0.000000000000000000, 0.000000000000000000, 0.000000000000000000 ) ) ;
#20999=DIRECTION ( 'NONE',  ( 0.000000000000000000, 0.000000000000000000, 1.000000000000000000 ) ) ;
#21001=AXIS2_PLACEMENT_3D ( 'NONE', #17994, #29364, #21237 ) ;
#21002=CARTESIAN_POINT ( 'NONE',  ( 7.999999999999992895, 3.840921266749832252, 47.34345070675172451 ) ) ;
#21005=DIRECTION ( 'NONE',  ( -1.000000000000000000, 0.000000000000000000, 0.000000000000000000 ) ) ;
#21013=CARTESIAN_POINT ( 'NONE',  ( 0.000000000000000000, 32.32520163883631170, -34.09746168776000985 ) ) ;
#21016=EDGE_LOOP ( 'NONE', ( #4057, #19039, #32813, #3919 ) ) ;
#21021=LINE ( 'NONE', #21548, #9652 ) ;
#21030=DIRECTION ( 'NONE',  ( 0.000000000000000000, 0.000000000000000000, 1.000000000000000000 ) ) ;
#21041=CARTESIAN_POINT ( 'NONE',  ( 7.999999999999992895, -39.78933988720095982, -24.98727647985043987 ) ) ;
#21046=VERTEX_POINT ( 'NONE', #16481 ) ;
#21047=CIRCLE ( 'NONE', #22768, 20.00000000000000355 ) ;
#21052=ORIENTED_EDGE ( 'NONE', *, *, #29712, .F. ) ;
#21057=EDGE_LOOP ( 'NONE', ( #4186, #29230, #32393, #20611 ) ) ;
#21061=ORIENTED_EDGE ( 'NONE', *, *, #33878, .T. ) ;
#21064=DIRECTION ( 'NONE',  ( -1.000000000000000000, 0.000000000000000000, -0.000000000000000000 ) ) ;
#21077=LINE ( 'NONE', #15847, #4143 ) ;
#21082=ADVANCED_FACE ( 'NONE', ( #28542 ), #11981, .T. ) ;
#21085=CARTESIAN_POINT ( 'NONE',  ( 7.999999999999992895, 36.05989434073613609, 30.12041790338630776 ) ) ;
#21089=CARTESIAN_POINT ( 'NONE',  ( 7.999999999999992895, 47.32430374665932504, 21.55018039121545215 ) ) ;
#21097=AXIS2_PLACEMENT_3D ( 'NONE', #16091, #5495, #432 ) ;
#21098=VERTEX_POINT ( 'NONE', #24962 ) ;
#21100=DIRECTION ( 'NONE',  ( -1.000000000000000000, -0.000000000000000000, -0.000000000000000000 ) ) ;
#21102=DIRECTION ( 'NONE',  ( 0.000000000000000000, 0.000000000000000000, 1.000000000000000000 ) ) ;
#21115=EDGE_CURVE ( 'NONE', #21218, #9660, #2487, .T. ) ;
#21117=ADVANCED_FACE ( 'NONE', ( #30538 ), #25491, .T. ) ;
#21128=AXIS2_PLACEMENT_3D ( 'NONE', #18867, #18151, #32205 ) ;
#21137=DIRECTION ( 'NONE',  ( 0.000000000000000000, 0.000000000000000000, -1.000000000000000000 ) ) ;
#21138=FACE_OUTER_BOUND ( 'NONE', #7044, .T. ) ;
#21151=CARTESIAN_POINT ( 'NONE',  ( 7.999999999999992895, -11.46872990052349550, -45.56340405422456996 ) ) ;
#21158=ORIENTED_EDGE ( 'NONE', *, *, #27088, .F. ) ;
#21166=EDGE_CURVE ( 'NONE', #34766, #30554, #3531, .T. ) ;
#21169=VERTEX_POINT ( 'NONE', #31239 ) ;
#21183=CARTESIAN_POINT ( 'NONE',  ( 7.999999999999992895, -43.83938735307256707, -18.28286404005846677 ) ) ;
#21185=CIRCLE ( 'NONE', #26947, 20.00000000000000711 ) ;
#21192=DIRECTION ( 'NONE',  ( 0.000000000000000000, 0.000000000000000000, 1.000000000000000000 ) ) ;
#21194=EDGE_CURVE ( 'NONE', #28247, #30561, #28919, .T. ) ;
#21195=EDGE_CURVE ( 'NONE', #13985, #1301, #16822, .T. ) ;
#21198=VERTEX_POINT ( 'NONE', #12329 ) ;
#21201=DIRECTION ( 'NONE',  ( 0.000000000000000000, 0.7705132427757861446, 0.6374239897486932982 ) ) ;
#21202=ORIENTED_EDGE ( 'NONE', *, *, #3, .F. ) ;
#21204=DIRECTION ( 'NONE',  ( -1.000000000000000000, 0.000000000000000000, -0.000000000000000000 ) ) ;
#21210=ORIENTED_EDGE ( 'NONE', *, *, #886, .T. ) ;
#21218=VERTEX_POINT ( 'NONE', #32130 ) ;
#21224=CARTESIAN_POINT ( 'NONE',  ( -9.999999999999994671, 0.000000000000000000, 0.000000000000000000 ) ) ;
#21226=CARTESIAN_POINT ( 'NONE',  ( 0.000000000000000000, 15.49408907645171318, 44.90087086784599535 ) ) ;
#21227=AXIS2_PLACEMENT_3D ( 'NONE', #24253, #5518, #27494 ) ;
#21237=DIRECTION ( 'NONE',  ( 0.000000000000000000, 0.000000000000000000, 1.000000000000000000 ) ) ;
#21238=CARTESIAN_POINT ( 'NONE',  ( 7.999999999999992895, 0.000000000000000000, 0.000000000000000000 ) ) ;
#21258=ORIENTED_EDGE ( 'NONE', *, *, #30362, .F. ) ;
#21260=AXIS2_PLACEMENT_3D ( 'NONE', #27538, #24824, #33103 ) ;
#21263=AXIS2_PLACEMENT_3D ( 'NONE', #14671, #33783, #30899 ) ;
#21269=FACE_OUTER_BOUND ( 'NONE', #35051, .T. ) ;
#21272=DIRECTION ( 'NONE',  ( -1.000000000000000000, 0.000000000000000000, 0.000000000000000000 ) ) ;
#21280=ORIENTED_EDGE ( 'NONE', *, *, #26701, .F. ) ;
#21287=DIRECTION ( 'NONE',  ( -1.000000000000000000, -0.000000000000000000, 0.000000000000000000 ) ) ;
#21296=CARTESIAN_POINT ( 'NONE',  ( 4.000000000000003553, 43.55304910509406824, 28.41006711800001128 ) ) ;
#21302=DIRECTION ( 'NONE',  ( -1.000000000000000000, -0.000000000000000000, 0.000000000000000000 ) ) ;
#21307=AXIS2_PLACEMENT_3D ( 'NONE', #26589, #12725, #18292 ) ;
#21311=DIRECTION ( 'NONE',  ( -1.000000000000000000, -0.000000000000000000, -0.000000000000000000 ) ) ;
#21313=EDGE_CURVE ( 'NONE', #7438, #19094, #9985, .T. ) ;
#21326=CIRCLE ( 'NONE', #11011, 20.00000000000000355 ) ;
#21327=ADVANCED_FACE ( 'NONE', ( #1710 ), #20767, .T. ) ;
#21328=CARTESIAN_POINT ( 'NONE',  ( 7.999999999999992895, -44.47301969247433817, -16.68249143361957820 ) ) ;
#21332=ORIENTED_EDGE ( 'NONE', *, *, #6432, .F. ) ;
#21333=CARTESIAN_POINT ( 'NONE',  ( 7.999999999999992895, -3.840921266749481422, -47.34345070675177425 ) ) ;
#21338=VERTEX_POINT ( 'NONE', #29074 ) ;
#21341=ORIENTED_EDGE ( 'NONE', *, *, #26222, .F. ) ;
#21344=EDGE_CURVE ( 'NONE', #2400, #26214, #12696, .T. ) ;
#21345=CYLINDRICAL_SURFACE ( 'NONE', #4172, 20.00000000000000711 ) ;
#21346=ORIENTED_EDGE ( 'NONE', *, *, #25198, .F. ) ;
#21352=LINE ( 'NONE', #34527, #31495 ) ;
#21354=EDGE_CURVE ( 'NONE', #19035, #30069, #32952, .T. ) ;
#21364=DIRECTION ( 'NONE',  ( -1.000000000000000000, 0.000000000000000000, 0.000000000000000000 ) ) ;
#21384=CIRCLE ( 'NONE', #34648, 20.00000000000000711 ) ;
#21387=EDGE_CURVE ( 'NONE', #6691, #1965, #23126, .T. ) ;
#21390=ORIENTED_EDGE ( 'NONE', *, *, #10525, .T. ) ;
#21393=DIRECTION ( 'NONE',  ( 0.000000000000000000, 0.000000000000000000, 1.000000000000000000 ) ) ;
#21394=FACE_OUTER_BOUND ( 'NONE', #8893, .T. ) ;
#21408=DIRECTION ( 'NONE',  ( -1.000000000000000000, 0.000000000000000000, -0.000000000000000000 ) ) ;
#21416=VECTOR ( 'NONE', #26559, 1000.000000000000000 ) ;
#21419=ORIENTED_EDGE ( 'NONE', *, *, #2777, .F. ) ;
#21420=ORIENTED_EDGE ( 'NONE', *, *, #18568, .T. ) ;
#21422=ORIENTED_EDGE ( 'NONE', *, *, #31008, .F. ) ;
#21429=CARTESIAN_POINT ( 'NONE',  ( 0.000000000000000000, -44.75336757549789013, 14.30704879393590545 ) ) ;
#21437=AXIS2_PLACEMENT_3D ( 'NONE', #14568, #25938, #34035 ) ;
#21439=ORIENTED_EDGE ( 'NONE', *, *, #24718, .F. ) ;
#21443=CARTESIAN_POINT ( 'NONE',  ( 0.000000000000000000, -32.00046193115124282, -34.40241257139719977 ) ) ;
#21455=DIRECTION ( 'NONE',  ( -1.000000000000000000, -0.000000000000000000, -0.000000000000000000 ) ) ;
#21460=CIRCLE ( 'NONE', #32401, 52.00000000000000711 ) ;
#21462=DIRECTION ( 'NONE',  ( 0.000000000000000000, 0.000000000000000000, 1.000000000000000000 ) ) ;
#21471=ORIENTED_EDGE ( 'NONE', *, *, #836, .T. ) ;
#21473=EDGE_CURVE ( 'NONE', #29218, #33428, #18975, .T. ) ;
#21476=CIRCLE ( 'NONE', #25510, 52.00000000000000711 ) ;
#21484=AXIS2_PLACEMENT_3D ( 'NONE', #5382, #27696, #35445 ) ;
#21488=DIRECTION ( 'NONE',  ( -1.000000000000000000, -0.000000000000000000, 0.000000000000000000 ) ) ;
#21496=CARTESIAN_POINT ( 'NONE',  ( 0.000000000000000000, -46.11014828289849277, 9.022736828080537563 ) ) ;
#21500=CIRCLE ( 'NONE', #26126, 20.00000000000000711 ) ;
#21504=ORIENTED_EDGE ( 'NONE', *, *, #10155, .F. ) ;
#21516=DIRECTION ( 'NONE',  ( 0.000000000000000000, 0.000000000000000000, 1.000000000000000000 ) ) ;
#21518=EDGE_CURVE ( 'NONE', #10719, #21916, #24939, .T. ) ;
#21526=AXIS2_PLACEMENT_3D ( 'NONE', #1414, #25552, #1239 ) ;
#21530=DIRECTION ( 'NONE',  ( -1.000000000000000000, -0.000000000000000000, 0.000000000000000000 ) ) ;
#21531=LINE ( 'NONE', #30027, #33916 ) ;
#21536=ADVANCED_FACE ( 'NONE', ( #29800 ), #4781, .T. ) ;
#21540=ORIENTED_EDGE ( 'NONE', *, *, #26015, .T. ) ;
#21548=CARTESIAN_POINT ( 'NONE',  ( 7.999999999999992895, 26.17370628620655637, 39.63700417846175128 ) ) ;
#21550=EDGE_CURVE ( 'NONE', #16904, #24590, #23809, .T. ) ;
#21559=VECTOR ( 'NONE', #35189, 1000.000000000000000 ) ;
#21577=FACE_OUTER_BOUND ( 'NONE', #25115, .T. ) ;
#21579=AXIS2_PLACEMENT_3D ( 'NONE', #32682, #27282, #21864 ) ;
#21586=ADVANCED_FACE ( 'NONE', ( #8870 ), #22549, .T. ) ;
#21589=VERTEX_POINT ( 'NONE', #30845 ) ;
#21590=CARTESIAN_POINT ( 'NONE',  ( 0.000000000000000000, -46.77034588191320097, 22.72740077717213936 ) ) ;
#21598=ORIENTED_EDGE ( 'NONE', *, *, #6021, .F. ) ;
#21603=VERTEX_POINT ( 'NONE', #16791 ) ;
#21604=ORIENTED_EDGE ( 'NONE', *, *, #15417, .F. ) ;
#21608=EDGE_LOOP ( 'NONE', ( #22167, #30733, #16820, #23332 ) ) ;
#21611=CIRCLE ( 'NONE', #15852, 20.00000000000000711 ) ;
#21612=EDGE_CURVE ( 'NONE', #31611, #10641, #34275, .T. ) ;
#21615=CYLINDRICAL_SURFACE ( 'NONE', #13167, 52.00000000000000711 ) ;
#21624=DIRECTION ( 'NONE',  ( 0.000000000000000000, 0.7705132427757861446, 0.6374239897486934092 ) ) ;
#21638=VECTOR ( 'NONE', #15284, 1000.000000000000000 ) ;
#21646=ADVANCED_FACE ( 'NONE', ( #33904 ), #28324, .T. ) ;
#21648=EDGE_CURVE ( 'NONE', #12363, #35108, #4376, .T. ) ;
#21651=VECTOR ( 'NONE', #19157, 1000.000000000000000 ) ;
#21652=DIRECTION ( 'NONE',  ( -1.000000000000000000, -0.000000000000000000, -0.000000000000000000 ) ) ;
#21662=CARTESIAN_POINT ( 'NONE',  ( 0.000000000000000000, 44.47301969247469344, -16.68249143361863318 ) ) ;
#21670=AXIS2_PLACEMENT_3D ( 'NONE', #35041, #26570, #12883 ) ;
#21677=AXIS2_PLACEMENT_3D ( 'NONE', #929, #22886, #28477 ) ;
#21685=DIRECTION ( 'NONE',  ( -1.000000000000000000, 0.000000000000000000, 0.000000000000000000 ) ) ;
#21687=DIRECTION ( 'NONE',  ( -1.000000000000000000, 0.000000000000000000, 0.000000000000000000 ) ) ;
#21697=ORIENTED_EDGE ( 'NONE', *, *, #7348, .F. ) ;
#21699=AXIS2_PLACEMENT_3D ( 'NONE', #17511, #33553, #6717 ) ;
#21704=CIRCLE ( 'NONE', #12511, 47.49900000000001654 ) ;
#21708=CARTESIAN_POINT ( 'NONE',  ( 7.999999999999992895, -36.06787431788650622, -37.45808914225528952 ) ) ;
#21714=VECTOR ( 'NONE', #6839, 1000.000000000000000 ) ;
#21718=CIRCLE ( 'NONE', #21128, 20.00000000000000355 ) ;
#21722=DIRECTION ( 'NONE',  ( -1.000000000000000000, 0.000000000000000000, 0.000000000000000000 ) ) ;
#21723=EDGE_CURVE ( 'NONE', #31137, #22200, #23927, .T. ) ;
#21728=DIRECTION ( 'NONE',  ( -1.000000000000000000, 0.000000000000000000, -0.000000000000000000 ) ) ;
#21732=ORIENTED_EDGE ( 'NONE', *, *, #28317, .T. ) ;
#21734=DIRECTION ( 'NONE',  ( -1.000000000000000000, -0.000000000000000000, 0.000000000000000000 ) ) ;
#21746=CARTESIAN_POINT ( 'NONE',  ( 7.999999999999992895, -30.93515269692089120, -36.04401931830286543 ) ) ;
#21755=CARTESIAN_POINT ( 'NONE',  ( 0.000000000000000000, 43.83938735307295076, -18.28286404005752175 ) ) ;
#21758=CARTESIAN_POINT ( 'NONE',  ( 0.000000000000000000, -47.49120266317497396, 0.8606222198173640869 ) ) ;
#21762=DIRECTION ( 'NONE',  ( -1.000000000000000000, 0.000000000000000000, 0.000000000000000000 ) ) ;
#21765=EDGE_CURVE ( 'NONE', #22834, #8928, #12473, .T. ) ;
#21767=ORIENTED_EDGE ( 'NONE', *, *, #28925, .T. ) ;
#21770=VECTOR ( 'NONE', #32974, 1000.000000000000000 ) ;
#21776=CARTESIAN_POINT ( 'NONE',  ( 0.000000000000000000, -27.79676263918161894, -37.88001506494798321 ) ) ;
#21777=EDGE_CURVE ( 'NONE', #4539, #30241, #14134, .T. ) ;
#21780=ADVANCED_FACE ( 'NONE', ( #12291 ), #34082, .T. ) ;
#21789=ORIENTED_EDGE ( 'NONE', *, *, #18068, .T. ) ;
#21798=CARTESIAN_POINT ( 'NONE',  ( 4.000000000000003553, 19.74581912682909390, -48.10512059033372623 ) ) ;
#21807=ADVANCED_FACE ( 'NONE', ( #12659 ), #23636, .T. ) ;
#21820=VECTOR ( 'NONE', #8373, 1000.000000000000000 ) ;
#21831=AXIS2_PLACEMENT_3D ( 'NONE', #22423, #5707, #16667 ) ;
#21833=AXIS2_PLACEMENT_3D ( 'NONE', #3217, #24995, #11480 ) ;
#21834=ADVANCED_FACE ( 'NONE', ( #1141 ), #18219, .T. ) ;
#21835=DIRECTION ( 'NONE',  ( 0.000000000000000000, 0.000000000000000000, 1.000000000000000000 ) ) ;
#21836=ORIENTED_EDGE ( 'NONE', *, *, #23028, .F. ) ;
#21837=ORIENTED_EDGE ( 'NONE', *, *, #6475, .T. ) ;
#21846=VECTOR ( 'NONE', #34658, 1000.000000000000000 ) ;
#21853=FACE_OUTER_BOUND ( 'NONE', #15050, .T. ) ;
#21857=CARTESIAN_POINT ( 'NONE',  ( 0.000000000000000000, -37.91532898920942074, 28.61088654061626357 ) ) ;
#21864=DIRECTION ( 'NONE',  ( 0.000000000000000000, 0.000000000000000000, 1.000000000000000000 ) ) ;
#21880=ORIENTED_EDGE ( 'NONE', *, *, #22725, .F. ) ;
#21895=CIRCLE ( 'NONE', #6348, 47.49900000000001654 ) ;
#21903=( NAMED_UNIT ( * ) PLANE_ANGLE_UNIT ( ) SI_UNIT ( $, .RADIAN. ) );
#21909=CARTESIAN_POINT ( 'NONE',  ( 7.999999999999992895, -26.17370628620682638, 39.63700417846155233 ) ) ;
#21914=CARTESIAN_POINT ( 'NONE',  ( 7.999999999999992895, -42.60732521687556584, -19.80331771201704427 ) ) ;
#21916=VERTEX_POINT ( 'NONE', #12116 ) ;
#21920=AXIS2_PLACEMENT_3D ( 'NONE', #34170, #28942, #34350 ) ;
#21923=VERTEX_POINT ( 'NONE', #5098 ) ;
#21927=CARTESIAN_POINT ( 'NONE',  ( 7.999999999999992895, 0.000000000000000000, 0.000000000000000000 ) ) ;
#21936=ADVANCED_FACE ( 'NONE', ( #27412 ), #4747, .T. ) ;
#21941=CARTESIAN_POINT ( 'NONE',  ( 0.000000000000000000, -47.22458491092824318, 5.098390039074071289 ) ) ;
#21942=DIRECTION ( 'NONE',  ( 0.000000000000000000, 0.000000000000000000, 1.000000000000000000 ) ) ;
#21945=DIRECTION ( 'NONE',  ( -1.000000000000000000, 0.000000000000000000, -0.000000000000000000 ) ) ;
#21950=ORIENTED_EDGE ( 'NONE', *, *, #33602, .T. ) ;
#21958=CYLINDRICAL_SURFACE ( 'NONE', #7315, 52.00000000000000711 ) ;
#21960=ORIENTED_EDGE ( 'NONE', *, *, #20713, .T. ) ;
#21961=CARTESIAN_POINT ( 'NONE',  ( 4.000000000000003553, 51.93417535146742381, -2.615612846549375536 ) ) ;
#21966=CIRCLE ( 'NONE', #16792, 20.00000000000000711 ) ;
#21968=EDGE_CURVE ( 'NONE', #26304, #2304, #12424, .T. ) ;
#21977=ADVANCED_FACE ( 'NONE', ( #27056 ), #4917, .T. ) ;
#21991=CARTESIAN_POINT ( 'NONE',  ( 0.000000000000000000, 0.000000000000000000, 0.000000000000000000 ) ) ;
#22003=CIRCLE ( 'NONE', #21437, 20.00000000000000711 ) ;
#22005=ORIENTED_EDGE ( 'NONE', *, *, #35245, .T. ) ;
#22014=EDGE_CURVE ( 'NONE', #33987, #8021, #11300, .T. ) ;
#22023=DIRECTION ( 'NONE',  ( 0.000000000000000000, 0.7705132427757904745, -0.6374239897486881912 ) ) ;
#22033=VERTEX_POINT ( 'NONE', #21089 ) ;
#22036=CARTESIAN_POINT ( 'NONE',  ( 0.000000000000000000, -51.85248208264515313, -3.914090171286743747 ) ) ;
#22037=FACE_OUTER_BOUND ( 'NONE', #4459, .T. ) ;
#22038=CYLINDRICAL_SURFACE ( 'NONE', #29176, 52.00000000000000711 ) ;
#22045=DIRECTION ( 'NONE',  ( 0.000000000000000000, 0.000000000000000000, 1.000000000000000000 ) ) ;
#22048=AXIS2_PLACEMENT_3D ( 'NONE', #512, #12205, #28067 ) ;
#22052=CARTESIAN_POINT ( 'NONE',  ( 7.999999999999992895, -0.2227391519119825691, 46.98410307550729215 ) ) ;
#22068=DIRECTION ( 'NONE',  ( -1.000000000000000000, -0.000000000000000000, -0.000000000000000000 ) ) ;
#22071=CARTESIAN_POINT ( 'NONE',  ( 7.999999999999992895, 19.74581912682842244, 48.10512059033400334 ) ) ;
#22073=CARTESIAN_POINT ( 'NONE',  ( 7.999999999999992895, -22.82995208772657492, -41.06517797613687293 ) ) ;
#22077=DIRECTION ( 'NONE',  ( -1.000000000000000000, 0.000000000000000000, 0.000000000000000000 ) ) ;
#22079=AXIS2_PLACEMENT_3D ( 'NONE', #13161, #15641, #24136 ) ;
#22084=CARTESIAN_POINT ( 'NONE',  ( 7.999999999999992895, -5.871425383721907920, 51.66745943012281117 ) ) ;
#22088=ORIENTED_EDGE ( 'NONE', *, *, #14940, .T. ) ;
#22099=ORIENTED_EDGE ( 'NONE', *, *, #27941, .T. ) ;
#22106=ORIENTED_EDGE ( 'NONE', *, *, #32345, .T. ) ;
#22107=DIRECTION ( 'NONE',  ( -1.000000000000000000, -0.000000000000000000, 0.000000000000000000 ) ) ;
#22108=AXIS2_PLACEMENT_3D ( 'NONE', #12035, #11673, #22641 ) ;
#22117=DIRECTION ( 'NONE',  ( 1.000000000000000000, 0.000000000000000000, 0.000000000000000000 ) ) ;
#22121=ORIENTED_EDGE ( 'NONE', *, *, #33878, .F. ) ;
#22123=LINE ( 'NONE', #32766, #30747 ) ;
#22125=ORIENTED_EDGE ( 'NONE', *, *, #3827, .F. ) ;
#22128=DIRECTION ( 'NONE',  ( 0.000000000000000000, 0.5877852522924743583, -0.8090169943749466741 ) ) ;
#22131=ORIENTED_EDGE ( 'NONE', *, *, #4691, .T. ) ;
#22140=CARTESIAN_POINT ( 'NONE',  ( -9.999999999999994671, 0.000000000000000000, 0.000000000000000000 ) ) ;
#22143=VECTOR ( 'NONE', #27927, 1000.000000000000000 ) ;
#22148=EDGE_LOOP ( 'NONE', ( #20696, #12318, #3568, #2238 ) ) ;
#22152=DIRECTION ( 'NONE',  ( 0.000000000000000000, -0.8443279255020201823, 0.5358267949789887741 ) ) ;
#22153=DIRECTION ( 'NONE',  ( -1.000000000000000000, 0.000000000000000000, 0.000000000000000000 ) ) ;
#22164=CIRCLE ( 'NONE', #6644, 47.49900000000002365 ) ;
#22165=VERTEX_POINT ( 'NONE', #14232 ) ;
#22166=CARTESIAN_POINT ( 'NONE',  ( 7.999999999999992895, 0.000000000000000000, 52.00000000000000711 ) ) ;
#22167=ORIENTED_EDGE ( 'NONE', *, *, #1421, .F. ) ;
#22168=EDGE_CURVE ( 'NONE', #23898, #31607, #4984, .T. ) ;
#22183=ORIENTED_EDGE ( 'NONE', *, *, #2451, .F. ) ;
#22187=AXIS2_PLACEMENT_3D ( 'NONE', #24767, #8357, #2990 ) ;
#22192=FACE_OUTER_BOUND ( 'NONE', #14112, .T. ) ;
#22197=CARTESIAN_POINT ( 'NONE',  ( 7.999999999999992895, 0.000000000000000000, 0.000000000000000000 ) ) ;
#22200=VERTEX_POINT ( 'NONE', #33156 ) ;
#22202=CARTESIAN_POINT ( 'NONE',  ( 7.999999999999992895, 24.72041153920790180, -40.55929306992661765 ) ) ;
#22203=DIRECTION ( 'NONE',  ( -1.000000000000000000, 0.000000000000000000, -0.000000000000000000 ) ) ;
#22207=DIRECTION ( 'NONE',  ( 0.000000000000000000, 0.000000000000000000, 1.000000000000000000 ) ) ;
#22208=FACE_OUTER_BOUND ( 'NONE', #2122, .T. ) ;
#22212=EDGE_CURVE ( 'NONE', #34767, #31708, #11369, .T. ) ;
#22220=CARTESIAN_POINT ( 'NONE',  ( -9.999999999999994671, 0.000000000000000000, 0.000000000000000000 ) ) ;
#22229=ORIENTED_EDGE ( 'NONE', *, *, #29293, .F. ) ;
#22230=ORIENTED_EDGE ( 'NONE', *, *, #9123, .T. ) ;
#22234=VECTOR ( 'NONE', #907, 1000.000000000000000 ) ;
#22240=AXIS2_PLACEMENT_3D ( 'NONE', #27278, #2621, #35570 ) ;
#22241=DIRECTION ( 'NONE',  ( -1.000000000000000000, -0.000000000000000000, -0.000000000000000000 ) ) ;
#22244=CARTESIAN_POINT ( 'NONE',  ( 7.999999999999992895, 46.87740477351717061, -3.172455868805379442 ) ) ;
#22245=DIRECTION ( 'NONE',  ( 0.000000000000000000, 0.000000000000000000, 1.000000000000000000 ) ) ;
#22247=DIRECTION ( 'NONE',  ( 0.000000000000000000, -0.4817536741017223734, 0.8763066800438596982 ) ) ;
#22260=CARTESIAN_POINT ( 'NONE',  ( 0.000000000000000000, -30.03615769709705319, -42.44795908869020451 ) ) ;
#22262=AXIS2_PLACEMENT_3D ( 'NONE', #33035, #11420, #29813 ) ;
#22265=ORIENTED_EDGE ( 'NONE', *, *, #3104, .T. ) ;
#22268=ORIENTED_EDGE ( 'NONE', *, *, #31892, .T. ) ;
#22270=ORIENTED_EDGE ( 'NONE', *, *, #12015, .F. ) ;
#22276=ORIENTED_EDGE ( 'NONE', *, *, #5319, .F. ) ;
#22277=ORIENTED_EDGE ( 'NONE', *, *, #25198, .T. ) ;
#22279=DIRECTION ( 'NONE',  ( 0.000000000000000000, 0.000000000000000000, 1.000000000000000000 ) ) ;
#22280=DIRECTION ( 'NONE',  ( -1.000000000000000000, 0.000000000000000000, 0.000000000000000000 ) ) ;
#22282=LINE ( 'NONE', #25357, #20083 ) ;
#22286=AXIS2_PLACEMENT_3D ( 'NONE', #30563, #27340, #13827 ) ;
#22290=CARTESIAN_POINT ( 'NONE',  ( 7.999999999999992895, 0.000000000000000000, 0.000000000000000000 ) ) ;
#22295=CARTESIAN_POINT ( 'NONE',  ( 0.000000000000000000, 5.871425383722286284, -51.66745943012276854 ) ) ;
#22301=EDGE_CURVE ( 'NONE', #9489, #16062, #4338, .T. ) ;
#22303=EDGE_CURVE ( 'NONE', #16934, #15970, #1634, .T. ) ;
#22304=DIRECTION ( 'NONE',  ( 0.000000000000000000, 0.000000000000000000, 1.000000000000000000 ) ) ;
#22307=ORIENTED_EDGE ( 'NONE', *, *, #21765, .T. ) ;
#22313=LINE ( 'NONE', #33306, #12673 ) ;
#22316=VERTEX_POINT ( 'NONE', #11886 ) ;
#22327=ADVANCED_FACE ( 'NONE', ( #34950 ), #23955, .T. ) ;
#22332=DIRECTION ( 'NONE',  ( 0.000000000000000000, 0.000000000000000000, -1.000000000000000000 ) ) ;
#22335=CARTESIAN_POINT ( 'NONE',  ( 4.000000000000003553, 49.25004636492413823, -16.68630974939705425 ) ) ;
#22337=CARTESIAN_POINT ( 'NONE',  ( 7.999999999999992895, 9.744342220504046637, -46.48873837489789196 ) ) ;
#22340=FACE_OUTER_BOUND ( 'NONE', #14374, .T. ) ;
#22346=CARTESIAN_POINT ( 'NONE',  ( 0.000000000000000000, -29.60891106212763191, -37.14118181634798788 ) ) ;
#22356=DIRECTION ( 'NONE',  ( 1.000000000000000000, -0.000000000000000000, -0.000000000000000000 ) ) ;
#22357=ORIENTED_EDGE ( 'NONE', *, *, #7549, .F. ) ;
#22359=AXIS2_PLACEMENT_3D ( 'NONE', #28144, #948, #8686 ) ;
#22364=DIRECTION ( 'NONE',  ( -1.000000000000000000, 0.000000000000000000, 0.000000000000000000 ) ) ;
#22373=DIRECTION ( 'NONE',  ( -1.000000000000000000, -0.000000000000000000, -0.000000000000000000 ) ) ;
#22377=DIRECTION ( 'NONE',  ( 1.000000000000000000, 0.000000000000000000, 0.000000000000000000 ) ) ;
#22378=DIRECTION ( 'NONE',  ( -1.000000000000000000, -0.000000000000000000, 0.000000000000000000 ) ) ;
#22379=DIRECTION ( 'NONE',  ( 0.000000000000000000, 0.000000000000000000, 1.000000000000000000 ) ) ;
#22384=FACE_OUTER_BOUND ( 'NONE', #27850, .T. ) ;
#22385=CARTESIAN_POINT ( 'NONE',  ( 0.000000000000000000, -50.95304419620817526, -10.38206564895716255 ) ) ;
#22387=CIRCLE ( 'NONE', #24140, 52.00000000000000711 ) ;
#22391=ORIENTED_EDGE ( 'NONE', *, *, #25863, .T. ) ;
#22392=DIRECTION ( 'NONE',  ( 0.000000000000000000, 0.000000000000000000, 1.000000000000000000 ) ) ;
#22395=EDGE_LOOP ( 'NONE', ( #30650, #17677, #30111, #27855 ) ) ;
#22399=ORIENTED_EDGE ( 'NONE', *, *, #3178, .F. ) ;
#22401=DIRECTION ( 'NONE',  ( 0.000000000000000000, 0.000000000000000000, -1.000000000000000000 ) ) ;
#22405=ADVANCED_FACE ( 'NONE', ( #7387 ), #35301, .T. ) ;
#22412=AXIS2_PLACEMENT_3D ( 'NONE', #22452, #25180, #11137 ) ;
#22413=LINE ( 'NONE', #8559, #30897 ) ;
#22414=DIRECTION ( 'NONE',  ( -1.000000000000000000, 0.000000000000000000, -0.000000000000000000 ) ) ;
#22415=FACE_OUTER_BOUND ( 'NONE', #14764, .T. ) ;
#22423=CARTESIAN_POINT ( 'NONE',  ( 0.000000000000000000, 0.000000000000000000, 0.000000000000000000 ) ) ;
#22424=ORIENTED_EDGE ( 'NONE', *, *, #30642, .T. ) ;
#22437=VECTOR ( 'NONE', #9999, 1000.000000000000000 ) ;
#22439=AXIS2_PLACEMENT_3D ( 'NONE', #26511, #12454, #31711 ) ;
#22442=DIRECTION ( 'NONE',  ( 1.000000000000000000, -0.000000000000000000, 0.000000000000000000 ) ) ;
#22447=EDGE_CURVE ( 'NONE', #2304, #7406, #5313, .T. ) ;
#22449=EDGE_CURVE ( 'NONE', #15607, #27203, #7907, .T. ) ;
#22451=EDGE_CURVE ( 'NONE', #33603, #21198, #7651, .T. ) ;
#22452=CARTESIAN_POINT ( 'NONE',  ( 7.999999999999992895, 0.000000000000000000, 0.000000000000000000 ) ) ;
#22460=DIRECTION ( 'NONE',  ( 0.000000000000000000, -0.6845471059286794002, -0.7289686274214203232 ) ) ;
#22466=ADVANCED_FACE ( 'NONE', ( #12789 ), #4533, .T. ) ;
#22473=ORIENTED_EDGE ( 'NONE', *, *, #20937, .T. ) ;
#22479=CARTESIAN_POINT ( 'NONE',  ( 7.999999999999992895, -13.85708833599938217, -45.43276465116679930 ) ) ;
#22481=VERTEX_POINT ( 'NONE', #1188 ) ;
#22485=FACE_OUTER_BOUND ( 'NONE', #29643, .T. ) ;
#22492=VECTOR ( 'NONE', #32737, 1000.000000000000000 ) ;
#22495=ORIENTED_EDGE ( 'NONE', *, *, #30244, .T. ) ;
#22498=ORIENTED_EDGE ( 'NONE', *, *, #32106, .T. ) ;
#22514=CIRCLE ( 'NONE', #6996, 20.00000000000000355 ) ;
#22517=DIRECTION ( 'NONE',  ( 1.000000000000000000, 0.000000000000000000, 0.000000000000000000 ) ) ;
#22530=VERTEX_POINT ( 'NONE', #25496 ) ;
#22533=DIRECTION ( 'NONE',  ( 0.000000000000000000, 0.000000000000000000, 1.000000000000000000 ) ) ;
#22534=ORIENTED_EDGE ( 'NONE', *, *, #1867, .T. ) ;
#22539=ORIENTED_EDGE ( 'NONE', *, *, #6558, .F. ) ;
#22542=FACE_OUTER_BOUND ( 'NONE', #20474, .T. ) ;
#22546=DIRECTION ( 'NONE',  ( 0.000000000000000000, 0.000000000000000000, 1.000000000000000000 ) ) ;
#22549=CYLINDRICAL_SURFACE ( 'NONE', #11267, 20.00000000000000355 ) ;
#22550=CIRCLE ( 'NONE', #6443, 52.00000000000000711 ) ;
#22553=DIRECTION ( 'NONE',  ( -1.000000000000000000, 0.000000000000000000, -0.000000000000000000 ) ) ;
#22558=AXIS2_PLACEMENT_3D ( 'NONE', #20184, #26151, #20727 ) ;
#22560=LINE ( 'NONE', #433, #29943 ) ;
#22567=DIRECTION ( 'NONE',  ( 0.000000000000000000, 0.7705132427757903635, -0.6374239897486881912 ) ) ;
#22569=CYLINDRICAL_SURFACE ( 'NONE', #3064, 20.00000000000000355 ) ;
#22573=AXIS2_PLACEMENT_3D ( 'NONE', #23822, #26348, #1681 ) ;
#22574=VERTEX_POINT ( 'NONE', #12881 ) ;
#22593=CARTESIAN_POINT ( 'NONE',  ( 7.999999999999992895, 0.000000000000000000, 0.000000000000000000 ) ) ;
#22595=DIRECTION ( 'NONE',  ( 0.000000000000000000, 0.9048270524660176894, 0.4257792915650767118 ) ) ;
#22599=CARTESIAN_POINT ( 'NONE',  ( 0.000000000000000000, 14.30000000000000071, 0.000000000000000000 ) ) ;
#22605=ADVANCED_FACE ( 'NONE', ( #1537 ), #17729, .T. ) ;
#22606=DIRECTION ( 'NONE',  ( 0.000000000000000000, 0.000000000000000000, 1.000000000000000000 ) ) ;
#22609=ORIENTED_EDGE ( 'NONE', *, *, #2684, .F. ) ;
#22619=DIRECTION ( 'NONE',  ( 1.000000000000000000, 0.000000000000000000, 0.000000000000000000 ) ) ;
#22620=DIRECTION ( 'NONE',  ( 0.000000000000000000, 0.000000000000000000, -1.000000000000000000 ) ) ;
#22624=DIRECTION ( 'NONE',  ( 0.000000000000000000, 0.1253332335643045359, -0.9921147013144778759 ) ) ;
#22628=AXIS2_PLACEMENT_3D ( 'NONE', #20059, #6749, #6562 ) ;
#22632=CARTESIAN_POINT ( 'NONE',  ( 7.999999999999992895, 42.60732521687570795, 19.80331771201672453 ) ) ;
#22634=CARTESIAN_POINT ( 'NONE',  ( 7.999999999999992895, 10.58300524425836109, 3.000000000000002665 ) ) ;
#22641=DIRECTION ( 'NONE',  ( 0.000000000000000000, 0.000000000000000000, 1.000000000000000000 ) ) ;
#22643=ORIENTED_EDGE ( 'NONE', *, *, #6679, .T. ) ;
#22651=ORIENTED_EDGE ( 'NONE', *, *, #19790, .T. ) ;
#22653=AXIS2_PLACEMENT_3D ( 'NONE', #26988, #30039, #10770 ) ;
#22655=VECTOR ( 'NONE', #16002, 1000.000000000000000 ) ;
#22657=ORIENTED_EDGE ( 'NONE', *, *, #28851, .T. ) ;
#22660=EDGE_CURVE ( 'NONE', #10046, #22033, #22550, .T. ) ;
#22664=VERTEX_POINT ( 'NONE', #2441 ) ;
#22667=VERTEX_POINT ( 'NONE', #22036 ) ;
#22673=CARTESIAN_POINT ( 'NONE',  ( 0.000000000000000000, -5.667686777402029641, 46.64153600743602368 ) ) ;
#22681=ORIENTED_EDGE ( 'NONE', *, *, #10871, .F. ) ;
#22683=ORIENTED_EDGE ( 'NONE', *, *, #16789, .F. ) ;
#22694=EDGE_CURVE ( 'NONE', #25236, #28380, #21966, .T. ) ;
#22712=PRODUCT_DEFINITION_SHAPE ( 'NONE', 'NONE',  #5129 ) ;
#22713=AXIS2_PLACEMENT_3D ( 'NONE', #28372, #20416, #22959 ) ;
#22717=DIRECTION ( 'NONE',  ( 0.000000000000000000, 0.000000000000000000, 1.000000000000000000 ) ) ;
#22719=CIRCLE ( 'NONE', #4377, 20.00000000000000000 ) ;
#22722=CARTESIAN_POINT ( 'NONE',  ( 0.000000000000000000, 30.03615769709734451, 42.44795908869000556 ) ) ;
#22725=EDGE_CURVE ( 'NONE', #25525, #6691, #9919, .T. ) ;
#22730=FACE_OUTER_BOUND ( 'NONE', #2017, .T. ) ;
#22731=EDGE_CURVE ( 'NONE', #23819, #4059, #7035, .T. ) ;
#22733=DIRECTION ( 'NONE',  ( 0.000000000000000000, 0.000000000000000000, 1.000000000000000000 ) ) ;
#22744=DIRECTION ( 'NONE',  ( 0.000000000000000000, -0.9980267284282708928, -0.06279051952932447611 ) ) ;
#22746=CIRCLE ( 'NONE', #7799, 20.00000000000001066 ) ;
#22747=CARTESIAN_POINT ( 'NONE',  ( 7.999999999999992895, 0.000000000000000000, 0.000000000000000000 ) ) ;
#22749=CARTESIAN_POINT ( 'NONE',  ( 7.999999999999992895, -5.667686777402029641, 46.64153600743602368 ) ) ;
#22754=ORIENTED_EDGE ( 'NONE', *, *, #17657, .F. ) ;
#22755=ORIENTED_EDGE ( 'NONE', *, *, #26210, .F. ) ;
#22757=DIRECTION ( 'NONE',  ( -1.000000000000000000, 0.000000000000000000, 0.000000000000000000 ) ) ;
#22759=AXIS2_PLACEMENT_3D ( 'NONE', #13205, #21100, #1497 ) ;
#22766=DIRECTION ( 'NONE',  ( -1.000000000000000000, -0.000000000000000000, 0.000000000000000000 ) ) ;
#22768=AXIS2_PLACEMENT_3D ( 'NONE', #9422, #20031, #33920 ) ;
#22769=EDGE_CURVE ( 'NONE', #32263, #30, #12210, .T. ) ;
#22770=FACE_OUTER_BOUND ( 'NONE', #35470, .T. ) ;
#22780=DIRECTION ( 'NONE',  ( -1.000000000000000000, -0.000000000000000000, 0.000000000000000000 ) ) ;
#22781=CARTESIAN_POINT ( 'NONE',  ( 0.000000000000000000, -27.43636312076294814, -38.14186064215180494 ) ) ;
#22789=DIRECTION ( 'NONE',  ( -1.000000000000000000, -0.000000000000000000, 0.000000000000000000 ) ) ;
#22798=CARTESIAN_POINT ( 'NONE',  ( 7.999999999999992895, 35.20873326984128227, -31.88259874183993503 ) ) ;
#22802=VECTOR ( 'NONE', #27107, 1000.000000000000000 ) ;
#22809=CIRCLE ( 'NONE', #33751, 47.49900000000002365 ) ;
#22812=DIRECTION ( 'NONE',  ( -1.000000000000000000, -0.000000000000000000, -0.000000000000000000 ) ) ;
#22813=ADVANCED_FACE ( 'NONE', ( #25457 ), #425, .T. ) ;
#22815=VECTOR ( 'NONE', #26924, 1000.000000000000000 ) ;
#22816=CARTESIAN_POINT ( 'NONE',  ( -9.999999999999994671, 0.000000000000000000, 0.000000000000000000 ) ) ;
#22819=CARTESIAN_POINT ( 'NONE',  ( 0.000000000000000000, 18.53613841426789577, 48.58406706613910586 ) ) ;
#22826=AXIS2_PLACEMENT_3D ( 'NONE', #10585, #13298, #10763 ) ;
#22834=VERTEX_POINT ( 'NONE', #33206 ) ;
#22837=DIRECTION ( 'NONE',  ( 0.000000000000000000, 0.000000000000000000, 1.000000000000000000 ) ) ;
#22843=ORIENTED_EDGE ( 'NONE', *, *, #22303, .F. ) ;
#22861=CARTESIAN_POINT ( 'NONE',  ( 7.999999999999992895, 24.72041153920790180, -40.55929306992661765 ) ) ;
#22871=ADVANCED_FACE ( 'NONE', ( #16798 ), #14624, .T. ) ;
#22872=CYLINDRICAL_SURFACE ( 'NONE', #26422, 47.49900000000001654 ) ;
#22879=VERTEX_POINT ( 'NONE', #33725 ) ;
#22881=DIRECTION ( 'NONE',  ( -1.000000000000000000, 0.000000000000000000, 0.000000000000000000 ) ) ;
#22883=ORIENTED_EDGE ( 'NONE', *, *, #4071, .F. ) ;
#22886=DIRECTION ( 'NONE',  ( 1.000000000000000000, 0.000000000000000000, 0.000000000000000000 ) ) ;
#22888=ORIENTED_EDGE ( 'NONE', *, *, #25166, .T. ) ;
#22890=DIRECTION ( 'NONE',  ( 0.000000000000000000, -0.6845471059286794002, -0.7289686274214203232 ) ) ;
#22900=CIRCLE ( 'NONE', #17156, 47.49900000000000944 ) ;
#22905=EDGE_CURVE ( 'NONE', #32382, #7789, #14100, .T. ) ;
#22910=DIRECTION ( 'NONE',  ( 0.000000000000000000, 0.000000000000000000, 1.000000000000000000 ) ) ;
#22921=DIRECTION ( 'NONE',  ( 0.000000000000000000, -0.6845471059286952764, 0.7289686274214054462 ) ) ;
#22928=DIRECTION ( 'NONE',  ( 0.000000000000000000, 0.8443279255020126328, 0.5358267949790005424 ) ) ;
#22929=EDGE_LOOP ( 'NONE', ( #6416, #2561, #23168, #19952 ) ) ;
#22930=ORIENTED_EDGE ( 'NONE', *, *, #4225, .T. ) ;
#22933=ADVANCED_FACE ( 'NONE', ( #25821 ), #31735, .T. ) ;
#22937=LINE ( 'NONE', #30875, #19484 ) ;
#22938=EDGE_CURVE ( 'NONE', #5386, #128, #31197, .T. ) ;
#22942=CARTESIAN_POINT ( 'NONE',  ( 7.999999999999992895, 0.000000000000000000, 0.000000000000000000 ) ) ;
#22945=DIRECTION ( 'NONE',  ( 0.000000000000000000, -8.881784197001252323E-16, -1.000000000000000000 ) ) ;
#22956=FACE_OUTER_BOUND ( 'NONE', #11871, .T. ) ;
#22957=CARTESIAN_POINT ( 'NONE',  ( 0.000000000000000000, -39.55064067543080597, 25.36340625197344778 ) ) ;
#22959=DIRECTION ( 'NONE',  ( 0.000000000000000000, 0.000000000000000000, 1.000000000000000000 ) ) ;
#22960=CARTESIAN_POINT ( 'NONE',  ( 7.999999999999992895, 41.20225022064671805, -23.63323037071357646 ) ) ;
#22961=CYLINDRICAL_SURFACE ( 'NONE', #21263, 52.00000000000000711 ) ;
#22964=LINE ( 'NONE', #19889, #4321 ) ;
#22966=ORIENTED_EDGE ( 'NONE', *, *, #11943, .T. ) ;
#22972=ORIENTED_EDGE ( 'NONE', *, *, #4724, .T. ) ;
#22977=DIRECTION ( 'NONE',  ( 0.000000000000000000, 0.000000000000000000, 1.000000000000000000 ) ) ;
#22983=VERTEX_POINT ( 'NONE', #15334 ) ;
#23001=DIRECTION ( 'NONE',  ( -1.000000000000000000, -0.000000000000000000, -0.000000000000000000 ) ) ;
#23007=AXIS2_PLACEMENT_3D ( 'NONE', #7213, #16015, #1837 ) ;
#23009=CIRCLE ( 'NONE', #22439, 20.00000000000001421 ) ;
#23019=EDGE_CURVE ( 'NONE', #9731, #352, #34083, .T. ) ;
#23028=EDGE_CURVE ( 'NONE', #11969, #6500, #23641, .T. ) ;
#23029=FACE_OUTER_BOUND ( 'NONE', #21016, .T. ) ;
#23039=LINE ( 'NONE', #22861, #21714 ) ;
#23045=ORIENTED_EDGE ( 'NONE', *, *, #7214, .T. ) ;
#23076=ORIENTED_EDGE ( 'NONE', *, *, #17174, .T. ) ;
#23077=CARTESIAN_POINT ( 'NONE',  ( 0.000000000000000000, -0.6505223195679143977, -51.99593080916758936 ) ) ;
#23082=CIRCLE ( 'NONE', #2427, 20.00000000000000711 ) ;
#23087=CARTESIAN_POINT ( 'NONE',  ( 7.999999999999992895, -35.20873326984057883, -31.88259874184068465 ) ) ;
#23093=CARTESIAN_POINT ( 'NONE',  ( 7.999999999999992895, -24.72041153920704915, -40.55929306992714345 ) ) ;
#23097=DIRECTION ( 'NONE',  ( 0.000000000000000000, 0.000000000000000000, 1.000000000000000000 ) ) ;
#23103=CARTESIAN_POINT ( 'NONE',  ( 4.000000000000003553, -46.77034588191288833, -22.72740077717277885 ) ) ;
#23104=ORIENTED_EDGE ( 'NONE', *, *, #5170, .F. ) ;
#23112=AXIS2_PLACEMENT_3D ( 'NONE', #24419, #2469, #26961 ) ;
#23113=( NAMED_UNIT ( * ) PLANE_ANGLE_UNIT ( ) SI_UNIT ( $, .RADIAN. ) );
#23120=DIRECTION ( 'NONE',  ( 1.000000000000000000, 0.000000000000000000, 0.000000000000000000 ) ) ;
#23124=CARTESIAN_POINT ( 'NONE',  ( 7.999999999999992895, 0.000000000000000000, 0.000000000000000000 ) ) ;
#23126=LINE ( 'NONE', #26928, #32386 ) ;
#23131=CIRCLE ( 'NONE', #7613, 20.00000000000000711 ) ;
#23134=DIRECTION ( 'NONE',  ( 0.000000000000000000, -0.9980267284282708928, -0.06279051952932436509 ) ) ;
#23135=EDGE_CURVE ( 'NONE', #1926, #14743, #13397, .T. ) ;
#23146=CARTESIAN_POINT ( 'NONE',  ( 7.999999999999992895, 43.83938735307269496, 18.28286404005814703 ) ) ;
#23147=EDGE_LOOP ( 'NONE', ( #1846, #7690, #32495, #22270 ) ) ;
#23149=AXIS2_PLACEMENT_3D ( 'NONE', #19697, #17007, #28017 ) ;
#23153=ADVANCED_FACE ( 'NONE', ( #32277 ), #29935, .T. ) ;
#23163=VECTOR ( 'NONE', #17338, 1000.000000000000000 ) ;
#23168=ORIENTED_EDGE ( 'NONE', *, *, #12552, .F. ) ;
#23171=ORIENTED_EDGE ( 'NONE', *, *, #12100, .F. ) ;
#23173=AXIS2_PLACEMENT_3D ( 'NONE', #6258, #22619, #33612 ) ;
#23175=DIRECTION ( 'NONE',  ( -1.000000000000000000, 0.000000000000000000, 0.000000000000000000 ) ) ;
#23184=DIRECTION ( 'NONE',  ( 0.000000000000000000, -0.9980267284282708928, -0.06279051952932447611 ) ) ;
#23185=LINE ( 'NONE', #34180, #4973 ) ;
#23186=CARTESIAN_POINT ( 'NONE',  ( 0.000000000000000000, 7.162210897276456656, -51.50439529848821252 ) ) ;
#23189=CIRCLE ( 'NONE', #1931, 47.49900000000000944 ) ;
#23190=DIRECTION ( 'NONE',  ( -1.000000000000000000, 0.000000000000000000, 0.000000000000000000 ) ) ;
#23199=ORIENTED_EDGE ( 'NONE', *, *, #28778, .T. ) ;
#23207=DIRECTION ( 'NONE',  ( 1.000000000000000000, -0.000000000000000000, -0.000000000000000000 ) ) ;
#23215=CARTESIAN_POINT ( 'NONE',  ( 4.000000000000003553, -46.77034588191320097, 22.72740077717213936 ) ) ;
#23225=ORIENTED_EDGE ( 'NONE', *, *, #19126, .T. ) ;
#23227=CARTESIAN_POINT ( 'NONE',  ( 0.000000000000000000, 36.05989434073613609, 30.12041790338630776 ) ) ;
#23229=ORIENTED_EDGE ( 'NONE', *, *, #2694, .F. ) ;
#23233=ORIENTED_EDGE ( 'NONE', *, *, #15817, .T. ) ;
#23236=CIRCLE ( 'NONE', #30135, 20.00000000000000355 ) ;
#23247=CARTESIAN_POINT ( 'NONE',  ( 7.999999999999992895, -11.90021268425586953, 45.45261810511210143 ) ) ;
#23249=CARTESIAN_POINT ( 'NONE',  ( 0.000000000000000000, 0.000000000000000000, 0.000000000000000000 ) ) ;
#23251=ORIENTED_EDGE ( 'NONE', *, *, #1289, .F. ) ;
#23259=DIRECTION ( 'NONE',  ( -1.000000000000000000, 0.000000000000000000, 0.000000000000000000 ) ) ;
#23261=AXIS2_PLACEMENT_3D ( 'NONE', #16007, #2367, #20869 ) ;
#23263=DIRECTION ( 'NONE',  ( 1.000000000000000000, -0.000000000000000000, -0.000000000000000000 ) ) ;
#23269=ORIENTED_EDGE ( 'NONE', *, *, #13467, .T. ) ;
#23274=EDGE_CURVE ( 'NONE', #15107, #26850, #35252, .T. ) ;
#23286=VERTEX_POINT ( 'NONE', #7181 ) ;
#23288=SURFACE_STYLE_USAGE ( .BOTH. , #26008 ) ;
#23289=ORIENTED_EDGE ( 'NONE', *, *, #27271, .T. ) ;
#23294=EDGE_CURVE ( 'NONE', #3630, #27872, #32036, .T. ) ;
#23304=CIRCLE ( 'NONE', #11240, 20.00000000000000355 ) ;
#23308=EDGE_CURVE ( 'NONE', #27224, #31131, #1895, .T. ) ;
#23312=AXIS2_PLACEMENT_3D ( 'NONE', #26580, #20964, #12892 ) ;
#23317=CARTESIAN_POINT ( 'NONE',  ( 0.000000000000000000, -42.03146605346803000, 22.12489237027305577 ) ) ;
#23322=DIRECTION ( 'NONE',  ( 0.000000000000000000, 0.000000000000000000, 1.000000000000000000 ) ) ;
#23330=ORIENTED_EDGE ( 'NONE', *, *, #16687, .F. ) ;
#23332=ORIENTED_EDGE ( 'NONE', *, *, #18476, .F. ) ;
#23334=CARTESIAN_POINT ( 'NONE',  ( 4.000000000000003553, 30.03615769709734451, 42.44795908869000556 ) ) ;
#23336=FACE_OUTER_BOUND ( 'NONE', #30401, .T. ) ;
#23337=AXIS2_PLACEMENT_3D ( 'NONE', #22197, #25631, #958 ) ;
#23339=DIRECTION ( 'NONE',  ( -1.000000000000000000, 0.000000000000000000, 0.000000000000000000 ) ) ;
#23340=EDGE_LOOP ( 'NONE', ( #31159, #26178, #34976, #23045 ) ) ;
#23362=CARTESIAN_POINT ( 'NONE',  ( 7.999999999999992895, 27.79676263918186052, 37.88001506494778425 ) ) ;
#23365=CARTESIAN_POINT ( 'NONE',  ( 0.000000000000000000, 30.93515269692114344, 36.04401931830264516 ) ) ;
#23374=AXIS2_PLACEMENT_3D ( 'NONE', #15345, #17333, #11956 ) ;
#23380=VECTOR ( 'NONE', #11726, 1000.000000000000000 ) ;
#23383=CIRCLE ( 'NONE', #2162, 52.00000000000000711 ) ;
#23387=AXIS2_PLACEMENT_3D ( 'NONE', #2091, #31776, #23134 ) ;
#23388=EDGE_CURVE ( 'NONE', #7932, #7369, #24349, .T. ) ;
#23390=CIRCLE ( 'NONE', #31438, 20.00000000000000711 ) ;
#23392=ORIENTED_EDGE ( 'NONE', *, *, #29524, .F. ) ;
#23403=CARTESIAN_POINT ( 'NONE',  ( 0.000000000000000000, -46.19362259308826424, -8.585149169758999221 ) ) ;
#23406=DIRECTION ( 'NONE',  ( -1.000000000000000000, 0.000000000000000000, -0.000000000000000000 ) ) ;
#23412=ORIENTED_EDGE ( 'NONE', *, *, #20765, .F. ) ;
#23413=DIRECTION ( 'NONE',  ( -1.000000000000000000, -0.000000000000000000, -0.000000000000000000 ) ) ;
#23417=ORIENTED_EDGE ( 'NONE', *, *, #34979, .T. ) ;
#23420=EDGE_LOOP ( 'NONE', ( #20060, #27179, #26026, #2334 ) ) ;
#23431=AXIS2_PLACEMENT_3D ( 'NONE', #10294, #26860, #29735 ) ;
#23440=EDGE_CURVE ( 'NONE', #35265, #19439, #2173, .T. ) ;
#23441=FACE_OUTER_BOUND ( 'NONE', #1966, .T. ) ;
#23451=AXIS2_PLACEMENT_3D ( 'NONE', #34995, #32984, #5104 ) ;
#23462=DIRECTION ( 'NONE',  ( -1.000000000000000000, -0.000000000000000000, -0.000000000000000000 ) ) ;
#23477=VERTEX_POINT ( 'NONE', #2516 ) ;
#23481=VECTOR ( 'NONE', #5992, 1000.000000000000000 ) ;
#23486=CARTESIAN_POINT ( 'NONE',  ( 0.000000000000000000, 41.20225022064671805, -23.63323037071357646 ) ) ;
#23491=CARTESIAN_POINT ( 'NONE',  ( 7.999999999999992895, 0.000000000000000000, 0.000000000000000000 ) ) ;
#23493=ORIENTED_EDGE ( 'NONE', *, *, #15541, .F. ) ;
#23494=AXIS2_PLACEMENT_3D ( 'NONE', #621, #31227, #5860 ) ;
#23498=CARTESIAN_POINT ( 'NONE',  ( 7.999999999999992895, 0.000000000000000000, 0.000000000000000000 ) ) ;
#23501=CIRCLE ( 'NONE', #19465, 20.00000000000000711 ) ;
#23503=DIRECTION ( 'NONE',  ( -1.000000000000000000, -0.000000000000000000, -0.000000000000000000 ) ) ;
#23506=ORIENTED_EDGE ( 'NONE', *, *, #27315, .T. ) ;
#23508=PLANE ( 'NONE',  #6636 ) ;
#23510=ORIENTED_EDGE ( 'NONE', *, *, #26040, .T. ) ;
#23528=CARTESIAN_POINT ( 'NONE',  ( 7.999999999999992895, -38.92705108641750655, 27.21837053747785973 ) ) ;
#23531=ORIENTED_EDGE ( 'NONE', *, *, #27539, .F. ) ;
#23533=DIRECTION ( 'NONE',  ( -1.000000000000000000, 0.000000000000000000, -0.000000000000000000 ) ) ;
#23534=FACE_OUTER_BOUND ( 'NONE', #34045, .T. ) ;
#23542=CARTESIAN_POINT ( 'NONE',  ( 0.000000000000000000, 0.6505223195682995341, 51.99593080916758936 ) ) ;
#23544=FILL_AREA_STYLE_COLOUR ( '', #10354 ) ;
#23555=DIRECTION ( 'NONE',  ( 0.000000000000000000, 0.9048270524660175784, 0.4257792915650767673 ) ) ;
#23560=AXIS2_PLACEMENT_3D ( 'NONE', #503, #30569, #17046 ) ;
#23561=VERTEX_POINT ( 'NONE', #24294 ) ;
#23563=CARTESIAN_POINT ( 'NONE',  ( 0.000000000000000000, 0.000000000000000000, 0.000000000000000000 ) ) ;
#23565=CARTESIAN_POINT ( 'NONE',  ( 7.999999999999992895, 46.90537658765329354, 2.727856614654466938 ) ) ;
#23569=EDGE_LOOP ( 'NONE', ( #18941, #7776, #9388, #32494 ) ) ;
#23573=EDGE_CURVE ( 'NONE', #11680, #16904, #18001, .T. ) ;
#23578=CIRCLE ( 'NONE', #29915, 52.00000000000000711 ) ;
#23590=CARTESIAN_POINT ( 'NONE',  ( 7.999999999999992895, 0.000000000000000000, 0.000000000000000000 ) ) ;
#23596=FACE_OUTER_BOUND ( 'NONE', #5070, .T. ) ;
#23600=ORIENTED_EDGE ( 'NONE', *, *, #21765, .F. ) ;
#23605=CIRCLE ( 'NONE', #12082, 52.00000000000000711 ) ;
#23612=ORIENTED_EDGE ( 'NONE', *, *, #18476, .T. ) ;
#23614=EDGE_CURVE ( 'NONE', #2022, #423, #2514, .T. ) ;
#23618=ADVANCED_FACE ( 'NONE', ( #5901 ), #25352, .T. ) ;
#23622=ORIENTED_EDGE ( 'NONE', *, *, #28647, .T. ) ;
#23636=CYLINDRICAL_SURFACE ( 'NONE', #16416, 47.49900000000001654 ) ;
#23639=CIRCLE ( 'NONE', #25930, 20.00000000000000711 ) ;
#23640=CYLINDRICAL_SURFACE ( 'NONE', #16549, 52.00000000000000711 ) ;
#23641=LINE ( 'NONE', #34628, #19684 ) ;
#23642=VECTOR ( 'NONE', #23207, 1000.000000000000000 ) ;
#23654=ORIENTED_EDGE ( 'NONE', *, *, #11492, .F. ) ;
#23666=STYLED_ITEM ( 'NONE', ( #20218 ), #6921 ) ;
#23671=LINE ( 'NONE', #34298, #21846 ) ;
#23674=DIRECTION ( 'NONE',  ( 0.000000000000000000, 0.000000000000000000, 1.000000000000000000 ) ) ;
#23681=DIRECTION ( 'NONE',  ( 0.000000000000000000, -0.4817536741017223179, 0.8763066800438598092 ) ) ;
#23690=CIRCLE ( 'NONE', #27707, 52.00000000000000711 ) ;
#23692=DIRECTION ( 'NONE',  ( -1.000000000000000000, 0.000000000000000000, 0.000000000000000000 ) ) ;
#23695=DIRECTION ( 'NONE',  ( -1.000000000000000000, -0.000000000000000000, -0.000000000000000000 ) ) ;
#23704=DIRECTION ( 'NONE',  ( 0.000000000000000000, 0.000000000000000000, 1.000000000000000000 ) ) ;
#23709=AXIS2_PLACEMENT_3D ( 'NONE', #21085, #29750, #32090 ) ;
#23711=AXIS2_PLACEMENT_3D ( 'NONE', #18836, #5176, #15948 ) ;
#23712=ORIENTED_EDGE ( 'NONE', *, *, #18957, .T. ) ;
#23713=CARTESIAN_POINT ( 'NONE',  ( 0.000000000000000000, 0.000000000000000000, 0.000000000000000000 ) ) ;
#23714=DIRECTION ( 'NONE',  ( 0.000000000000000000, 0.000000000000000000, 1.000000000000000000 ) ) ;
#23725=DIRECTION ( 'NONE',  ( -1.000000000000000000, 0.000000000000000000, -0.000000000000000000 ) ) ;
#23729=DIRECTION ( 'NONE',  ( -1.000000000000000000, 0.000000000000000000, -0.000000000000000000 ) ) ;
#23741=ORIENTED_EDGE ( 'NONE', *, *, #10320, .F. ) ;
#23742=ORIENTED_EDGE ( 'NONE', *, *, #30871, .F. ) ;
#23753=DIRECTION ( 'NONE',  ( 0.000000000000000000, 0.000000000000000000, 1.000000000000000000 ) ) ;
#23756=FACE_OUTER_BOUND ( 'NONE', #6731, .T. ) ;
#23768=CARTESIAN_POINT ( 'NONE',  ( 7.999999999999992895, 0.000000000000000000, 0.000000000000000000 ) ) ;
#23769=ORIENTED_EDGE ( 'NONE', *, *, #11845, .T. ) ;
#23770=DIRECTION ( 'NONE',  ( 0.000000000000000000, -0.7705132427757815927, -0.6374239897486989603 ) ) ;
#23782=VERTEX_POINT ( 'NONE', #19919 ) ;
#23783=AXIS2_PLACEMENT_3D ( 'NONE', #23491, #31591, #34842 ) ;
#23785=CARTESIAN_POINT ( 'NONE',  ( 7.999999999999992895, 19.44205635905542451, 43.33776004284616334 ) ) ;
#23788=VERTEX_POINT ( 'NONE', #3752 ) ;
#23790=EDGE_CURVE ( 'NONE', #32535, #8148, #26094, .T. ) ;
#23794=VECTOR ( 'NONE', #14660, 1000.000000000000000 ) ;
#23796=ORIENTED_EDGE ( 'NONE', *, *, #11639, .F. ) ;
#23803=CARTESIAN_POINT ( 'NONE',  ( 7.999999999999992895, 0.000000000000000000, 0.000000000000000000 ) ) ;
#23804=ORIENTED_EDGE ( 'NONE', *, *, #33030, .T. ) ;
#23805=ORIENTED_EDGE ( 'NONE', *, *, #28806, .T. ) ;
#23806=DIRECTION ( 'NONE',  ( 0.000000000000000000, 0.000000000000000000, 1.000000000000000000 ) ) ;
#23809=CIRCLE ( 'NONE', #27821, 20.00000000000000711 ) ;
#23817=VECTOR ( 'NONE', #19148, 1000.000000000000000 ) ;
#23818=ADVANCED_FACE ( 'NONE', ( #16875 ), #25721, .T. ) ;
#23819=VERTEX_POINT ( 'NONE', #11659 ) ;
#23822=CARTESIAN_POINT ( 'NONE',  ( 0.000000000000000000, 0.000000000000000000, 0.000000000000000000 ) ) ;
#23836=ORIENTED_EDGE ( 'NONE', *, *, #16068, .F. ) ;
#23839=ORIENTED_EDGE ( 'NONE', *, *, #16095, .T. ) ;
#23848=ADVANCED_FACE ( 'NONE', ( #28236 ), #3576, .T. ) ;
#23859=CARTESIAN_POINT ( 'NONE',  ( 7.999999999999992895, 0.000000000000000000, 0.000000000000000000 ) ) ;
#23863=LINE ( 'NONE', #32314, #34336 ) ;
#23865=CARTESIAN_POINT ( 'NONE',  ( 7.999999999999992895, -46.90537658765327933, -2.727856614654800005 ) ) ;
#23866=DIRECTION ( 'NONE',  ( -1.000000000000000000, 0.000000000000000000, 0.000000000000000000 ) ) ;
#23868=AXIS2_PLACEMENT_3D ( 'NONE', #8441, #685, #6271 ) ;
#23869=DIRECTION ( 'NONE',  ( 0.000000000000000000, 0.4817536741017101609, 0.8763066800438663595 ) ) ;
#23874=DIRECTION ( 'NONE',  ( 0.000000000000000000, 0.000000000000000000, -1.000000000000000000 ) ) ;
#23875=DIRECTION ( 'NONE',  ( 0.000000000000000000, 0.9980267284282713369, 0.06279051952931692659 ) ) ;
#23876=VECTOR ( 'NONE', #32901, 1000.000000000000000 ) ;
#23877=ORIENTED_EDGE ( 'NONE', *, *, #31134, .F. ) ;
#23884=VERTEX_POINT ( 'NONE', #31288 ) ;
#23886=AXIS2_PLACEMENT_3D ( 'NONE', #17502, #9407, #11752 ) ;
#23892=ORIENTED_EDGE ( 'NONE', *, *, #22303, .T. ) ;
#23894=EDGE_CURVE ( 'NONE', #19390, #31137, #29550, .T. ) ;
#23898=VERTEX_POINT ( 'NONE', #17944 ) ;
#23901=DIRECTION ( 'NONE',  ( -1.000000000000000000, -0.000000000000000000, 0.000000000000000000 ) ) ;
#23902=CARTESIAN_POINT ( 'NONE',  ( 50.00005079999998969, 10.58300524425836109, 3.000000000000002665 ) ) ;
#23910=CYLINDRICAL_SURFACE ( 'NONE', #33711, 20.00000000000000355 ) ;
#23912=DIRECTION ( 'NONE',  ( 0.000000000000000000, -0.6845471059286792892, -0.7289686274214203232 ) ) ;
#23916=DIRECTION ( 'NONE',  ( -0.000000000000000000, 0.000000000000000000, 1.000000000000000000 ) ) ;
#23925=ORIENTED_EDGE ( 'NONE', *, *, #25683, .F. ) ;
#23927=CIRCLE ( 'NONE', #23337, 52.00000000000000711 ) ;
#23929=CIRCLE ( 'NONE', #22108, 11.00000000000000000 ) ;
#23935=ORIENTED_EDGE ( 'NONE', *, *, #5165, .T. ) ;
#23942=FACE_OUTER_BOUND ( 'NONE', #25056, .T. ) ;
#23955=CYLINDRICAL_SURFACE ( 'NONE', #389, 47.49900000000001654 ) ;
#23957=CARTESIAN_POINT ( 'NONE',  ( 0.000000000000000000, 30.93515269692163372, -36.04401931830219752 ) ) ;
#23958=CARTESIAN_POINT ( 'NONE',  ( 7.999999999999992895, 44.61570720899074161, 14.73072383765644489 ) ) ;
#23965=VECTOR ( 'NONE', #1015, 1000.000000000000000 ) ;
#23972=LINE ( 'NONE', #18195, #4464 ) ;
#23973=AXIS2_PLACEMENT_3D ( 'NONE', #20158, #17112, #19982 ) ;
#23974=CARTESIAN_POINT ( 'NONE',  ( 7.999999999999992895, 44.47301969247445896, 16.68249143361927267 ) ) ;
#23976=ORIENTED_EDGE ( 'NONE', *, *, #4443, .F. ) ;
#23977=CYLINDRICAL_SURFACE ( 'NONE', #28599, 52.00000000000000711 ) ;
#23981=ORIENTED_EDGE ( 'NONE', *, *, #7748, .F. ) ;
#23983=CIRCLE ( 'NONE', #11911, 20.00000000000000000 ) ;
#23992=VECTOR ( 'NONE', #10362, 1000.000000000000000 ) ;
#23995=CARTESIAN_POINT ( 'NONE',  ( 7.999999999999992895, 32.32520163883631170, -34.09746168776000985 ) ) ;
#24012=VECTOR ( 'NONE', #33136, 1000.000000000000000 ) ;
#24027=VECTOR ( 'NONE', #2618, 1000.000000000000000 ) ;
#24030=EDGE_LOOP ( 'NONE', ( #13701, #24839, #23976, #10293 ) ) ;
#24041=CYLINDRICAL_SURFACE ( 'NONE', #17259, 20.00000000000000355 ) ;
#24044=VECTOR ( 'NONE', #21204, 1000.000000000000000 ) ;
#24058=CARTESIAN_POINT ( 'NONE',  ( 0.000000000000000000, 47.49120266317496686, 0.8606222198176832761 ) ) ;
#24059=DIRECTION ( 'NONE',  ( -1.000000000000000000, -0.000000000000000000, 0.000000000000000000 ) ) ;
#24061=AXIS2_PLACEMENT_3D ( 'NONE', #15099, #1626, #31514 ) ;
#24063=DIRECTION ( 'NONE',  ( -1.000000000000000000, 0.000000000000000000, 0.000000000000000000 ) ) ;
#24070=DIRECTION ( 'NONE',  ( 0.000000000000000000, 0.000000000000000000, 1.000000000000000000 ) ) ;
#24084=ORIENTED_EDGE ( 'NONE', *, *, #2972, .T. ) ;
#24092=VECTOR ( 'NONE', #9797, 1000.000000000000000 ) ;
#24104=CARTESIAN_POINT ( 'NONE',  ( 7.999999999999992895, -3.840921266750157326, 47.34345070675169609 ) ) ;
#24105=CARTESIAN_POINT ( 'NONE',  ( 0.000000000000000000, 0.000000000000000000, 0.000000000000000000 ) ) ;
#24109=EDGE_CURVE ( 'NONE', #4840, #25508, #8267, .T. ) ;
#24110=CARTESIAN_POINT ( 'NONE',  ( 0.000000000000000000, 42.03146605346819342, -22.12489237027273603 ) ) ;
#24117=CARTESIAN_POINT ( 'NONE',  ( 0.000000000000000000, 0.000000000000000000, 0.000000000000000000 ) ) ;
#24119=ORIENTED_EDGE ( 'NONE', *, *, #4084, .F. ) ;
#24122=CYLINDRICAL_SURFACE ( 'NONE', #578, 47.49900000000001654 ) ;
#24124=CARTESIAN_POINT ( 'NONE',  ( 7.999999999999992895, 46.77034588191337861, -22.72740077717178053 ) ) ;
#24127=CARTESIAN_POINT ( 'NONE',  ( 7.999999999999992895, 0.000000000000000000, 0.000000000000000000 ) ) ;
#24129=CARTESIAN_POINT ( 'NONE',  ( 0.000000000000000000, 0.000000000000000000, 0.000000000000000000 ) ) ;
#24133=DIRECTION ( 'NONE',  ( -1.000000000000000000, 0.000000000000000000, -0.000000000000000000 ) ) ;
#24136=DIRECTION ( 'NONE',  ( 0.000000000000000000, 0.000000000000000000, 1.000000000000000000 ) ) ;
#24137=ORIENTED_EDGE ( 'NONE', *, *, #9480, .T. ) ;
#24140=AXIS2_PLACEMENT_3D ( 'NONE', #29495, #34540, #34907 ) ;
#24143=ORIENTED_EDGE ( 'NONE', *, *, #20937, .F. ) ;
#24147=VERTEX_POINT ( 'NONE', #16435 ) ;
#24154=EDGE_CURVE ( 'NONE', #11680, #9813, #5833, .T. ) ;
#24157=ORIENTED_EDGE ( 'NONE', *, *, #34559, .F. ) ;
#24163=CIRCLE ( 'NONE', #30488, 52.00000000000000711 ) ;
#24170=CARTESIAN_POINT ( 'NONE',  ( 7.999999999999992895, -42.41764978026620270, 20.20639853260275487 ) ) ;
#24173=ORIENTED_EDGE ( 'NONE', *, *, #9885, .T. ) ;
#24174=CIRCLE ( 'NONE', #8632, 47.49900000000002365 ) ;
#24184=EDGE_CURVE ( 'NONE', #8054, #33836, #16295, .T. ) ;
#24197=ORIENTED_EDGE ( 'NONE', *, *, #15650, .T. ) ;
#24198=ORIENTED_EDGE ( 'NONE', *, *, #14848, .F. ) ;
#24223=DIRECTION ( 'NONE',  ( -1.000000000000000000, 0.000000000000000000, 0.000000000000000000 ) ) ;
#24224=EDGE_CURVE ( 'NONE', #8679, #9355, #12306, .T. ) ;
#24228=CIRCLE ( 'NONE', #635, 20.00000000000000000 ) ;
#24232=ORIENTED_EDGE ( 'NONE', *, *, #15449, .T. ) ;
#24233=EDGE_LOOP ( 'NONE', ( #17933, #8191, #9084, #10979 ) ) ;
#24237=EDGE_LOOP ( 'NONE', ( #10079, #30207, #317, #12362 ) ) ;
#24239=EDGE_CURVE ( 'NONE', #12895, #574, #24397, .T. ) ;
#24240=ORIENTED_EDGE ( 'NONE', *, *, #27776, .T. ) ;
#24241=CIRCLE ( 'NONE', #14440, 20.00000000000000711 ) ;
#24242=AXIS2_PLACEMENT_3D ( 'NONE', #24117, #10058, #18515 ) ;
#24245=ORIENTED_EDGE ( 'NONE', *, *, #3, .T. ) ;
#24253=CARTESIAN_POINT ( 'NONE',  ( 7.999999999999992895, 0.000000000000000000, 0.000000000000000000 ) ) ;
#24257=DIRECTION ( 'NONE',  ( -1.000000000000000000, 0.000000000000000000, -0.000000000000000000 ) ) ;
#24265=CARTESIAN_POINT ( 'NONE',  ( 0.000000000000000000, -46.87740477351715640, -3.172455868805712509 ) ) ;
#24277=CARTESIAN_POINT ( 'NONE',  ( 7.999999999999992895, -42.60732521687585006, 19.80331771201643321 ) ) ;
#24283=ORIENTED_EDGE ( 'NONE', *, *, #27645, .F. ) ;
#24294=CARTESIAN_POINT ( 'NONE',  ( 7.999999999999992895, 1.347111479062088405E-15, -11.00000000000000000 ) ) ;
#24300=ADVANCED_FACE ( 'NONE', ( #22730 ), #15150, .T. ) ;
#24302=ADVANCED_FACE ( 'NONE', ( #28325 ), #12474, .T. ) ;
#24305=DIRECTION ( 'NONE',  ( -1.000000000000000000, -0.000000000000000000, -0.000000000000000000 ) ) ;
#24309=ORIENTED_EDGE ( 'NONE', *, *, #24239, .T. ) ;
#24312=ORIENTED_EDGE ( 'NONE', *, *, #30173, .T. ) ;
#24316=VECTOR ( 'NONE', #24737, 1000.000000000000000 ) ;
#24322=DIRECTION ( 'NONE',  ( -1.000000000000000000, -0.000000000000000000, -0.000000000000000000 ) ) ;
#24328=DIRECTION ( 'NONE',  ( -1.000000000000000000, 0.000000000000000000, -0.000000000000000000 ) ) ;
#24331=ORIENTED_EDGE ( 'NONE', *, *, #7688, .F. ) ;
#24334=DIRECTION ( 'NONE',  ( -1.000000000000000000, 0.000000000000000000, 0.000000000000000000 ) ) ;
#24338=FACE_OUTER_BOUND ( 'NONE', #10459, .T. ) ;
#24339=VECTOR ( 'NONE', #30697, 1000.000000000000000 ) ;
#24342=EDGE_CURVE ( 'NONE', #7666, #22879, #2049, .T. ) ;
#24349=CIRCLE ( 'NONE', #7648, 52.00000000000000711 ) ;
#24356=ORIENTED_EDGE ( 'NONE', *, *, #27764, .T. ) ;
#24359=AXIS2_PLACEMENT_3D ( 'NONE', #22073, #24963, #22245 ) ;
#24367=ORIENTED_EDGE ( 'NONE', *, *, #25127, .T. ) ;
#24368=EDGE_LOOP ( 'NONE', ( #28081, #28269, #3518, #16851 ) ) ;
#24372=AXIS2_PLACEMENT_3D ( 'NONE', #22816, #28410, #6612 ) ;
#24374=ORIENTED_EDGE ( 'NONE', *, *, #13656, .T. ) ;
#24385=CARTESIAN_POINT ( 'NONE',  ( 7.999999999999992895, 0.000000000000000000, 0.000000000000000000 ) ) ;
#24387=DIRECTION ( 'NONE',  ( -1.000000000000000000, 0.000000000000000000, -0.000000000000000000 ) ) ;
#24393=CYLINDRICAL_SURFACE ( 'NONE', #1014, 20.00000000000000355 ) ;
#24397=CIRCLE ( 'NONE', #8854, 11.00000000000000000 ) ;
#24409=CIRCLE ( 'NONE', #13483, 20.00000000000000711 ) ;
#24410=CARTESIAN_POINT ( 'NONE',  ( 7.999999999999992895, 0.000000000000000000, 0.000000000000000000 ) ) ;
#24419=CARTESIAN_POINT ( 'NONE',  ( 0.000000000000000000, 44.75336757549778355, 14.30704879393622520 ) ) ;
#24428=DIRECTION ( 'NONE',  ( 0.000000000000000000, -0.2486898871648415554, -0.9685831611286345177 ) ) ;
#24429=VECTOR ( 'NONE', #24981, 1000.000000000000000 ) ;
#24438=DIRECTION ( 'NONE',  ( 0.000000000000000000, 0.000000000000000000, 1.000000000000000000 ) ) ;
#24439=CARTESIAN_POINT ( 'NONE',  ( 7.999999999999992895, 0.000000000000000000, 0.000000000000000000 ) ) ;
#24441=( LENGTH_UNIT ( ) NAMED_UNIT ( * ) SI_UNIT ( .MILLI., .METRE. ) );
#24449=ORIENTED_EDGE ( 'NONE', *, *, #22694, .F. ) ;
#24452=ORIENTED_EDGE ( 'NONE', *, *, #31327, .F. ) ;
#24457=LINE ( 'NONE', #11129, #14811 ) ;
#24461=ORIENTED_EDGE ( 'NONE', *, *, #19956, .F. ) ;
#24462=ORIENTED_EDGE ( 'NONE', *, *, #31271, .F. ) ;
#24469=DIRECTION ( 'NONE',  ( -1.000000000000000000, -0.000000000000000000, 0.000000000000000000 ) ) ;
#24475=CARTESIAN_POINT ( 'NONE',  ( 7.999999999999992895, 11.90021268425617329, -45.45261810511203038 ) ) ;
#24484=DIRECTION ( 'NONE',  ( 0.000000000000000000, -0.2486898871648622888, 0.9685831611286290777 ) ) ;
#24492=AXIS2_PLACEMENT_3D ( 'NONE', #25643, #25830, #437 ) ;
#24497=ORIENTED_EDGE ( 'NONE', *, *, #11974, .T. ) ;
#24499=EDGE_CURVE ( 'NONE', #18878, #29834, #1678, .T. ) ;
#24514=DIRECTION ( 'NONE',  ( -1.000000000000000000, -0.000000000000000000, -0.000000000000000000 ) ) ;
#24522=CARTESIAN_POINT ( 'NONE',  ( 7.999999999999992895, 0.000000000000000000, 0.000000000000000000 ) ) ;
#24530=DIRECTION ( 'NONE',  ( -1.000000000000000000, -0.000000000000000000, -0.000000000000000000 ) ) ;
#24532=DIRECTION ( 'NONE',  ( -1.000000000000000000, -0.000000000000000000, 0.000000000000000000 ) ) ;
#24534=ORIENTED_EDGE ( 'NONE', *, *, #22447, .F. ) ;
#24535=CARTESIAN_POINT ( 'NONE',  ( 7.999999999999992895, -46.21320724403641833, -10.97699764142004497 ) ) ;
#24543=ADVANCED_FACE ( 'NONE', ( #16039 ), #32623, .T. ) ;
#24544=ORIENTED_EDGE ( 'NONE', *, *, #30713, .T. ) ;
#24549=ORIENTED_EDGE ( 'NONE', *, *, #31642, .F. ) ;
#24561=CIRCLE ( 'NONE', #15327, 20.00000000000000355 ) ;
#24562=AXIS2_PLACEMENT_3D ( 'NONE', #24385, #29967, #22023 ) ;
#24570=VECTOR ( 'NONE', #35181, 1000.000000000000000 ) ;
#24572=LINE ( 'NONE', #29976, #23817 ) ;
#24574=ORIENTED_EDGE ( 'NONE', *, *, #10563, .F. ) ;
#24583=CARTESIAN_POINT ( 'NONE',  ( -9.999999999999994671, 0.000000000000000000, 0.000000000000000000 ) ) ;
#24585=CARTESIAN_POINT ( 'NONE',  ( 0.000000000000000000, -42.41764978026620270, 20.20639853260275487 ) ) ;
#24589=VECTOR ( 'NONE', #32714, 1000.000000000000000 ) ;
#24590=VERTEX_POINT ( 'NONE', #2575 ) ;
#24592=DIRECTION ( 'NONE',  ( -1.000000000000000000, -0.000000000000000000, -0.000000000000000000 ) ) ;
#24594=DIRECTION ( 'NONE',  ( 0.000000000000000000, 0.000000000000000000, 1.000000000000000000 ) ) ;
#24598=VERTEX_POINT ( 'NONE', #10847 ) ;
#24602=CIRCLE ( 'NONE', #2769, 20.00000000000000711 ) ;
#24608=DIRECTION ( 'NONE',  ( -1.000000000000000000, 0.000000000000000000, -0.000000000000000000 ) ) ;
#24611=AXIS2_PLACEMENT_3D ( 'NONE', #18223, #34264, #1313 ) ;
#24625=CIRCLE ( 'NONE', #9088, 20.00000000000000355 ) ;
#24627=CARTESIAN_POINT ( 'NONE',  ( 0.000000000000000000, -43.83938735307282997, 18.28286404005782728 ) ) ;
#24629=ORIENTED_EDGE ( 'NONE', *, *, #25863, .F. ) ;
#24631=EDGE_CURVE ( 'NONE', #4840, #6112, #5441, .T. ) ;
#24634=ORIENTED_EDGE ( 'NONE', *, *, #27329, .F. ) ;
#24636=ORIENTED_EDGE ( 'NONE', *, *, #12876, .F. ) ;
#24640=VECTOR ( 'NONE', #2755, 1000.000000000000000 ) ;
#24643=ORIENTED_EDGE ( 'NONE', *, *, #4651, .F. ) ;
#24659=DIRECTION ( 'NONE',  ( -1.000000000000000000, -0.000000000000000000, 0.000000000000000000 ) ) ;
#24660=DIRECTION ( 'NONE',  ( 1.000000000000000000, -0.000000000000000000, 0.000000000000000000 ) ) ;
#24662=ORIENTED_EDGE ( 'NONE', *, *, #11126, .F. ) ;
#24666=CYLINDRICAL_SURFACE ( 'NONE', #20362, 47.49900000000001654 ) ;
#24679=ORIENTED_EDGE ( 'NONE', *, *, #16239, .F. ) ;
#24681=DIRECTION ( 'NONE',  ( -1.000000000000000000, -0.000000000000000000, -0.000000000000000000 ) ) ;
#24684=ADVANCED_FACE ( 'NONE', ( #13542 ), #5961, .T. ) ;
#24699=AXIS2_PLACEMENT_3D ( 'NONE', #6831, #15093, #28446 ) ;
#24708=EDGE_CURVE ( 'NONE', #30567, #21603, #11370, .T. ) ;
#24718=EDGE_CURVE ( 'NONE', #9669, #15756, #17461, .T. ) ;
#24719=CARTESIAN_POINT ( 'NONE',  ( 7.999999999999992895, -47.32430374665948136, 21.55018039121511819 ) ) ;
#24720=ORIENTED_EDGE ( 'NONE', *, *, #7739, .F. ) ;
#24727=STYLED_ITEM ( 'NONE', ( #35609 ), #10310 ) ;
#24737=DIRECTION ( 'NONE',  ( 1.000000000000000000, -0.000000000000000000, 0.000000000000000000 ) ) ;
#24739=CARTESIAN_POINT ( 'NONE',  ( 7.999999999999992895, -47.22458491092824318, 5.098390039074071289 ) ) ;
#24749=ORIENTED_EDGE ( 'NONE', *, *, #4921, .T. ) ;
#24762=EDGE_CURVE ( 'NONE', #29218, #32215, #2642, .T. ) ;
#24763=EDGE_CURVE ( 'NONE', #26196, #10004, #20424, .T. ) ;
#24766=ORIENTED_EDGE ( 'NONE', *, *, #264, .T. ) ;
#24767=CARTESIAN_POINT ( 'NONE',  ( 0.000000000000000000, 0.000000000000000000, 0.000000000000000000 ) ) ;
#24769=DIRECTION ( 'NONE',  ( 0.000000000000000000, -0.7705132427757949154, 0.6374239897486827511 ) ) ;
#24783=DIRECTION ( 'NONE',  ( -1.000000000000000000, 0.000000000000000000, -0.000000000000000000 ) ) ;
#24784=FACE_OUTER_BOUND ( 'NONE', #18464, .T. ) ;
#24788=EDGE_CURVE ( 'NONE', #3037, #27614, #33652, .T. ) ;
#24799=AXIS2_PLACEMENT_3D ( 'NONE', #9913, #28658, #20876 ) ;
#24806=ORIENTED_EDGE ( 'NONE', *, *, #1333, .T. ) ;
#24811=ORIENTED_EDGE ( 'NONE', *, *, #19865, .T. ) ;
#24813=CARTESIAN_POINT ( 'NONE',  ( -9.999999999999994671, 0.000000000000000000, 0.000000000000000000 ) ) ;
#24817=ORIENTED_EDGE ( 'NONE', *, *, #10323, .F. ) ;
#24822=ORIENTED_EDGE ( 'NONE', *, *, #6179, .T. ) ;
#24823=VECTOR ( 'NONE', #8240, 1000.000000000000000 ) ;
#24824=DIRECTION ( 'NONE',  ( -1.000000000000000000, -0.000000000000000000, -0.000000000000000000 ) ) ;
#24829=DIRECTION ( 'NONE',  ( 0.000000000000000000, -0.4817536741017036661, -0.8763066800438699122 ) ) ;
#24833=CARTESIAN_POINT ( 'NONE',  ( 4.000000000000003553, 0.6505223195690454929, -51.99593080916758936 ) ) ;
#24839=ORIENTED_EDGE ( 'NONE', *, *, #28647, .F. ) ;
#24843=ORIENTED_EDGE ( 'NONE', *, *, #24631, .T. ) ;
#24847=ORIENTED_EDGE ( 'NONE', *, *, #24788, .T. ) ;
#24854=CARTESIAN_POINT ( 'NONE',  ( 7.999999999999992895, 27.43636312076375461, -38.14186064215119387 ) ) ;
#24858=ORIENTED_EDGE ( 'NONE', *, *, #10982, .F. ) ;
#24862=FACE_OUTER_BOUND ( 'NONE', #23147, .T. ) ;
#24878=ORIENTED_EDGE ( 'NONE', *, *, #25380, .F. ) ;
#24881=DIRECTION ( 'NONE',  ( -1.000000000000000000, 0.000000000000000000, 0.000000000000000000 ) ) ;
#24883=EDGE_CURVE ( 'NONE', #21916, #30516, #28111, .T. ) ;
#24891=CARTESIAN_POINT ( 'NONE',  ( 4.000000000000003553, -43.55304910509385508, -28.41006711800031326 ) ) ;
#24892=VERTEX_POINT ( 'NONE', #3453 ) ;
#24893=DIRECTION ( 'NONE',  ( 0.000000000000000000, -0.9980267284282723361, 0.06279051952930261860 ) ) ;
#24910=VECTOR ( 'NONE', #20947, 1000.000000000000000 ) ;
#24911=ADVANCED_FACE ( 'NONE', ( #4874 ), #7389, .T. ) ;
#24923=CIRCLE ( 'NONE', #7099, 20.00000000000000711 ) ;
#24926=DIRECTION ( 'NONE',  ( 0.000000000000000000, 0.000000000000000000, -1.000000000000000000 ) ) ;
#24927=DIRECTION ( 'NONE',  ( -1.000000000000000000, -0.000000000000000000, 0.000000000000000000 ) ) ;
#24939=CIRCLE ( 'NONE', #7112, 52.00000000000000711 ) ;
#24951=EDGE_CURVE ( 'NONE', #22316, #30516, #17556, .T. ) ;
#24956=LINE ( 'NONE', #14131, #570 ) ;
#24958=EDGE_CURVE ( 'NONE', #16010, #26553, #7212, .T. ) ;
#24959=CARTESIAN_POINT ( 'NONE',  ( 0.000000000000000000, 0.000000000000000000, 3.000000000000002665 ) ) ;
#24960=EDGE_CURVE ( 'NONE', #1374, #21589, #31940, .T. ) ;
#24961=DIRECTION ( 'NONE',  ( -1.000000000000000000, 0.000000000000000000, 0.000000000000000000 ) ) ;
#24962=CARTESIAN_POINT ( 'NONE',  ( 7.999999999999992895, 45.78515115856061612, -12.64416602183615623 ) ) ;
#24963=DIRECTION ( 'NONE',  ( -1.000000000000000000, -0.000000000000000000, 0.000000000000000000 ) ) ;
#24966=FACE_OUTER_BOUND ( 'NONE', #7210, .T. ) ;
#24973=ORIENTED_EDGE ( 'NONE', *, *, #9512, .T. ) ;
#24981=DIRECTION ( 'NONE',  ( -1.000000000000000000, 0.000000000000000000, 0.000000000000000000 ) ) ;
#24995=DIRECTION ( 'NONE',  ( -1.000000000000000000, 0.000000000000000000, -0.000000000000000000 ) ) ;
#25009=DIRECTION ( 'NONE',  ( 0.000000000000000000, 0.000000000000000000, -1.000000000000000000 ) ) ;
#25018=VERTEX_POINT ( 'NONE', #34758 ) ;
#25024=CIRCLE ( 'NONE', #14087, 20.00000000000000711 ) ;
#25027=ADVANCED_FACE ( 'NONE', ( #31684 ), #32053, .T. ) ;
#25030=VERTEX_POINT ( 'NONE', #23957 ) ;
#25031=DIRECTION ( 'NONE',  ( 0.000000000000000000, -0.3681245526846654292, -0.9297764858882563432 ) ) ;
#25035=ORIENTED_EDGE ( 'NONE', *, *, #3495, .F. ) ;
#25039=ORIENTED_EDGE ( 'NONE', *, *, #14732, .T. ) ;
#25053=DIRECTION ( 'NONE',  ( -1.000000000000000000, 0.000000000000000000, 0.000000000000000000 ) ) ;
#25054=CARTESIAN_POINT ( 'NONE',  ( 7.999999999999992895, -27.79676263918213763, 37.88001506494759241 ) ) ;
#25056=EDGE_LOOP ( 'NONE', ( #33562, #3593, #25205, #26409 ) ) ;
#25063=EDGE_LOOP ( 'NONE', ( #15073, #19642, #26009, #6125 ) ) ;
#25073=ORIENTED_EDGE ( 'NONE', *, *, #16382, .T. ) ;
#25074=ORIENTED_EDGE ( 'NONE', *, *, #22451, .F. ) ;
#25086=DIRECTION ( 'NONE',  ( -1.000000000000000000, 0.000000000000000000, -0.000000000000000000 ) ) ;
#25093=DIRECTION ( 'NONE',  ( 0.000000000000000000, 0.000000000000000000, 1.000000000000000000 ) ) ;
#25095=LINE ( 'NONE', #19840, #1319 ) ;
#25098=ORIENTED_EDGE ( 'NONE', *, *, #18480, .F. ) ;
#25101=DIRECTION ( 'NONE',  ( 0.000000000000000000, 0.000000000000000000, 1.000000000000000000 ) ) ;
#25104=AXIS2_PLACEMENT_3D ( 'NONE', #26387, #2093, #26202 ) ;
#25107=CARTESIAN_POINT ( 'NONE',  ( 4.000000000000003553, 7.162210897276456656, -51.50439529848821252 ) ) ;
#25108=DIRECTION ( 'NONE',  ( -1.000000000000000000, -0.000000000000000000, -0.000000000000000000 ) ) ;
#25109=CIRCLE ( 'NONE', #19882, 47.49900000000001654 ) ;
#25111=DIRECTION ( 'NONE',  ( 0.000000000000000000, 0.000000000000000000, 1.000000000000000000 ) ) ;
#25112=EDGE_CURVE ( 'NONE', #6684, #688, #12985, .T. ) ;
#25115=EDGE_LOOP ( 'NONE', ( #7594, #13318, #1683, #29023 ) ) ;
#25116=EDGE_CURVE ( 'NONE', #20467, #7261, #22164, .T. ) ;
#25120=AXIS2_PLACEMENT_3D ( 'NONE', #23498, #34493, #31955 ) ;
#25124=ORIENTED_EDGE ( 'NONE', *, *, #1601, .T. ) ;
#25127=EDGE_CURVE ( 'NONE', #30873, #34917, #15834, .T. ) ;
#25130=ADVANCED_FACE ( 'NONE', ( #21577 ), #19065, .T. ) ;
#25136=CARTESIAN_POINT ( 'NONE',  ( 0.000000000000000000, 50.95304419620825342, 10.38206564895680017 ) ) ;
#25140=CARTESIAN_POINT ( 'NONE',  ( 0.000000000000000000, -43.55304910509385508, -28.41006711800031326 ) ) ;
#25145=CIRCLE ( 'NONE', #9618, 47.49900000000001654 ) ;
#25149=ADVANCED_FACE ( 'NONE', ( #19234 ), #7909, .T. ) ;
#25151=SURFACE_STYLE_USAGE ( .BOTH. , #10937 ) ;
#25152=ORIENTED_EDGE ( 'NONE', *, *, #14047, .T. ) ;
#25157=VECTOR ( 'NONE', #13943, 1000.000000000000000 ) ;
#25166=EDGE_CURVE ( 'NONE', #31607, #26780, #2716, .T. ) ;
#25169=VECTOR ( 'NONE', #35484, 1000.000000000000000 ) ;
#25173=EDGE_CURVE ( 'NONE', #10239, #25998, #5579, .T. ) ;
#25178=CIRCLE ( 'NONE', #18250, 20.00000000000000000 ) ;
#25180=DIRECTION ( 'NONE',  ( -1.000000000000000000, -0.000000000000000000, -0.000000000000000000 ) ) ;
#25181=ORIENTED_EDGE ( 'NONE', *, *, #19383, .F. ) ;
#25185=CARTESIAN_POINT ( 'NONE',  ( 7.999999999999992895, 0.000000000000000000, 0.000000000000000000 ) ) ;
#25193=VECTOR ( 'NONE', #17074, 1000.000000000000000 ) ;
#25198=EDGE_CURVE ( 'NONE', #22664, #30, #34866, .T. ) ;
#25200=CARTESIAN_POINT ( 'NONE',  ( 7.999999999999992895, -27.79676263918161894, -37.88001506494798321 ) ) ;
#25201=ORIENTED_EDGE ( 'NONE', *, *, #17409, .F. ) ;
#25205=ORIENTED_EDGE ( 'NONE', *, *, #15046, .F. ) ;
#25206=ORIENTED_EDGE ( 'NONE', *, *, #12355, .T. ) ;
#25210=ORIENTED_EDGE ( 'NONE', *, *, #32106, .F. ) ;
#25212=CYLINDRICAL_SURFACE ( 'NONE', #11529, 20.00000000000000355 ) ;
#25220=ORIENTED_EDGE ( 'NONE', *, *, #20902, .T. ) ;
#25223=ORIENTED_EDGE ( 'NONE', *, *, #29524, .T. ) ;
#25226=FACE_OUTER_BOUND ( 'NONE', #2363, .T. ) ;
#25230=AXIS2_PLACEMENT_3D ( 'NONE', #31062, #14844, #6390 ) ;
#25235=ADVANCED_FACE ( 'NONE', ( #14713 ), #28243, .T. ) ;
#25236=VERTEX_POINT ( 'NONE', #34004 ) ;
#25240=EDGE_LOOP ( 'NONE', ( #28880, #31044, #15216, #7410 ) ) ;
#25251=EDGE_LOOP ( 'NONE', ( #29983, #8981, #15892, #7230, #10245, #33293 ) ) ;
#25252=ORIENTED_EDGE ( 'NONE', *, *, #6321, .F. ) ;
#25253=DIRECTION ( 'NONE',  ( 1.000000000000000000, -0.000000000000000000, -0.000000000000000000 ) ) ;
#25256=DIRECTION ( 'NONE',  ( -1.000000000000000000, 0.000000000000000000, 0.000000000000000000 ) ) ;
#25264=AXIS2_PLACEMENT_3D ( 'NONE', #31850, #9714, #10065 ) ;
#25265=DIRECTION ( 'NONE',  ( -1.000000000000000000, -0.000000000000000000, 0.000000000000000000 ) ) ;
#25267=DIRECTION ( 'NONE',  ( 0.000000000000000000, -1.000000000000000000, 0.000000000000000000 ) ) ;
#25268=CARTESIAN_POINT ( 'NONE',  ( 0.000000000000000000, -36.06787431788704623, 37.45808914225476371 ) ) ;
#25289=LINE ( 'NONE', #25107, #15282 ) ;
#25290=CARTESIAN_POINT ( 'NONE',  ( 0.000000000000000000, 0.000000000000000000, 0.000000000000000000 ) ) ;
#25292=DIRECTION ( 'NONE',  ( -1.000000000000000000, -0.000000000000000000, -0.000000000000000000 ) ) ;
#25305=AXIS2_PLACEMENT_3D ( 'NONE', #29886, #3228, #35469 ) ;
#25308=AXIS2_PLACEMENT_3D ( 'NONE', #35087, #10409, #35257 ) ;
#25311=CIRCLE ( 'NONE', #14340, 52.00000000000000711 ) ;
#25313=DIRECTION ( 'NONE',  ( -1.000000000000000000, 0.000000000000000000, 0.000000000000000000 ) ) ;
#25318=ADVANCED_FACE ( 'NONE', ( #33822 ), #9146, .T. ) ;
#25326=DIRECTION ( 'NONE',  ( -1.000000000000000000, 0.000000000000000000, 0.000000000000000000 ) ) ;
#25327=CARTESIAN_POINT ( 'NONE',  ( 0.000000000000000000, 0.000000000000000000, 0.000000000000000000 ) ) ;
#25328=ORIENTED_EDGE ( 'NONE', *, *, #3260, .T. ) ;
#25343=VECTOR ( 'NONE', #6537, 1000.000000000000000 ) ;
#25345=DIRECTION ( 'NONE',  ( 1.000000000000000000, 0.000000000000000000, -0.000000000000000000 ) ) ;
#25347=ADVANCED_FACE ( 'NONE', ( #28774 ), #17771, .T. ) ;
#25352=CYLINDRICAL_SURFACE ( 'NONE', #14547, 52.00000000000000711 ) ;
#25355=EDGE_CURVE ( 'NONE', #30827, #31611, #26215, .T. ) ;
#25357=CARTESIAN_POINT ( 'NONE',  ( 7.999999999999992895, -8.053585752061602321, -46.81126742072033409 ) ) ;
#25369=AXIS2_PLACEMENT_3D ( 'NONE', #355, #16567, #5775 ) ;
#25370=DIRECTION ( 'NONE',  ( -1.000000000000000000, 0.000000000000000000, 0.000000000000000000 ) ) ;
#25380=EDGE_CURVE ( 'NONE', #15928, #9731, #23185, .T. ) ;
#25382=ORIENTED_EDGE ( 'NONE', *, *, #32537, .F. ) ;
#25390=CIRCLE ( 'NONE', #19051, 47.49900000000001654 ) ;
#25395=VERTEX_POINT ( 'NONE', #30759 ) ;
#25396=ORIENTED_EDGE ( 'NONE', *, *, #24951, .F. ) ;
#25399=ADVANCED_FACE ( 'NONE', ( #29492 ), #26436, .T. ) ;
#25401=ORIENTED_EDGE ( 'NONE', *, *, #22168, .F. ) ;
#25419=FACE_OUTER_BOUND ( 'NONE', #2647, .T. ) ;
#25422=ORIENTED_EDGE ( 'NONE', *, *, #2653, .F. ) ;
#25424=DIRECTION ( 'NONE',  ( -1.000000000000000000, 0.000000000000000000, 0.000000000000000000 ) ) ;
#25429=AXIS2_PLACEMENT_3D ( 'NONE', #23768, #34756, #1990 ) ;
#25433=ORIENTED_EDGE ( 'NONE', *, *, #5094, .F. ) ;
#25438=VERTEX_POINT ( 'NONE', #35083 ) ;
#25445=AXIS2_PLACEMENT_3D ( 'NONE', #25847, #23120, #31587 ) ;
#25446=EDGE_LOOP ( 'NONE', ( #35377, #12476, #29363, #23506 ) ) ;
#25447=DIRECTION ( 'NONE',  ( 0.000000000000000000, 0.000000000000000000, 1.000000000000000000 ) ) ;
#25454=DIRECTION ( 'NONE',  ( 0.000000000000000000, 0.000000000000000000, 1.000000000000000000 ) ) ;
#25457=FACE_OUTER_BOUND ( 'NONE', #34056, .T. ) ;
#25459=ORIENTED_EDGE ( 'NONE', *, *, #19989, .F. ) ;
#25460=CARTESIAN_POINT ( 'NONE',  ( 7.999999999999992895, -47.49120266317497396, 0.8606222198173640869 ) ) ;
#25465=DIRECTION ( 'NONE',  ( -1.000000000000000000, 0.000000000000000000, 0.000000000000000000 ) ) ;
#25467=CARTESIAN_POINT ( 'NONE',  ( 0.000000000000000000, -17.50309955389579386, -43.60271849949381817 ) ) ;
#25469=FACE_OUTER_BOUND ( 'NONE', #13416, .T. ) ;
#25487=CYLINDRICAL_SURFACE ( 'NONE', #28719, 47.49900000000001654 ) ;
#25488=EDGE_CURVE ( 'NONE', #12307, #13559, #29099, .T. ) ;
#25491=CYLINDRICAL_SURFACE ( 'NONE', #34084, 20.00000000000000711 ) ;
#25496=CARTESIAN_POINT ( 'NONE',  ( 7.999999999999992895, 18.53613841426858500, -48.58406706613885007 ) ) ;
#25497=CARTESIAN_POINT ( 'NONE',  ( 0.000000000000000000, 13.85708833600033252, -45.43276465116652219 ) ) ;
#25500=CARTESIAN_POINT ( 'NONE',  ( 7.999999999999992895, 0.000000000000000000, 0.000000000000000000 ) ) ;
#25502=CARTESIAN_POINT ( 'NONE',  ( 7.999999999999992895, 0.000000000000000000, 0.000000000000000000 ) ) ;
#25503=CARTESIAN_POINT ( 'NONE',  ( 7.999999999999992895, 3.840921266750509488, -47.34345070675166767 ) ) ;
#25507=DIRECTION ( 'NONE',  ( 0.000000000000000000, -0.1253332335643113360, 0.9921147013144769877 ) ) ;
#25508=VERTEX_POINT ( 'NONE', #4299 ) ;
#25509=ORIENTED_EDGE ( 'NONE', *, *, #19133, .T. ) ;
#25510=AXIS2_PLACEMENT_3D ( 'NONE', #9740, #20700, #26131 ) ;
#25513=LINE ( 'NONE', #4098, #27310 ) ;
#25518=ADVANCED_FACE ( 'NONE', ( #7512 ), #34537, .T. ) ;
#25521=CYLINDRICAL_SURFACE ( 'NONE', #35556, 20.00000000000000355 ) ;
#25522=SHAPE_DEFINITION_REPRESENTATION ( #22712, #7982 ) ;
#25523=CARTESIAN_POINT ( 'NONE',  ( 7.999999999999992895, 49.25004636492413113, -16.68630974939708267 ) ) ;
#25525=VERTEX_POINT ( 'NONE', #21002 ) ;
#25531=DIRECTION ( 'NONE',  ( 0.000000000000000000, 0.000000000000000000, 1.000000000000000000 ) ) ;
#25532=EDGE_CURVE ( 'NONE', #18497, #30005, #14122, .T. ) ;
#25536=EDGE_CURVE ( 'NONE', #6545, #35594, #18726, .T. ) ;
#25540=AXIS2_PLACEMENT_3D ( 'NONE', #2437, #728, #32848 ) ;
#25544=DIRECTION ( 'NONE',  ( 0.000000000000000000, 0.4817536741017100499, 0.8763066800438665815 ) ) ;
#25550=ORIENTED_EDGE ( 'NONE', *, *, #4997, .F. ) ;
#25552=DIRECTION ( 'NONE',  ( 1.000000000000000000, 0.000000000000000000, 0.000000000000000000 ) ) ;
#25553=EDGE_CURVE ( 'NONE', #26780, #19478, #3842, .T. ) ;
#25558=DIRECTION ( 'NONE',  ( 0.000000000000000000, -0.9822872507286904975, 0.1873813145857149698 ) ) ;
#25560=ORIENTED_EDGE ( 'NONE', *, *, #7911, .T. ) ;
#25564=CIRCLE ( 'NONE', #30721, 47.49900000000001654 ) ;
#25569=ADVANCED_FACE ( 'NONE', ( #18130 ), #23910, .T. ) ;
#25572=DIRECTION ( 'NONE',  ( -1.000000000000000000, -0.000000000000000000, 0.000000000000000000 ) ) ;
#25582=CARTESIAN_POINT ( 'NONE',  ( 4.000000000000003553, 25.61928775981107265, -45.25098998563451147 ) ) ;
#25584=DIRECTION ( 'NONE',  ( -1.000000000000000000, 0.000000000000000000, 0.000000000000000000 ) ) ;
#25603=DIRECTION ( 'NONE',  ( 0.000000000000000000, 0.000000000000000000, 1.000000000000000000 ) ) ;
#25610=ORIENTED_EDGE ( 'NONE', *, *, #18232, .F. ) ;
#25614=ADVANCED_FACE ( 'NONE', ( #10934 ), #11110, .T. ) ;
#25623=CARTESIAN_POINT ( 'NONE',  ( 7.999999999999992895, -34.03046037009232094, -33.13733193845841640 ) ) ;
#25624=AXIS2_PLACEMENT_3D ( 'NONE', #7119, #6944, #4445 ) ;
#25626=DIRECTION ( 'NONE',  ( -1.000000000000000000, -0.000000000000000000, -0.000000000000000000 ) ) ;
#25627=CARTESIAN_POINT ( 'NONE',  ( 0.000000000000000000, -20.99948489194393275, -42.60488980472803888 ) ) ;
#25631=DIRECTION ( 'NONE',  ( -1.000000000000000000, -0.000000000000000000, -0.000000000000000000 ) ) ;
#25633=DIRECTION ( 'NONE',  ( -1.000000000000000000, 0.000000000000000000, -0.000000000000000000 ) ) ;
#25638=CARTESIAN_POINT ( 'NONE',  ( 0.000000000000000000, -42.03146605346771025, -22.12489237027362421 ) ) ;
#25640=AXIS2_PLACEMENT_3D ( 'NONE', #29812, #35045, #15377 ) ;
#25643=CARTESIAN_POINT ( 'NONE',  ( 0.000000000000000000, 44.61570720899095477, -14.73072383765580717 ) ) ;
#25648=AXIS2_PLACEMENT_3D ( 'NONE', #33183, #30489, #6337 ) ;
#25649=DIRECTION ( 'NONE',  ( 0.000000000000000000, -0.1253332335643113360, 0.9921147013144769877 ) ) ;
#25658=AXIS2_PLACEMENT_3D ( 'NONE', #6093, #31294, #25727 ) ;
#25664=CIRCLE ( 'NONE', #10132, 20.00000000000001066 ) ;
#25672=CIRCLE ( 'NONE', #31417, 20.00000000000000355 ) ;
#25676=CARTESIAN_POINT ( 'NONE',  ( 7.999999999999992895, 46.19362259308845609, -8.585149169757999132 ) ) ;
#25680=DIRECTION ( 'NONE',  ( 0.000000000000000000, -0.2486898871648415554, -0.9685831611286345177 ) ) ;
#25683=EDGE_CURVE ( 'NONE', #5115, #12651, #31995, .T. ) ;
#25684=CARTESIAN_POINT ( 'NONE',  ( 0.000000000000000000, 0.000000000000000000, 52.00000000000000711 ) ) ;
#25688=DIRECTION ( 'NONE',  ( 0.000000000000000000, 0.000000000000000000, -1.000000000000000000 ) ) ;
#25691=AXIS2_PLACEMENT_3D ( 'NONE', #9364, #31331, #6657 ) ;
#25701=AXIS2_PLACEMENT_3D ( 'NONE', #1725, #32489, #18271 ) ;
#25704=DIRECTION ( 'NONE',  ( -1.000000000000000000, 0.000000000000000000, 0.000000000000000000 ) ) ;
#25707=CARTESIAN_POINT ( 'NONE',  ( 0.000000000000000000, 46.87740477351717061, -3.172455868805379442 ) ) ;
#25721=CYLINDRICAL_SURFACE ( 'NONE', #13999, 20.00000000000000711 ) ;
#25724=FACE_OUTER_BOUND ( 'NONE', #33521, .T. ) ;
#25727=DIRECTION ( 'NONE',  ( 0.000000000000000000, 0.000000000000000000, 1.000000000000000000 ) ) ;
#25730=ORIENTED_EDGE ( 'NONE', *, *, #10772, .T. ) ;
#25734=ORIENTED_EDGE ( 'NONE', *, *, #32912, .F. ) ;
#25741=LINE ( 'NONE', #1071, #10602 ) ;
#25742=VERTEX_POINT ( 'NONE', #2488 ) ;
#25750=VECTOR ( 'NONE', #2905, 1000.000000000000000 ) ;
#25765=DIRECTION ( 'NONE',  ( -1.000000000000000000, 0.000000000000000000, 0.000000000000000000 ) ) ;
#25779=DIRECTION ( 'NONE',  ( 0.000000000000000000, -0.9510565162951500895, -0.3090169943749581649 ) ) ;
#25782=AXIS2_PLACEMENT_3D ( 'NONE', #26227, #29959, #1566 ) ;
#25784=ORIENTED_EDGE ( 'NONE', *, *, #28883, .T. ) ;
#25797=DIRECTION ( 'NONE',  ( 0.000000000000000000, 0.000000000000000000, 1.000000000000000000 ) ) ;
#25798=DIRECTION ( 'NONE',  ( -1.000000000000000000, -0.000000000000000000, 0.000000000000000000 ) ) ;
#25800=ORIENTED_EDGE ( 'NONE', *, *, #16705, .F. ) ;
#25804=EDGE_LOOP ( 'NONE', ( #24309, #30418, #18866, #28804 ) ) ;
#25805=ORIENTED_EDGE ( 'NONE', *, *, #16025, .F. ) ;
#25807=EDGE_CURVE ( 'NONE', #29543, #19637, #6230, .T. ) ;
#25821=FACE_OUTER_BOUND ( 'NONE', #34610, .T. ) ;
#25829=AXIS2_PLACEMENT_3D ( 'NONE', #11881, #19615, #22152 ) ;
#25830=DIRECTION ( 'NONE',  ( -1.000000000000000000, 0.000000000000000000, -0.000000000000000000 ) ) ;
#25839=ORIENTED_EDGE ( 'NONE', *, *, #9869, .T. ) ;
#25842=ORIENTED_EDGE ( 'NONE', *, *, #14127, .F. ) ;
#25846=ADVANCED_FACE ( 'NONE', ( #6571 ), #14857, .T. ) ;
#25847=CARTESIAN_POINT ( 'NONE',  ( 0.000000000000000000, 0.000000000000000000, 0.000000000000000000 ) ) ;
#25850=CARTESIAN_POINT ( 'NONE',  ( 7.999999999999992895, -43.83938735307282997, 18.28286404005782728 ) ) ;
#25863=EDGE_CURVE ( 'NONE', #15928, #25438, #13041, .T. ) ;
#25864=CIRCLE ( 'NONE', #15474, 47.49900000000001654 ) ;
#25865=LINE ( 'NONE', #24833, #11788 ) ;
#25880=VERTEX_POINT ( 'NONE', #19883 ) ;
#25882=CARTESIAN_POINT ( 'NONE',  ( 7.999999999999992895, -27.79676263918161894, -37.88001506494798321 ) ) ;
#25885=AXIS2_PLACEMENT_3D ( 'NONE', #2698, #19529, #34934 ) ;
#25887=CARTESIAN_POINT ( 'NONE',  ( 7.999999999999992895, 43.55304910509447325, -28.41006711799937179 ) ) ;
#25888=ORIENTED_EDGE ( 'NONE', *, *, #32911, .F. ) ;
#25892=CARTESIAN_POINT ( 'NONE',  ( 7.999999999999992895, 0.000000000000000000, 0.000000000000000000 ) ) ;
#25904=CARTESIAN_POINT ( 'NONE',  ( 0.000000000000000000, 46.87740477351717061, 16.82754413119462455 ) ) ;
#25906=DIRECTION ( 'NONE',  ( -1.000000000000000000, -0.000000000000000000, -0.000000000000000000 ) ) ;
#25907=CARTESIAN_POINT ( 'NONE',  ( 0.000000000000000000, -44.61570720899105424, 14.73072383765550164 ) ) ;
#25909=CIRCLE ( 'NONE', #10387, 20.00000000000000355 ) ;
#25917=CARTESIAN_POINT ( 'NONE',  ( 7.999999999999992895, 2.123073309835863842, -47.45152853935333326 ) ) ;
#25926=ORIENTED_EDGE ( 'NONE', *, *, #8200, .F. ) ;
#25928=EDGE_CURVE ( 'NONE', #25030, #16010, #25109, .T. ) ;
#25929=LINE ( 'NONE', #23215, #29303 ) ;
#25930=AXIS2_PLACEMENT_3D ( 'NONE', #18765, #29769, #13378 ) ;
#25932=ORIENTED_EDGE ( 'NONE', *, *, #1360, .T. ) ;
#25938=DIRECTION ( 'NONE',  ( -1.000000000000000000, -0.000000000000000000, 0.000000000000000000 ) ) ;
#25944=CARTESIAN_POINT ( 'NONE',  ( 7.999999999999992895, 47.22458491092828581, -5.098390039073752433 ) ) ;
#25945=FACE_OUTER_BOUND ( 'NONE', #303, .T. ) ;
#25963=ORIENTED_EDGE ( 'NONE', *, *, #28431, .T. ) ;
#25975=ORIENTED_EDGE ( 'NONE', *, *, #28159, .T. ) ;
#25976=DIRECTION ( 'NONE',  ( -1.000000000000000000, -0.000000000000000000, -0.000000000000000000 ) ) ;
#25995=LINE ( 'NONE', #15701, #3238 ) ;
#25998=VERTEX_POINT ( 'NONE', #4257 ) ;
#25999=DIRECTION ( 'NONE',  ( -1.000000000000000000, 0.000000000000000000, 0.000000000000000000 ) ) ;
#26008=SURFACE_SIDE_STYLE ('',( #9970 ) ) ;
#26009=ORIENTED_EDGE ( 'NONE', *, *, #16337, .T. ) ;
#26010=ORIENTED_EDGE ( 'NONE', *, *, #22168, .T. ) ;
#26013=EDGE_CURVE ( 'NONE', #11969, #34614, #27438, .T. ) ;
#26015=EDGE_CURVE ( 'NONE', #30768, #13700, #26391, .T. ) ;
#26017=CARTESIAN_POINT ( 'NONE',  ( 4.000000000000003553, -51.19683565102450729, 9.104066087303298360 ) ) ;
#26018=AXIS2_PLACEMENT_3D ( 'NONE', #30507, #9239, #22733 ) ;
#26020=LINE ( 'NONE', #9983, #9202 ) ;
#26021=DIRECTION ( 'NONE',  ( -1.000000000000000000, -0.000000000000000000, -0.000000000000000000 ) ) ;
#26022=EDGE_CURVE ( 'NONE', #7932, #3037, #4436, .T. ) ;
#26025=CARTESIAN_POINT ( 'NONE',  ( 7.999999999999992895, -2.123073309834833111, -47.45152853935339010 ) ) ;
#26026=ORIENTED_EDGE ( 'NONE', *, *, #22301, .F. ) ;
#26028=AXIS2_PLACEMENT_3D ( 'NONE', #26735, #21302, #32470 ) ;
#26031=CARTESIAN_POINT ( 'NONE',  ( 0.000000000000000000, 44.25018368420744252, 27.31155879685197263 ) ) ;
#26040=EDGE_CURVE ( 'NONE', #4109, #8056, #23383, .T. ) ;
#26042=AXIS2_PLACEMENT_3D ( 'NONE', #15512, #23462, #18043 ) ;
#26047=LINE ( 'NONE', #28567, #31897 ) ;
#26050=EDGE_LOOP ( 'NONE', ( #12234, #1938, #13751, #32167 ) ) ;
#26072=CARTESIAN_POINT ( 'NONE',  ( 0.000000000000000000, -47.32430374665948136, 21.55018039121510398 ) ) ;
#26074=CARTESIAN_POINT ( 'NONE',  ( 0.000000000000000000, 0.000000000000000000, 0.000000000000000000 ) ) ;
#26087=ORIENTED_EDGE ( 'NONE', *, *, #5305, .T. ) ;
#26094=CIRCLE ( 'NONE', #22048, 52.00000000000000711 ) ;
#26095=DIRECTION ( 'NONE',  ( 0.000000000000000000, -0.9822872507286865007, -0.1873813145857355644 ) ) ;
#26102=CIRCLE ( 'NONE', #2553, 47.49900000000000944 ) ;
#26116=ORIENTED_EDGE ( 'NONE', *, *, #21518, .T. ) ;
#26118=CARTESIAN_POINT ( 'NONE',  ( 7.999999999999992895, 22.82995208772687334, 41.06517797613670950 ) ) ;
#26126=AXIS2_PLACEMENT_3D ( 'NONE', #15973, #16146, #27162 ) ;
#26131=DIRECTION ( 'NONE',  ( 0.000000000000000000, 0.000000000000000000, 1.000000000000000000 ) ) ;
#26151=DIRECTION ( 'NONE',  ( -1.000000000000000000, -0.000000000000000000, -0.000000000000000000 ) ) ;
#26156=DIRECTION ( 'NONE',  ( 0.000000000000000000, 0.000000000000000000, 1.000000000000000000 ) ) ;
#26157=ORIENTED_EDGE ( 'NONE', *, *, #34299, .T. ) ;
#26160=CARTESIAN_POINT ( 'NONE',  ( 4.000000000000003553, 24.47917365150010127, -45.87777302070911389 ) ) ;
#26162=ORIENTED_EDGE ( 'NONE', *, *, #11007, .T. ) ;
#26167=EDGE_CURVE ( 'NONE', #29381, #29599, #84, .T. ) ;
#26174=CIRCLE ( 'NONE', #14082, 52.00000000000000711 ) ;
#26178=ORIENTED_EDGE ( 'NONE', *, *, #27997, .F. ) ;
#26185=CIRCLE ( 'NONE', #10664, 20.00000000000000711 ) ;
#26195=CARTESIAN_POINT ( 'NONE',  ( 0.000000000000000000, -44.61570720899084819, -14.73072383765613935 ) ) ;
#26196=VERTEX_POINT ( 'NONE', #10898 ) ;
#26202=DIRECTION ( 'NONE',  ( 0.000000000000000000, -0.9510565162951500895, -0.3090169943749581649 ) ) ;
#26203=DIRECTION ( 'NONE',  ( 0.000000000000000000, 0.000000000000000000, 1.000000000000000000 ) ) ;
#26207=DIRECTION ( 'NONE',  ( 0.000000000000000000, -0.9980267284282723361, 0.06279051952930261860 ) ) ;
#26210=EDGE_CURVE ( 'NONE', #4109, #8679, #35384, .T. ) ;
#26213=CARTESIAN_POINT ( 'NONE',  ( 7.999999999999992895, -2.123073309835510791, 47.45152853935334747 ) ) ;
#26214=VERTEX_POINT ( 'NONE', #29811 ) ;
#26215=CIRCLE ( 'NONE', #15861, 52.00000000000000711 ) ;
#26222=EDGE_CURVE ( 'NONE', #4505, #9311, #10746, .T. ) ;
#26224=ORIENTED_EDGE ( 'NONE', *, *, #11458, .T. ) ;
#26226=CIRCLE ( 'NONE', #22759, 52.00000000000000711 ) ;
#26227=CARTESIAN_POINT ( 'NONE',  ( 7.999999999999992895, 42.41764978026606769, 20.20639853260304619 ) ) ;
#26233=AXIS2_PLACEMENT_3D ( 'NONE', #32492, #5156, #5328 ) ;
#26240=CARTESIAN_POINT ( 'NONE',  ( 0.000000000000000000, 0.6505223195690454929, -51.99593080916758936 ) ) ;
#26245=CARTESIAN_POINT ( 'NONE',  ( 7.999999999999992895, 47.00885577955422434, -6.806061952191799769 ) ) ;
#26254=DIRECTION ( 'NONE',  ( 0.000000000000000000, 0.000000000000000000, -1.000000000000000000 ) ) ;
#26256=ADVANCED_FACE ( 'NONE', ( #27643 ), #18628, .T. ) ;
#26258=EDGE_CURVE ( 'NONE', #27614, #7369, #605, .T. ) ;
#26259=DIRECTION ( 'NONE',  ( -1.000000000000000000, -0.000000000000000000, -0.000000000000000000 ) ) ;
#26270=AXIS2_PLACEMENT_3D ( 'NONE', #8846, #5640, #24893 ) ;
#26274=LINE ( 'NONE', #17791, #28062 ) ;
#26276=CARTESIAN_POINT ( 'NONE',  ( 7.999999999999992895, 39.55064067543064965, 25.36340625197373910 ) ) ;
#26277=ORIENTED_EDGE ( 'NONE', *, *, #24342, .T. ) ;
#26280=CIRCLE ( 'NONE', #10756, 20.00000000000000711 ) ;
#26299=ORIENTED_EDGE ( 'NONE', *, *, #27523, .F. ) ;
#26300=CARTESIAN_POINT ( 'NONE',  ( 0.000000000000000000, 11.46872990052444408, -45.56340405422432127 ) ) ;
#26301=DIRECTION ( 'NONE',  ( -1.000000000000000000, 0.000000000000000000, 0.000000000000000000 ) ) ;
#26304=VERTEX_POINT ( 'NONE', #25460 ) ;
#26310=ORIENTED_EDGE ( 'NONE', *, *, #28883, .F. ) ;
#26311=VECTOR ( 'NONE', #7673, 1000.000000000000000 ) ;
#26317=CIRCLE ( 'NONE', #8492, 47.49900000000000944 ) ;
#26322=ORIENTED_EDGE ( 'NONE', *, *, #35259, .F. ) ;
#26325=AXIS2_PLACEMENT_3D ( 'NONE', #8014, #29461, #8188 ) ;
#26331=CARTESIAN_POINT ( 'NONE',  ( 0.000000000000000000, 0.000000000000000000, 0.000000000000000000 ) ) ;
#26334=LINE ( 'NONE', #32086, #9155 ) ;
#26337=AXIS2_PLACEMENT_3D ( 'NONE', #6483, #3799, #28454 ) ;
#26341=AXIS2_PLACEMENT_3D ( 'NONE', #7365, #26636, #13135 ) ;
#26343=DIRECTION ( 'NONE',  ( -1.000000000000000000, 0.000000000000000000, 0.000000000000000000 ) ) ;
#26347=CARTESIAN_POINT ( 'NONE',  ( 0.000000000000000000, -18.53613841426757602, -48.58406706613921244 ) ) ;
#26348=DIRECTION ( 'NONE',  ( -1.000000000000000000, -0.000000000000000000, -0.000000000000000000 ) ) ;
#26351=ORIENTED_EDGE ( 'NONE', *, *, #27329, .T. ) ;
#26358=ORIENTED_EDGE ( 'NONE', *, *, #25355, .F. ) ;
#26359=FACE_OUTER_BOUND ( 'NONE', #24237, .T. ) ;
#26367=ORIENTED_EDGE ( 'NONE', *, *, #14396, .T. ) ;
#26369=VECTOR ( 'NONE', #30660, 1000.000000000000000 ) ;
#26380=ORIENTED_EDGE ( 'NONE', *, *, #7218, .F. ) ;
#26387=CARTESIAN_POINT ( 'NONE',  ( 7.999999999999992895, -6.109652351741458709, -46.58570277113513214 ) ) ;
#26391=LINE ( 'NONE', #20603, #5588 ) ;
#26398=FACE_OUTER_BOUND ( 'NONE', #18736, .T. ) ;
#26403=ORIENTED_EDGE ( 'NONE', *, *, #25112, .F. ) ;
#26409=ORIENTED_EDGE ( 'NONE', *, *, #16358, .F. ) ;
#26410=CARTESIAN_POINT ( 'NONE',  ( 4.000000000000003553, -13.56094713063537327, -50.20060470671755581 ) ) ;
#26414=ORIENTED_EDGE ( 'NONE', *, *, #22694, .T. ) ;
#26415=ORIENTED_EDGE ( 'NONE', *, *, #18068, .F. ) ;
#26422=AXIS2_PLACEMENT_3D ( 'NONE', #27930, #13894, #3278 ) ;
#26433=CARTESIAN_POINT ( 'NONE',  ( 7.999999999999992895, -49.25004636492401033, 16.68630974939741662 ) ) ;
#26436=CYLINDRICAL_SURFACE ( 'NONE', #8388, 20.00000000000000355 ) ;
#26447=CARTESIAN_POINT ( 'NONE',  ( 0.000000000000000000, 47.32430374665962347, -21.55018039121475582 ) ) ;
#26454=VERTEX_POINT ( 'NONE', #28506 ) ;
#26456=CARTESIAN_POINT ( 'NONE',  ( 7.999999999999992895, 20.99948489194482448, -42.60488980472762677 ) ) ;
#26473=DIRECTION ( 'NONE',  ( 0.000000000000000000, 0.000000000000000000, 1.000000000000000000 ) ) ;
#26476=AXIS2_PLACEMENT_3D ( 'NONE', #27984, #20375, #608 ) ;
#26487=VERTEX_POINT ( 'NONE', #7397 ) ;
#26508=VERTEX_POINT ( 'NONE', #5240 ) ;
#26511=CARTESIAN_POINT ( 'NONE',  ( 7.999999999999992895, -39.78933988720132220, 24.98727647984988565 ) ) ;
#26516=EDGE_CURVE ( 'NONE', #31713, #19471, #7201, .T. ) ;
#26524=CARTESIAN_POINT ( 'NONE',  ( -9.999999999999994671, 0.000000000000000000, 0.000000000000000000 ) ) ;
#26528=DIRECTION ( 'NONE',  ( 0.000000000000000000, 0.000000000000000000, 1.000000000000000000 ) ) ;
#26533=CIRCLE ( 'NONE', #34600, 47.49900000000000944 ) ;
#26536=DIRECTION ( 'NONE',  ( -1.000000000000000000, 0.000000000000000000, -0.000000000000000000 ) ) ;
#26540=DIRECTION ( 'NONE',  ( 0.000000000000000000, 0.9048270524660176894, 0.4257792915650767118 ) ) ;
#26541=ADVANCED_FACE ( 'NONE', ( #23596 ), #13338, .T. ) ;
#26551=DIRECTION ( 'NONE',  ( -1.000000000000000000, -0.000000000000000000, -0.000000000000000000 ) ) ;
#26553=VERTEX_POINT ( 'NONE', #10088 ) ;
#26557=CIRCLE ( 'NONE', #8155, 20.00000000000000355 ) ;
#26559=DIRECTION ( 'NONE',  ( 1.000000000000000000, -0.000000000000000000, -0.000000000000000000 ) ) ;
#26564=DIRECTION ( 'NONE',  ( 0.000000000000000000, 0.000000000000000000, -1.000000000000000000 ) ) ;
#26567=CYLINDRICAL_SURFACE ( 'NONE', #15353, 47.49900000000001654 ) ;
#26570=DIRECTION ( 'NONE',  ( 1.000000000000000000, 0.000000000000000000, 0.000000000000000000 ) ) ;
#26574=LINE ( 'NONE', #12708, #14191 ) ;
#26580=CARTESIAN_POINT ( 'NONE',  ( 0.000000000000000000, 22.82995208772746665, -41.06517797613640397 ) ) ;
#26584=EDGE_CURVE ( 'NONE', #4328, #25742, #6581, .T. ) ;
#26588=ORIENTED_EDGE ( 'NONE', *, *, #30655, .T. ) ;
#26589=CARTESIAN_POINT ( 'NONE',  ( 0.000000000000000000, 0.000000000000000000, 0.000000000000000000 ) ) ;
#26592=ORIENTED_EDGE ( 'NONE', *, *, #10155, .T. ) ;
#26596=VERTEX_POINT ( 'NONE', #15475 ) ;
#26613=CARTESIAN_POINT ( 'NONE',  ( 0.000000000000000000, -49.65209126885753221, -15.44894276735603356 ) ) ;
#26615=AXIS2_PLACEMENT_3D ( 'NONE', #22244, #634, #6561 ) ;
#26616=CARTESIAN_POINT ( 'NONE',  ( 0.000000000000000000, 11.90021268425617329, -45.45261810511203038 ) ) ;
#26618=CARTESIAN_POINT ( 'NONE',  ( 4.000000000000003553, -35.11945359308137427, 38.34871548466002622 ) ) ;
#26631=FACE_OUTER_BOUND ( 'NONE', #6774, .T. ) ;
#26635=ORIENTED_EDGE ( 'NONE', *, *, #3903, .F. ) ;
#26636=DIRECTION ( 'NONE',  ( -1.000000000000000000, 0.000000000000000000, 0.000000000000000000 ) ) ;
#26640=EDGE_CURVE ( 'NONE', #22316, #10719, #22123, .T. ) ;
#26647=CARTESIAN_POINT ( 'NONE',  ( 0.000000000000000000, 0.000000000000000000, 0.000000000000000000 ) ) ;
#26650=CARTESIAN_POINT ( 'NONE',  ( 0.000000000000000000, 0.000000000000000000, 0.000000000000000000 ) ) ;
#26651=VECTOR ( 'NONE', #24532, 1000.000000000000000 ) ;
#26658=LINE ( 'NONE', #1812, #11870 ) ;
#26661=CARTESIAN_POINT ( 'NONE',  ( 7.999999999999992895, 0.000000000000000000, 0.000000000000000000 ) ) ;
#26680=CARTESIAN_POINT ( 'NONE',  ( 7.999999999999992895, 13.85708833600033074, -45.43276465116652219 ) ) ;
#26681=CIRCLE ( 'NONE', #32989, 20.00000000000000711 ) ;
#26684=ORIENTED_EDGE ( 'NONE', *, *, #27912, .T. ) ;
#26686=DIRECTION ( 'NONE',  ( 1.000000000000000000, 0.000000000000000000, 0.000000000000000000 ) ) ;
#26687=ADVANCED_FACE ( 'NONE', ( #30071 ), #24666, .T. ) ;
#26690=ORIENTED_EDGE ( 'NONE', *, *, #24708, .F. ) ;
#26693=CARTESIAN_POINT ( 'NONE',  ( -9.999999999999994671, 0.000000000000000000, 0.000000000000000000 ) ) ;
#26698=FACE_OUTER_BOUND ( 'NONE', #27827, .T. ) ;
#26701=EDGE_CURVE ( 'NONE', #22664, #8972, #18663, .T. ) ;
#26708=ORIENTED_EDGE ( 'NONE', *, *, #3146, .F. ) ;
#26711=LINE ( 'NONE', #18937, #1347 ) ;
#26716=ADVANCED_FACE ( 'NONE', ( #5586 ), #30766, .T. ) ;
#26719=CARTESIAN_POINT ( 'NONE',  ( 4.000000000000003553, -36.06787431788650622, -37.45808914225528952 ) ) ;
#26724=ORIENTED_EDGE ( 'NONE', *, *, #15574, .T. ) ;
#26735=CARTESIAN_POINT ( 'NONE',  ( 7.999999999999992895, 32.00046193115196758, -34.40241257139653186 ) ) ;
#26738=LINE ( 'NONE', #16073, #19373 ) ;
#26744=DIRECTION ( 'NONE',  ( -1.000000000000000000, 0.000000000000000000, -0.000000000000000000 ) ) ;
#26748=CARTESIAN_POINT ( 'NONE',  ( 7.999999999999992895, -42.60732521687585006, 19.80331771201643321 ) ) ;
#26754=AXIS2_PLACEMENT_3D ( 'NONE', #34904, #21722, #29663 ) ;
#26762=AXIS2_PLACEMENT_3D ( 'NONE', #7447, #19901, #31268 ) ;
#26763=FACE_OUTER_BOUND ( 'NONE', #4148, .T. ) ;
#26765=DIRECTION ( 'NONE',  ( 0.000000000000000000, -0.8443279255020087470, -0.5358267949790065376 ) ) ;
#26770=VECTOR ( 'NONE', #34218, 1000.000000000000000 ) ;
#26774=CARTESIAN_POINT ( 'NONE',  ( 0.000000000000000000, 0.000000000000000000, 0.000000000000000000 ) ) ;
#26776=ORIENTED_EDGE ( 'NONE', *, *, #17452, .F. ) ;
#26780=VERTEX_POINT ( 'NONE', #17422 ) ;
#26784=EDGE_CURVE ( 'NONE', #21338, #1167, #8301, .T. ) ;
#26795=VERTEX_POINT ( 'NONE', #33828 ) ;
#26804=CARTESIAN_POINT ( 'NONE',  ( 0.000000000000000000, 46.77034588191304465, 22.72740077717245910 ) ) ;
#26805=ORIENTED_EDGE ( 'NONE', *, *, #16599, .T. ) ;
#26810=CARTESIAN_POINT ( 'NONE',  ( 0.000000000000000000, -51.19683565102439360, -9.104066087303991139 ) ) ;
#26811=CARTESIAN_POINT ( 'NONE',  ( 0.000000000000000000, 10.58300524425836109, -3.000000000000002665 ) ) ;
#26812=CIRCLE ( 'NONE', #7266, 20.00000000000000355 ) ;
#26815=EDGE_CURVE ( 'NONE', #13426, #22165, #9691, .T. ) ;
#26817=ORIENTED_EDGE ( 'NONE', *, *, #9918, .F. ) ;
#26824=DIRECTION ( 'NONE',  ( -1.000000000000000000, 0.000000000000000000, 0.000000000000000000 ) ) ;
#26825=EDGE_CURVE ( 'NONE', #19482, #23782, #19223, .T. ) ;
#26828=DIRECTION ( 'NONE',  ( -1.000000000000000000, -0.000000000000000000, 0.000000000000000000 ) ) ;
#26836=ORIENTED_EDGE ( 'NONE', *, *, #31724, .T. ) ;
#26837=AXIS2_PLACEMENT_3D ( 'NONE', #25290, #11765, #11592 ) ;
#26839=DIRECTION ( 'NONE',  ( -1.000000000000000000, 0.000000000000000000, -0.000000000000000000 ) ) ;
#26840=ORIENTED_EDGE ( 'NONE', *, *, #15896, .T. ) ;
#26848=AXIS2_PLACEMENT_3D ( 'NONE', #25500, #33583, #815 ) ;
#26850=VERTEX_POINT ( 'NONE', #3422 ) ;
#26856=CIRCLE ( 'NONE', #19349, 20.00000000000000711 ) ;
#26859=ORIENTED_EDGE ( 'NONE', *, *, #22905, .F. ) ;
#26860=DIRECTION ( 'NONE',  ( -1.000000000000000000, -0.000000000000000000, -0.000000000000000000 ) ) ;
#26862=AXIS2_PLACEMENT_3D ( 'NONE', #34858, #24059, #9998 ) ;
#26868=AXIS2_PLACEMENT_3D ( 'NONE', #23247, #31544, #25797 ) ;
#26869=AXIS2_PLACEMENT_3D ( 'NONE', #24277, #15969, #21201 ) ;
#26872=ORIENTED_EDGE ( 'NONE', *, *, #28690, .T. ) ;
#26873=AXIS2_PLACEMENT_3D ( 'NONE', #7404, #2208, #4725 ) ;
#26878=DIRECTION ( 'NONE',  ( 0.000000000000000000, 0.000000000000000000, 1.000000000000000000 ) ) ;
#26880=EDGE_CURVE ( 'NONE', #14579, #4101, #12923, .T. ) ;
#26885=DIRECTION ( 'NONE',  ( -1.000000000000000000, 0.000000000000000000, 0.000000000000000000 ) ) ;
#26888=EDGE_CURVE ( 'NONE', #23561, #29894, #23929, .T. ) ;
#26895=ORIENTED_EDGE ( 'NONE', *, *, #35529, .T. ) ;
#26898=CARTESIAN_POINT ( 'NONE',  ( 7.999999999999992895, 0.000000000000000000, 0.000000000000000000 ) ) ;
#26900=CIRCLE ( 'NONE', #31483, 47.49900000000001654 ) ;
#26903=EDGE_LOOP ( 'NONE', ( #5990, #6156, #13262, #4716 ) ) ;
#26917=VECTOR ( 'NONE', #11534, 1000.000000000000000 ) ;
#26923=ADVANCED_FACE ( 'NONE', ( #31484, #28782 ), #4132, .F. ) ;
#26924=DIRECTION ( 'NONE',  ( -1.000000000000000000, -0.000000000000000000, 0.000000000000000000 ) ) ;
#26928=CARTESIAN_POINT ( 'NONE',  ( 4.000000000000003553, 5.871425383721550872, 51.66745943012285380 ) ) ;
#26939=CARTESIAN_POINT ( 'NONE',  ( 0.000000000000000000, -46.87740477351719193, 3.172455868805032608 ) ) ;
#26941=DIRECTION ( 'NONE',  ( 0.000000000000000000, -0.7705132427757949154, 0.6374239897486828621 ) ) ;
#26947=AXIS2_PLACEMENT_3D ( 'NONE', #8150, #19132, #27955 ) ;
#26955=EDGE_CURVE ( 'NONE', #17882, #6879, #1776, .T. ) ;
#26957=VERTEX_POINT ( 'NONE', #1956 ) ;
#26961=DIRECTION ( 'NONE',  ( 0.000000000000000000, 0.6845471059286899473, -0.7289686274214103312 ) ) ;
#26962=ORIENTED_EDGE ( 'NONE', *, *, #17253, .T. ) ;
#26965=DIRECTION ( 'NONE',  ( 0.000000000000000000, 0.000000000000000000, 1.000000000000000000 ) ) ;
#26970=LINE ( 'NONE', #30016, #26311 ) ;
#26977=CARTESIAN_POINT ( 'NONE',  ( 0.000000000000000000, 0.000000000000000000, 0.000000000000000000 ) ) ;
#26978=DIRECTION ( 'NONE',  ( 0.000000000000000000, 0.000000000000000000, 1.000000000000000000 ) ) ;
#26979=DIRECTION ( 'NONE',  ( 1.000000000000000000, -0.000000000000000000, -0.000000000000000000 ) ) ;
#26980=DIRECTION ( 'NONE',  ( -1.000000000000000000, 0.000000000000000000, -0.000000000000000000 ) ) ;
#26987=DIRECTION ( 'NONE',  ( 0.000000000000000000, 0.2486898871648552389, -0.9685831611286309650 ) ) ;
#26988=CARTESIAN_POINT ( 'NONE',  ( 7.999999999999992895, -22.82995208772716467, 41.06517797613655318 ) ) ;
#26992=EDGE_CURVE ( 'NONE', #15707, #20157, #12577, .T. ) ;
#26993=FACE_OUTER_BOUND ( 'NONE', #29265, .T. ) ;
#26994=DIRECTION ( 'NONE',  ( -1.000000000000000000, -0.000000000000000000, -0.000000000000000000 ) ) ;
#27000=DIRECTION ( 'NONE',  ( -1.000000000000000000, -0.000000000000000000, 0.000000000000000000 ) ) ;
#27001=CARTESIAN_POINT ( 'NONE',  ( 0.000000000000000000, -35.20873326984104068, 31.88259874184018372 ) ) ;
#27002=ORIENTED_EDGE ( 'NONE', *, *, #27776, .F. ) ;
#27009=DIRECTION ( 'NONE',  ( -1.000000000000000000, 0.000000000000000000, 0.000000000000000000 ) ) ;
#27015=VECTOR ( 'NONE', #10262, 1000.000000000000000 ) ;
#27028=LINE ( 'NONE', #16011, #25169 ) ;
#27030=ORIENTED_EDGE ( 'NONE', *, *, #1143, .F. ) ;
#27036=ORIENTED_EDGE ( 'NONE', *, *, #2259, .T. ) ;
#27038=AXIS2_PLACEMENT_3D ( 'NONE', #20764, #17898, #1175 ) ;
#27049=CIRCLE ( 'NONE', #21833, 20.00000000000000355 ) ;
#27050=DIRECTION ( 'NONE',  ( -1.000000000000000000, 0.000000000000000000, 0.000000000000000000 ) ) ;
#27056=FACE_OUTER_BOUND ( 'NONE', #15389, .T. ) ;
#27059=DIRECTION ( 'NONE',  ( -1.000000000000000000, -0.000000000000000000, -0.000000000000000000 ) ) ;
#27062=ADVANCED_FACE ( 'NONE', ( #10583 ), #5014, .T. ) ;
#27084=DIRECTION ( 'NONE',  ( 0.000000000000000000, 0.000000000000000000, 1.000000000000000000 ) ) ;
#27088=EDGE_CURVE ( 'NONE', #14794, #16713, #8896, .T. ) ;
#27097=CARTESIAN_POINT ( 'NONE',  ( 0.000000000000000000, 0.000000000000000000, 0.000000000000000000 ) ) ;
#27104=ADVANCED_FACE ( 'NONE', ( #9862 ), #16315, .T. ) ;
#27105=FACE_OUTER_BOUND ( 'NONE', #28257, .T. ) ;
#27107=DIRECTION ( 'NONE',  ( -1.000000000000000000, 0.000000000000000000, 0.000000000000000000 ) ) ;
#27109=CYLINDRICAL_SURFACE ( 'NONE', #22262, 47.49900000000001654 ) ;
#27112=DIRECTION ( 'NONE',  ( -1.000000000000000000, 0.000000000000000000, 0.000000000000000000 ) ) ;
#27115=ORIENTED_EDGE ( 'NONE', *, *, #16996, .F. ) ;
#27121=EDGE_CURVE ( 'NONE', #26795, #8310, #13982, .T. ) ;
#27135=VERTEX_POINT ( 'NONE', #482 ) ;
#27142=CIRCLE ( 'NONE', #17343, 20.00000000000000355 ) ;
#27150=ADVANCED_FACE ( 'NONE', ( #297 ), #19202, .F. ) ;
#27151=CARTESIAN_POINT ( 'NONE',  ( 0.000000000000000000, -18.53613841426824038, 48.58406706613897796 ) ) ;
#27152=DIRECTION ( 'NONE',  ( 0.000000000000000000, 0.000000000000000000, 1.000000000000000000 ) ) ;
#27155=DIRECTION ( 'NONE',  ( 0.000000000000000000, 0.000000000000000000, 1.000000000000000000 ) ) ;
#27157=FACE_OUTER_BOUND ( 'NONE', #34476, .T. ) ;
#27158=ORIENTED_EDGE ( 'NONE', *, *, #15431, .F. ) ;
#27159=AXIS2_PLACEMENT_3D ( 'NONE', #26661, #12967, #1814 ) ;
#27160=VERTEX_POINT ( 'NONE', #21909 ) ;
#27162=DIRECTION ( 'NONE',  ( 0.000000000000000000, 0.3681245526846720906, 0.9297764858882537897 ) ) ;
#27178=DIRECTION ( 'NONE',  ( -1.000000000000000000, -0.000000000000000000, 0.000000000000000000 ) ) ;
#27179=ORIENTED_EDGE ( 'NONE', *, *, #3496, .F. ) ;
#27184=CARTESIAN_POINT ( 'NONE',  ( 7.999999999999992895, 0.000000000000000000, -3.000000000000002665 ) ) ;
#27185=CIRCLE ( 'NONE', #16224, 47.49900000000001654 ) ;
#27198=VECTOR ( 'NONE', #9403, 1000.000000000000000 ) ;
#27200=VERTEX_POINT ( 'NONE', #8398 ) ;
#27203=VERTEX_POINT ( 'NONE', #22260 ) ;
#27205=CARTESIAN_POINT ( 'NONE',  ( 7.999999999999992895, 0.000000000000000000, 0.000000000000000000 ) ) ;
#27206=DIRECTION ( 'NONE',  ( -1.000000000000000000, 0.000000000000000000, 0.000000000000000000 ) ) ;
#27213=ORIENTED_EDGE ( 'NONE', *, *, #30690, .T. ) ;
#27216=ADVANCED_FACE ( 'NONE', ( #16671 ), #5197, .T. ) ;
#27222=AXIS2_PLACEMENT_3D ( 'NONE', #5617, #11012, #6304 ) ;
#27224=VERTEX_POINT ( 'NONE', #27685 ) ;
#27227=CARTESIAN_POINT ( 'NONE',  ( 0.000000000000000000, -25.61928775981012762, -45.25098998563503727 ) ) ;
#27228=CARTESIAN_POINT ( 'NONE',  ( 4.000000000000003553, 43.55304910509448035, -28.41006711799937179 ) ) ;
#27236=DIRECTION ( 'NONE',  ( 0.000000000000000000, 0.000000000000000000, 1.000000000000000000 ) ) ;
#27243=AXIS2_PLACEMENT_3D ( 'NONE', #19742, #513, #3225 ) ;
#27252=VERTEX_POINT ( 'NONE', #16847 ) ;
#27262=CARTESIAN_POINT ( 'NONE',  ( 7.999999999999992895, -0.2227391519113268437, -46.98410307550732057 ) ) ;
#27266=DIRECTION ( 'NONE',  ( -1.000000000000000000, -0.000000000000000000, 0.000000000000000000 ) ) ;
#27270=DIRECTION ( 'NONE',  ( 0.000000000000000000, 0.000000000000000000, 1.000000000000000000 ) ) ;
#27271=EDGE_CURVE ( 'NONE', #22983, #18045, #25024, .T. ) ;
#27273=DIRECTION ( 'NONE',  ( -1.000000000000000000, -0.000000000000000000, -0.000000000000000000 ) ) ;
#27278=CARTESIAN_POINT ( 'NONE',  ( 7.999999999999992895, 0.000000000000000000, 0.000000000000000000 ) ) ;
#27282=DIRECTION ( 'NONE',  ( -1.000000000000000000, -0.000000000000000000, -0.000000000000000000 ) ) ;
#27285=EDGE_CURVE ( 'NONE', #2557, #6413, #17199, .T. ) ;
#27286=DIRECTION ( 'NONE',  ( 1.000000000000000000, -0.000000000000000000, -0.000000000000000000 ) ) ;
#27292=CARTESIAN_POINT ( 'NONE',  ( 0.000000000000000000, 12.30077720129168384, -50.52416135122070528 ) ) ;
#27294=ORIENTED_EDGE ( 'NONE', *, *, #16924, .T. ) ;
#27298=VERTEX_POINT ( 'NONE', #28032 ) ;
#27299=VERTEX_POINT ( 'NONE', #3548 ) ;
#27301=EDGE_CURVE ( 'NONE', #19623, #31746, #31435, .T. ) ;
#27303=ORIENTED_EDGE ( 'NONE', *, *, #15541, .T. ) ;
#27304=ORIENTED_EDGE ( 'NONE', *, *, #7733, .F. ) ;
#27305=CYLINDRICAL_SURFACE ( 'NONE', #3469, 20.00000000000000711 ) ;
#27306=CARTESIAN_POINT ( 'NONE',  ( 7.999999999999992895, -32.32520163883607722, 34.09746168776025854 ) ) ;
#27307=CARTESIAN_POINT ( 'NONE',  ( 0.000000000000000000, 0.000000000000000000, 0.000000000000000000 ) ) ;
#27310=VECTOR ( 'NONE', #15040, 1000.000000000000000 ) ;
#27313=ADVANCED_FACE ( 'NONE', ( #28377 ), #11999, .T. ) ;
#27315=EDGE_CURVE ( 'NONE', #27252, #24147, #15229, .T. ) ;
#27320=CARTESIAN_POINT ( 'NONE',  ( 7.999999999999992895, -46.87740477351715640, -3.172455868805712509 ) ) ;
#27322=DIRECTION ( 'NONE',  ( -1.000000000000000000, 0.000000000000000000, 0.000000000000000000 ) ) ;
#27323=ORIENTED_EDGE ( 'NONE', *, *, #15367, .F. ) ;
#27324=EDGE_CURVE ( 'NONE', #7481, #779, #4094, .T. ) ;
#27326=CARTESIAN_POINT ( 'NONE',  ( 0.000000000000000000, 46.11014828289831513, 9.022736828081523441 ) ) ;
#27329=EDGE_CURVE ( 'NONE', #17430, #23884, #22964, .T. ) ;
#27334=DIRECTION ( 'NONE',  ( 0.000000000000000000, -0.9822872507286865007, -0.1873813145857355644 ) ) ;
#27339=CIRCLE ( 'NONE', #30215, 52.00000000000000711 ) ;
#27340=DIRECTION ( 'NONE',  ( 1.000000000000000000, 0.000000000000000000, 0.000000000000000000 ) ) ;
#27349=LINE ( 'NONE', #32559, #2337 ) ;
#27350=EDGE_CURVE ( 'NONE', #21603, #33166, #15826, .T. ) ;
#27362=DIRECTION ( 'NONE',  ( 0.000000000000000000, 0.000000000000000000, 1.000000000000000000 ) ) ;
#27365=CARTESIAN_POINT ( 'NONE',  ( 7.999999999999992895, -22.43957647427188817, 41.27978878573619426 ) ) ;
#27366=LINE ( 'NONE', #2717, #22655 ) ;
#27367=AXIS2_PLACEMENT_3D ( 'NONE', #33211, #13774, #8533 ) ;
#27373=CARTESIAN_POINT ( 'NONE',  ( 7.999999999999992895, 0.000000000000000000, 0.000000000000000000 ) ) ;
#27374=AXIS2_PLACEMENT_3D ( 'NONE', #20920, #1874, #7076 ) ;
#27377=EDGE_LOOP ( 'NONE', ( #30034, #30509, #23892, #2328 ) ) ;
#27378=AXIS2_PLACEMENT_3D ( 'NONE', #11565, #25256, #22533 ) ;
#27383=VECTOR ( 'NONE', #24660, 1000.000000000000000 ) ;
#27387=ORIENTED_EDGE ( 'NONE', *, *, #15383, .F. ) ;
#27388=DIRECTION ( 'NONE',  ( -1.000000000000000000, 0.000000000000000000, 0.000000000000000000 ) ) ;
#27390=DIRECTION ( 'NONE',  ( 1.000000000000000000, 0.000000000000000000, 0.000000000000000000 ) ) ;
#27391=ORIENTED_EDGE ( 'NONE', *, *, #9301, .T. ) ;
#27401=AXIS2_PLACEMENT_3D ( 'NONE', #12213, #28603, #31296 ) ;
#27406=DIRECTION ( 'NONE',  ( -1.000000000000000000, 0.000000000000000000, -0.000000000000000000 ) ) ;
#27412=FACE_OUTER_BOUND ( 'NONE', #14379, .T. ) ;
#27416=DIRECTION ( 'NONE',  ( -1.000000000000000000, 0.000000000000000000, 0.000000000000000000 ) ) ;
#27420=CARTESIAN_POINT ( 'NONE',  ( 0.000000000000000000, -44.47301969247457976, 16.68249143361895293 ) ) ;
#27438=CIRCLE ( 'NONE', #13620, 20.00000000000000355 ) ;
#27444=ADVANCED_FACE ( 'NONE', ( #31785 ), #15203, .T. ) ;
#27451=CARTESIAN_POINT ( 'NONE',  ( 7.999999999999992895, -51.85248208264520997, 3.914090171286008335 ) ) ;
#27458=DIRECTION ( 'NONE',  ( 0.000000000000000000, 0.000000000000000000, 1.000000000000000000 ) ) ;
#27464=VECTOR ( 'NONE', #13175, 1000.000000000000000 ) ;
#27467=VERTEX_POINT ( 'NONE', #21328 ) ;
#27469=DIRECTION ( 'NONE',  ( 0.000000000000000000, 0.000000000000000000, 1.000000000000000000 ) ) ;
#27475=AXIS2_PLACEMENT_3D ( 'NONE', #25676, #9451, #6397 ) ;
#27479=CARTESIAN_POINT ( 'NONE',  ( 7.999999999999992895, 42.03146605346819342, -22.12489237027273603 ) ) ;
#27482=CIRCLE ( 'NONE', #25829, 47.49900000000000944 ) ;
#27486=ORIENTED_EDGE ( 'NONE', *, *, #18010, .F. ) ;
#27490=AXIS2_PLACEMENT_3D ( 'NONE', #18720, #171, #32947 ) ;
#27491=CARTESIAN_POINT ( 'NONE',  ( 7.999999999999992895, 46.87740477351717061, -3.172455868805379442 ) ) ;
#27494=DIRECTION ( 'NONE',  ( 0.000000000000000000, 0.000000000000000000, 1.000000000000000000 ) ) ;
#27497=VECTOR ( 'NONE', #15154, 1000.000000000000000 ) ;
#27501=CYLINDRICAL_SURFACE ( 'NONE', #24359, 20.00000000000000355 ) ;
#27514=CARTESIAN_POINT ( 'NONE',  ( 7.999999999999992895, 30.93515269692114344, 36.04401931830264516 ) ) ;
#27515=EDGE_CURVE ( 'NONE', #2191, #128, #20413, .T. ) ;
#27522=ORIENTED_EDGE ( 'NONE', *, *, #24499, .F. ) ;
#27523=EDGE_CURVE ( 'NONE', #21923, #16080, #14666, .T. ) ;
#27531=ORIENTED_EDGE ( 'NONE', *, *, #10440, .F. ) ;
#27535=ADVANCED_FACE ( 'NONE', ( #12532 ), #23508, .T. ) ;
#27538=CARTESIAN_POINT ( 'NONE',  ( -9.999999999999994671, 0.000000000000000000, 0.000000000000000000 ) ) ;
#27539=EDGE_CURVE ( 'NONE', #933, #7078, #9821, .T. ) ;
#27550=ORIENTED_EDGE ( 'NONE', *, *, #16095, .F. ) ;
#27569=ORIENTED_EDGE ( 'NONE', *, *, #26992, .F. ) ;
#27572=CARTESIAN_POINT ( 'NONE',  ( 7.999999999999992895, -30.03615769709705319, -42.44795908869020451 ) ) ;
#27578=CIRCLE ( 'NONE', #10890, 52.00000000000000711 ) ;
#27579=CYLINDRICAL_SURFACE ( 'NONE', #6428, 20.00000000000000355 ) ;
#27585=DIRECTION ( 'NONE',  ( 0.000000000000000000, 0.000000000000000000, 1.000000000000000000 ) ) ;
#27586=DIRECTION ( 'NONE',  ( 0.000000000000000000, -0.6845471059286950544, 0.7289686274214053352 ) ) ;
#27601=DIRECTION ( 'NONE',  ( -1.000000000000000000, 0.000000000000000000, 0.000000000000000000 ) ) ;
#27613=ORIENTED_EDGE ( 'NONE', *, *, #1964, .F. ) ;
#27614=VERTEX_POINT ( 'NONE', #8353 ) ;
#27615=EDGE_CURVE ( 'NONE', #35403, #30561, #29989, .T. ) ;
#27619=CIRCLE ( 'NONE', #5756, 20.00000000000000355 ) ;
#27622=ORIENTED_EDGE ( 'NONE', *, *, #30527, .T. ) ;
#27632=CARTESIAN_POINT ( 'NONE',  ( 7.999999999999992895, 0.000000000000000000, 0.000000000000000000 ) ) ;
#27634=DIRECTION ( 'NONE',  ( -1.000000000000000000, -0.000000000000000000, 0.000000000000000000 ) ) ;
#27637=VECTOR ( 'NONE', #11590, 1000.000000000000000 ) ;
#27642=ORIENTED_EDGE ( 'NONE', *, *, #30440, .F. ) ;
#27643=FACE_OUTER_BOUND ( 'NONE', #16273, .T. ) ;
#27645=EDGE_CURVE ( 'NONE', #24892, #10989, #22719, .T. ) ;
#27646=DIRECTION ( 'NONE',  ( 1.000000000000000000, 0.000000000000000000, 0.000000000000000000 ) ) ;
#27662=CARTESIAN_POINT ( 'NONE',  ( 50.00005079999998969, 14.30000000000000071, 3.000000000000002665 ) ) ;
#27668=CARTESIAN_POINT ( 'NONE',  ( 50.00005079999998969, 1.347111479062088405E-15, -11.00000000000000000 ) ) ;
#27677=EDGE_CURVE ( 'NONE', #9355, #8056, #10717, .T. ) ;
#27682=( GEOMETRIC_REPRESENTATION_CONTEXT ( 3 ) GLOBAL_UNCERTAINTY_ASSIGNED_CONTEXT ( ( #12115 ) ) GLOBAL_UNIT_ASSIGNED_CONTEXT ( ( #4060, #4410, #28528 ) ) REPRESENTATION_CONTEXT ( 'NONE', 'WORKASPACE' ) );
#27685=CARTESIAN_POINT ( 'NONE',  ( 7.999999999999992895, -31.08872492059985149, 41.68322423723089543 ) ) ;
#27688=ORIENTED_EDGE ( 'NONE', *, *, #6696, .F. ) ;
#27689=ORIENTED_EDGE ( 'NONE', *, *, #10106, .F. ) ;
#27696=DIRECTION ( 'NONE',  ( -1.000000000000000000, -0.000000000000000000, 0.000000000000000000 ) ) ;
#27702=EDGE_LOOP ( 'NONE', ( #20926, #20826, #1662, #33927 ) ) ;
#27704=FACE_OUTER_BOUND ( 'NONE', #17934, .T. ) ;
#27707=AXIS2_PLACEMENT_3D ( 'NONE', #26774, #7324, #20981 ) ;
#27712=CARTESIAN_POINT ( 'NONE',  ( 7.999999999999992895, 46.87740477351717061, -3.172455868805379442 ) ) ;
#27715=ORIENTED_EDGE ( 'NONE', *, *, #8066, .T. ) ;
#27719=LINE ( 'NONE', #27887, #2007 ) ;
#27720=ADVANCED_FACE ( 'NONE', ( #2987 ), #88, .T. ) ;
#27742=EDGE_LOOP ( 'NONE', ( #4801, #15200, #18828, #27303 ) ) ;
#27760=ADVANCED_FACE ( 'NONE', ( #17157 ), #33737, .T. ) ;
#27764=EDGE_CURVE ( 'NONE', #9689, #30873, #8969, .T. ) ;
#27765=LINE ( 'NONE', #3105, #1699 ) ;
#27771=VECTOR ( 'NONE', #22414, 1000.000000000000000 ) ;
#27776=EDGE_CURVE ( 'NONE', #24590, #18097, #28166, .T. ) ;
#27778=EDGE_CURVE ( 'NONE', #35237, #5386, #25289, .T. ) ;
#27782=CIRCLE ( 'NONE', #4219, 47.49900000000000944 ) ;
#27786=AXIS2_PLACEMENT_3D ( 'NONE', #22749, #34103, #22928 ) ;
#27789=ORIENTED_EDGE ( 'NONE', *, *, #21313, .F. ) ;
#27799=DIRECTION ( 'NONE',  ( 0.000000000000000000, -0.1253332335642905193, -0.9921147013144796523 ) ) ;
#27803=CARTESIAN_POINT ( 'NONE',  ( 7.999999999999992895, 46.19362259308845609, -8.585149169757999132 ) ) ;
#27814=CARTESIAN_POINT ( 'NONE',  ( 7.999999999999992895, 46.87740477351717061, -3.172455868805379442 ) ) ;
#27818=CARTESIAN_POINT ( 'NONE',  ( 7.999999999999992895, -35.20873326984104068, 31.88259874184018372 ) ) ;
#27820=EDGE_LOOP ( 'NONE', ( #30523, #655, #396, #12575 ) ) ;
#27821=AXIS2_PLACEMENT_3D ( 'NONE', #32846, #35563, #10886 ) ;
#27822=FACE_OUTER_BOUND ( 'NONE', #13442, .T. ) ;
#27824=LINE ( 'NONE', #3160, #24339 ) ;
#27827=EDGE_LOOP ( 'NONE', ( #33830, #6810, #895, #10782 ) ) ;
#27838=LINE ( 'NONE', #24959, #17711 ) ;
#27848=DIRECTION ( 'NONE',  ( 1.000000000000000000, 0.000000000000000000, 0.000000000000000000 ) ) ;
#27850=EDGE_LOOP ( 'NONE', ( #22755, #23510, #30409, #11401 ) ) ;
#27855=ORIENTED_EDGE ( 'NONE', *, *, #29106, .T. ) ;
#27869=AXIS2_PLACEMENT_3D ( 'NONE', #13850, #33116, #19928 ) ;
#27872=VERTEX_POINT ( 'NONE', #6019 ) ;
#27883=DIRECTION ( 'NONE',  ( 0.000000000000000000, -0.9980267284282722251, 0.06279051952930256308 ) ) ;
#27886=CARTESIAN_POINT ( 'NONE',  ( 4.000000000000003553, -43.55304910509426009, 28.41006711799970574 ) ) ;
#27887=CARTESIAN_POINT ( 'NONE',  ( 4.000000000000003553, -13.56094713063606072, 50.20060470671736397 ) ) ;
#27888=ORIENTED_EDGE ( 'NONE', *, *, #2228, .T. ) ;
#27898=AXIS2_PLACEMENT_3D ( 'NONE', #33780, #34134, #14669 ) ;
#27901=VECTOR ( 'NONE', #17376, 1000.000000000000000 ) ;
#27906=CARTESIAN_POINT ( 'NONE',  ( 7.999999999999992895, 0.000000000000000000, 0.000000000000000000 ) ) ;
#27912=EDGE_CURVE ( 'NONE', #8310, #32263, #19297, .T. ) ;
#27918=DIRECTION ( 'NONE',  ( -1.000000000000000000, 0.000000000000000000, -0.000000000000000000 ) ) ;
#27923=AXIS2_PLACEMENT_3D ( 'NONE', #15149, #1489, #17501 ) ;
#27926=VECTOR ( 'NONE', #22356, 1000.000000000000000 ) ;
#27927=DIRECTION ( 'NONE',  ( -1.000000000000000000, 0.000000000000000000, -0.000000000000000000 ) ) ;
#27930=CARTESIAN_POINT ( 'NONE',  ( 7.999999999999992895, 0.000000000000000000, 0.000000000000000000 ) ) ;
#27935=EDGE_LOOP ( 'NONE', ( #11740, #4273, #33681, #8282 ) ) ;
#27937=CARTESIAN_POINT ( 'NONE',  ( 0.000000000000000000, 0.000000000000000000, 0.000000000000000000 ) ) ;
#27939=ORIENTED_EDGE ( 'NONE', *, *, #24184, .F. ) ;
#27941=EDGE_CURVE ( 'NONE', #28491, #403, #25995, .T. ) ;
#27944=VECTOR ( 'NONE', #16760, 1000.000000000000000 ) ;
#27948=CARTESIAN_POINT ( 'NONE',  ( 4.000000000000003553, -50.95304419620832448, 10.38206564895643957 ) ) ;
#27955=DIRECTION ( 'NONE',  ( 0.000000000000000000, 0.3681245526846719240, 0.9297764858882537897 ) ) ;
#27974=CARTESIAN_POINT ( 'NONE',  ( 7.999999999999992895, 32.00046193115148441, 34.40241257139697950 ) ) ;
#27984=CARTESIAN_POINT ( 'NONE',  ( 0.000000000000000000, 17.50309955389611716, 43.60271849949368317 ) ) ;
#27991=ORIENTED_EDGE ( 'NONE', *, *, #29153, .T. ) ;
#27996=VERTEX_POINT ( 'NONE', #164 ) ;
#27997=EDGE_CURVE ( 'NONE', #16080, #12983, #19068, .T. ) ;
#28001=EDGE_LOOP ( 'NONE', ( #25800, #12763, #10587, #12039 ) ) ;
#28003=AXIS2_PLACEMENT_3D ( 'NONE', #33019, #4778, #35372 ) ;
#28009=AXIS2_PLACEMENT_3D ( 'NONE', #16596, #11200, #33172 ) ;
#28017=DIRECTION ( 'NONE',  ( 0.000000000000000000, 0.7705132427757903635, -0.6374239897486881912 ) ) ;
#28024=DIRECTION ( 'NONE',  ( -1.000000000000000000, -0.000000000000000000, 0.000000000000000000 ) ) ;
#28032=CARTESIAN_POINT ( 'NONE',  ( 7.999999999999992895, -24.47917365149915270, -45.87777302070961127 ) ) ;
#28050=ADVANCED_FACE ( 'NONE', ( #8443 ), #13683, .T. ) ;
#28053=AXIS2_PLACEMENT_3D ( 'NONE', #27974, #25633, #14623 ) ;
#28056=AXIS2_PLACEMENT_3D ( 'NONE', #17812, #28812, #4162 ) ;
#28060=ORIENTED_EDGE ( 'NONE', *, *, #3495, .T. ) ;
#28062=VECTOR ( 'NONE', #30956, 1000.000000000000000 ) ;
#28067=DIRECTION ( 'NONE',  ( 0.000000000000000000, 0.000000000000000000, 1.000000000000000000 ) ) ;
#28073=DIRECTION ( 'NONE',  ( -1.000000000000000000, 0.000000000000000000, 0.000000000000000000 ) ) ;
#28074=DIRECTION ( 'NONE',  ( -1.000000000000000000, -0.000000000000000000, -0.000000000000000000 ) ) ;
#28075=VERTEX_POINT ( 'NONE', #11669 ) ;
#28079=DIRECTION ( 'NONE',  ( 0.000000000000000000, 0.4817536741017163782, -0.8763066800438630288 ) ) ;
#28081=ORIENTED_EDGE ( 'NONE', *, *, #5211, .T. ) ;
#28083=ADVANCED_FACE ( 'NONE', ( #32760 ), #2719, .T. ) ;
#28087=CIRCLE ( 'NONE', #15411, 52.00000000000000711 ) ;
#28091=VERTEX_POINT ( 'NONE', #14019 ) ;
#28092=CYLINDRICAL_SURFACE ( 'NONE', #19387, 20.00000000000000355 ) ;
#28104=CARTESIAN_POINT ( 'NONE',  ( 4.000000000000003553, -18.53613841426824038, 48.58406706613897796 ) ) ;
#28111=LINE ( 'NONE', #17815, #9504 ) ;
#28112=VERTEX_POINT ( 'NONE', #19584 ) ;
#28121=DIRECTION ( 'NONE',  ( 0.000000000000000000, 0.000000000000000000, 1.000000000000000000 ) ) ;
#28128=ORIENTED_EDGE ( 'NONE', *, *, #29574, .F. ) ;
#28129=VERTEX_POINT ( 'NONE', #30588 ) ;
#28132=EDGE_CURVE ( 'NONE', #22200, #29687, #17005, .T. ) ;
#28137=CIRCLE ( 'NONE', #22359, 20.00000000000000711 ) ;
#28143=ORIENTED_EDGE ( 'NONE', *, *, #25173, .T. ) ;
#28144=CARTESIAN_POINT ( 'NONE',  ( 7.999999999999992895, 0.2227391519123156360, -46.98410307550729215 ) ) ;
#28159=EDGE_CURVE ( 'NONE', #6112, #21169, #21611, .T. ) ;
#28160=DIRECTION ( 'NONE',  ( 0.000000000000000000, -0.4817536741017036661, -0.8763066800438699122 ) ) ;
#28165=EDGE_CURVE ( 'NONE', #4367, #17248, #13825, .T. ) ;
#28166=LINE ( 'NONE', #31036, #9546 ) ;
#28170=LINE ( 'NONE', #8891, #33798 ) ;
#28171=DIRECTION ( 'NONE',  ( 0.000000000000000000, 0.000000000000000000, 1.000000000000000000 ) ) ;
#28176=EDGE_CURVE ( 'NONE', #18999, #8679, #14691, .T. ) ;
#28189=CARTESIAN_POINT ( 'NONE',  ( 0.000000000000000000, 0.000000000000000000, 0.000000000000000000 ) ) ;
#28203=CARTESIAN_POINT ( 'NONE',  ( 0.000000000000000000, -17.08890430202718491, -43.76671000081963570 ) ) ;
#28205=EDGE_CURVE ( 'NONE', #33795, #6545, #28515, .T. ) ;
#28206=EDGE_CURVE ( 'NONE', #32324, #22667, #34302, .T. ) ;
#28211=VECTOR ( 'NONE', #31638, 1000.000000000000000 ) ;
#28224=VERTEX_POINT ( 'NONE', #9507 ) ;
#28236=FACE_OUTER_BOUND ( 'NONE', #3632, .T. ) ;
#28242=CARTESIAN_POINT ( 'NONE',  ( 7.999999999999992895, -17.50309955389579386, -43.60271849949381817 ) ) ;
#28243=CYLINDRICAL_SURFACE ( 'NONE', #25658, 20.00000000000000355 ) ;
#28247=VERTEX_POINT ( 'NONE', #23365 ) ;
#28250=ADVANCED_FACE ( 'NONE', ( #31644 ), #863, .T. ) ;
#28251=DIRECTION ( 'NONE',  ( 0.000000000000000000, -0.9048270524660145808, -0.4257792915650830956 ) ) ;
#28253=ORIENTED_EDGE ( 'NONE', *, *, #33056, .T. ) ;
#28255=FACE_OUTER_BOUND ( 'NONE', #16044, .T. ) ;
#28257=EDGE_LOOP ( 'NONE', ( #2147, #25734, #3072, #15827 ) ) ;
#28260=ORIENTED_EDGE ( 'NONE', *, *, #26815, .T. ) ;
#28263=AXIS2_PLACEMENT_3D ( 'NONE', #8769, #23175, #1049 ) ;
#28269=ORIENTED_EDGE ( 'NONE', *, *, #28159, .F. ) ;
#28286=ORIENTED_EDGE ( 'NONE', *, *, #28165, .F. ) ;
#28289=AXIS2_PLACEMENT_3D ( 'NONE', #25185, #508, #22624 ) ;
#28290=CARTESIAN_POINT ( 'NONE',  ( 7.999999999999992895, 46.77034588191305176, 22.72740077717247331 ) ) ;
#28295=EDGE_LOOP ( 'NONE', ( #6769, #10775, #395, #18360 ) ) ;
#28304=ORIENTED_EDGE ( 'NONE', *, *, #27285, .F. ) ;
#28308=ORIENTED_EDGE ( 'NONE', *, *, #21968, .F. ) ;
#28317=EDGE_CURVE ( 'NONE', #31456, #29619, #20112, .T. ) ;
#28324=CYLINDRICAL_SURFACE ( 'NONE', #19849, 47.49900000000001654 ) ;
#28325=FACE_OUTER_BOUND ( 'NONE', #4668, .T. ) ;
#28329=FACE_OUTER_BOUND ( 'NONE', #8750, .T. ) ;
#28336=DIRECTION ( 'NONE',  ( -1.000000000000000000, 0.000000000000000000, -0.000000000000000000 ) ) ;
#28354=VECTOR ( 'NONE', #35345, 1000.000000000000000 ) ;
#28359=VECTOR ( 'NONE', #93, 1000.000000000000000 ) ;
#28371=DIRECTION ( 'NONE',  ( -1.000000000000000000, -0.000000000000000000, 0.000000000000000000 ) ) ;
#28372=CARTESIAN_POINT ( 'NONE',  ( 0.000000000000000000, 0.000000000000000000, 0.000000000000000000 ) ) ;
#28373=CARTESIAN_POINT ( 'NONE',  ( 7.999999999999992895, -36.34385289850568057, -29.77717097092114074 ) ) ;
#28377=FACE_OUTER_BOUND ( 'NONE', #22929, .T. ) ;
#28380=VERTEX_POINT ( 'NONE', #27151 ) ;
#28381=CIRCLE ( 'NONE', #212, 47.49900000000000944 ) ;
#28384=FACE_OUTER_BOUND ( 'NONE', #17850, .T. ) ;
#28387=ORIENTED_EDGE ( 'NONE', *, *, #26888, .T. ) ;
#28409=AXIS2_PLACEMENT_3D ( 'NONE', #7019, #28817, #20689 ) ;
#28410=DIRECTION ( 'NONE',  ( -1.000000000000000000, -0.000000000000000000, -0.000000000000000000 ) ) ;
#28412=EDGE_CURVE ( 'NONE', #1640, #33383, #3831, .T. ) ;
#28429=EDGE_LOOP ( 'NONE', ( #7203, #17831, #11773, #618 ) ) ;
#28431=EDGE_CURVE ( 'NONE', #27252, #32280, #18495, .T. ) ;
#28435=ORIENTED_EDGE ( 'NONE', *, *, #1378, .T. ) ;
#28445=EDGE_CURVE ( 'NONE', #34437, #28224, #4490, .T. ) ;
#28446=DIRECTION ( 'NONE',  ( 0.000000000000000000, 0.000000000000000000, 1.000000000000000000 ) ) ;
#28447=ORIENTED_EDGE ( 'NONE', *, *, #8840, .T. ) ;
#28452=LINE ( 'NONE', #25582, #11668 ) ;
#28454=DIRECTION ( 'NONE',  ( 0.000000000000000000, 0.9048270524660175784, 0.4257792915650768784 ) ) ;
#28458=EDGE_LOOP ( 'NONE', ( #1651, #736, #18003, #27622 ) ) ;
#28464=DIRECTION ( 'NONE',  ( 0.000000000000000000, -0.9510565162951565288, 0.3090169943749383474 ) ) ;
#28475=ADVANCED_FACE ( 'NONE', ( #35256 ), #2490, .F. ) ;
#28477=DIRECTION ( 'NONE',  ( 0.000000000000000000, 0.000000000000000000, -1.000000000000000000 ) ) ;
#28479=ORIENTED_EDGE ( 'NONE', *, *, #2033, .T. ) ;
#28480=ORIENTED_EDGE ( 'NONE', *, *, #3391, .T. ) ;
#28482=CYLINDRICAL_SURFACE ( 'NONE', #9831, 47.49900000000001654 ) ;
#28490=EDGE_LOOP ( 'NONE', ( #25098, #15975, #11803, #19084 ) ) ;
#28491=VERTEX_POINT ( 'NONE', #30722 ) ;
#28496=CARTESIAN_POINT ( 'NONE',  ( 7.999999999999992895, 20.99948489194482448, -42.60488980472762677 ) ) ;
#28501=CARTESIAN_POINT ( 'NONE',  ( 7.999999999999992895, 0.000000000000000000, 0.000000000000000000 ) ) ;
#28503=CARTESIAN_POINT ( 'NONE',  ( -9.999999999999994671, 0.000000000000000000, 0.000000000000000000 ) ) ;
#28506=CARTESIAN_POINT ( 'NONE',  ( 0.000000000000000000, 49.65209126885763169, 15.44894276735568539 ) ) ;
#28515=CIRCLE ( 'NONE', #27401, 20.00000000000001066 ) ;
#28527=AXIS2_PLACEMENT_3D ( 'NONE', #31217, #25999, #9252 ) ;
#28528=( NAMED_UNIT ( * ) SI_UNIT ( $, .STERADIAN. ) SOLID_ANGLE_UNIT ( ) );
#28542=FACE_OUTER_BOUND ( 'NONE', #10238, .T. ) ;
#28551=CARTESIAN_POINT ( 'NONE',  ( 0.000000000000000000, -30.03615769709762873, 42.44795908868979950 ) ) ;
#28558=VERTEX_POINT ( 'NONE', #17017 ) ;
#28561=DIRECTION ( 'NONE',  ( 0.000000000000000000, 0.000000000000000000, 1.000000000000000000 ) ) ;
#28562=ORIENTED_EDGE ( 'NONE', *, *, #3765, .T. ) ;
#28567=CARTESIAN_POINT ( 'NONE',  ( 7.999999999999992895, -35.20873326984104068, 31.88259874184018372 ) ) ;
#28572=CIRCLE ( 'NONE', #18795, 20.00000000000000355 ) ;
#28574=CIRCLE ( 'NONE', #28009, 47.49900000000000944 ) ;
#28576=CARTESIAN_POINT ( 'NONE',  ( 0.000000000000000000, 29.60891106212840285, -37.14118181634734839 ) ) ;
#28581=EDGE_LOOP ( 'NONE', ( #31181, #2622, #26157, #19651 ) ) ;
#28589=DIRECTION ( 'NONE',  ( 0.000000000000000000, 0.000000000000000000, 1.000000000000000000 ) ) ;
#28595=CARTESIAN_POINT ( 'NONE',  ( 7.999999999999992895, -46.90537658765333617, 2.727856614654147638 ) ) ;
#28599=AXIS2_PLACEMENT_3D ( 'NONE', #5253, #2212, #7749 ) ;
#28603=DIRECTION ( 'NONE',  ( -1.000000000000000000, 0.000000000000000000, -0.000000000000000000 ) ) ;
#28618=CIRCLE ( 'NONE', #18266, 52.00000000000000711 ) ;
#28619=AXIS2_PLACEMENT_3D ( 'NONE', #34349, #23901, #15412 ) ;
#28620=DIRECTION ( 'NONE',  ( 0.000000000000000000, 0.000000000000000000, 1.000000000000000000 ) ) ;
#28627=ORIENTED_EDGE ( 'NONE', *, *, #24762, .F. ) ;
#28628=ORIENTED_EDGE ( 'NONE', *, *, #2259, .F. ) ;
#28632=CARTESIAN_POINT ( 'NONE',  ( 7.999999999999992895, -49.65209126885775248, 15.44894276735532479 ) ) ;
#28633=ORIENTED_EDGE ( 'NONE', *, *, #33056, .F. ) ;
#28636=DIRECTION ( 'NONE',  ( -1.000000000000000000, 0.000000000000000000, 0.000000000000000000 ) ) ;
#28646=ORIENTED_EDGE ( 'NONE', *, *, #21115, .F. ) ;
#28647=EDGE_CURVE ( 'NONE', #3876, #33861, #30879, .T. ) ;
#28649=ORIENTED_EDGE ( 'NONE', *, *, #12831, .F. ) ;
#28650=CIRCLE ( 'NONE', #18275, 20.00000000000000355 ) ;
#28656=EDGE_CURVE ( 'NONE', #8054, #10239, #28572, .T. ) ;
#28658=DIRECTION ( 'NONE',  ( -1.000000000000000000, -0.000000000000000000, 0.000000000000000000 ) ) ;
#28667=ORIENTED_EDGE ( 'NONE', *, *, #10156, .F. ) ;
#28669=DIRECTION ( 'NONE',  ( 0.000000000000000000, 0.000000000000000000, 1.000000000000000000 ) ) ;
#28670=ADVANCED_FACE ( 'NONE', ( #11801 ), #17371, .T. ) ;
#28671=DIRECTION ( 'NONE',  ( 0.000000000000000000, 0.000000000000000000, 1.000000000000000000 ) ) ;
#28676=VERTEX_POINT ( 'NONE', #22960 ) ;
#28680=CIRCLE ( 'NONE', #25230, 20.00000000000000711 ) ;
#28683=FACE_OUTER_BOUND ( 'NONE', #9315, .T. ) ;
#28685=ADVANCED_FACE ( 'NONE', ( #1366 ), #20605, .T. ) ;
#28690=EDGE_CURVE ( 'NONE', #26850, #18961, #13639, .T. ) ;
#28694=ORIENTED_EDGE ( 'NONE', *, *, #12975, .T. ) ;
#28703=VERTEX_POINT ( 'NONE', #17194 ) ;
#28705=DIRECTION ( 'NONE',  ( -1.000000000000000000, 0.000000000000000000, 0.000000000000000000 ) ) ;
#28711=VERTEX_POINT ( 'NONE', #25684 ) ;
#28719=AXIS2_PLACEMENT_3D ( 'NONE', #16653, #14476, #11442 ) ;
#28728=CIRCLE ( 'NONE', #8008, 20.00000000000000711 ) ;
#28737=CARTESIAN_POINT ( 'NONE',  ( 7.999999999999992895, -47.00885577955417460, 6.806061952192132836 ) ) ;
#28739=VERTEX_POINT ( 'NONE', #23317 ) ;
#28743=ORIENTED_EDGE ( 'NONE', *, *, #10165, .T. ) ;
#28746=ORIENTED_EDGE ( 'NONE', *, *, #3954, .F. ) ;
#28749=DIRECTION ( 'NONE',  ( 0.000000000000000000, 0.000000000000000000, -1.000000000000000000 ) ) ;
#28754=AXIS2_PLACEMENT_3D ( 'NONE', #30744, #5735, #22620 ) ;
#28761=ORIENTED_EDGE ( 'NONE', *, *, #32189, .F. ) ;
#28765=CYLINDRICAL_SURFACE ( 'NONE', #28821, 20.00000000000000711 ) ;
#28774=FACE_OUTER_BOUND ( 'NONE', #6256, .T. ) ;
#28778=EDGE_CURVE ( 'NONE', #1301, #17170, #15906, .T. ) ;
#28782=FACE_BOUND ( 'NONE', #25251, .T. ) ;
#28791=EDGE_LOOP ( 'NONE', ( #22888, #31026, #11586, #26010 ) ) ;
#28796=CYLINDRICAL_SURFACE ( 'NONE', #16162, 20.00000000000000355 ) ;
#28800=DIRECTION ( 'NONE',  ( -1.000000000000000000, 0.000000000000000000, 0.000000000000000000 ) ) ;
#28804=ORIENTED_EDGE ( 'NONE', *, *, #20768, .T. ) ;
#28806=EDGE_CURVE ( 'NONE', #13985, #33840, #15030, .T. ) ;
#28812=DIRECTION ( 'NONE',  ( 0.000000000000000000, 0.000000000000000000, 1.000000000000000000 ) ) ;
#28815=ORIENTED_EDGE ( 'NONE', *, *, #19406, .F. ) ;
#28817=DIRECTION ( 'NONE',  ( -1.000000000000000000, 0.000000000000000000, -0.000000000000000000 ) ) ;
#28821=AXIS2_PLACEMENT_3D ( 'NONE', #9844, #7501, #15763 ) ;
#28825=DIRECTION ( 'NONE',  ( -1.000000000000000000, 0.000000000000000000, 0.000000000000000000 ) ) ;
#28826=ORIENTED_EDGE ( 'NONE', *, *, #9702, .T. ) ;
#28828=DIRECTION ( 'NONE',  ( -1.000000000000000000, 0.000000000000000000, 0.000000000000000000 ) ) ;
#28830=COLOUR_RGB ( '', 0.66274510, 0.83137255, 0.94901961) ;
#28832=AXIS2_PLACEMENT_3D ( 'NONE', #4685, #35451, #7703 ) ;
#28837=ORIENTED_EDGE ( 'NONE', *, *, #33117, .T. ) ;
#28841=ORIENTED_EDGE ( 'NONE', *, *, #32345, .F. ) ;
#28842=VERTEX_POINT ( 'NONE', #31960 ) ;
#28846=ORIENTED_EDGE ( 'NONE', *, *, #29189, .T. ) ;
#28851=EDGE_CURVE ( 'NONE', #32250, #35186, #31446, .T. ) ;
#28854=AXIS2_PLACEMENT_3D ( 'NONE', #23803, #29571, #7583 ) ;
#28857=CARTESIAN_POINT ( 'NONE',  ( 4.000000000000003553, -49.25004636492401033, 16.68630974939741662 ) ) ;
#28860=EDGE_CURVE ( 'NONE', #28739, #29834, #29173, .T. ) ;
#28864=EDGE_CURVE ( 'NONE', #14196, #4114, #7297, .T. ) ;
#28869=CARTESIAN_POINT ( 'NONE',  ( 0.000000000000000000, 46.90537658765329354, 2.727856614654466938 ) ) ;
#28880=ORIENTED_EDGE ( 'NONE', *, *, #8563, .F. ) ;
#28883=EDGE_CURVE ( 'NONE', #2676, #17256, #35498, .T. ) ;
#28888=ADVANCED_FACE ( 'NONE', ( #4622 ), #15556, .T. ) ;
#28898=LINE ( 'NONE', #34125, #18614 ) ;
#28912=ORIENTED_EDGE ( 'NONE', *, *, #14127, .T. ) ;
#28919=CIRCLE ( 'NONE', #23149, 20.00000000000000355 ) ;
#28922=EDGE_LOOP ( 'NONE', ( #27323, #6424, #19929, #22005 ) ) ;
#28925=EDGE_CURVE ( 'NONE', #3630, #779, #26574, .T. ) ;
#28934=ORIENTED_EDGE ( 'NONE', *, *, #11463, .T. ) ;
#28942=DIRECTION ( 'NONE',  ( -1.000000000000000000, -0.000000000000000000, 0.000000000000000000 ) ) ;
#28951=DIRECTION ( 'NONE',  ( 0.000000000000000000, 0.000000000000000000, 1.000000000000000000 ) ) ;
#28954=DIRECTION ( 'NONE',  ( 0.000000000000000000, 0.000000000000000000, 1.000000000000000000 ) ) ;
#28957=VECTOR ( 'NONE', #1695, 1000.000000000000000 ) ;
#28963=CARTESIAN_POINT ( 'NONE',  ( 7.999999999999992895, 47.22458491092821475, 5.098390039074404356 ) ) ;
#28965=ORIENTED_EDGE ( 'NONE', *, *, #2694, .T. ) ;
#28980=CARTESIAN_POINT ( 'NONE',  ( 7.999999999999992895, -29.60891106212763191, -37.14118181634798788 ) ) ;
#28986=CYLINDRICAL_SURFACE ( 'NONE', #35270, 20.00000000000000355 ) ;
#28998=ORIENTED_EDGE ( 'NONE', *, *, #12717, .T. ) ;
#29000=ORIENTED_EDGE ( 'NONE', *, *, #15574, .F. ) ;
#29001=AXIS2_PLACEMENT_3D ( 'NONE', #17428, #15256, #12225 ) ;
#29002=AXIS2_PLACEMENT_3D ( 'NONE', #26118, #26301, #1637 ) ;
#29013=EDGE_CURVE ( 'NONE', #26850, #33784, #16265, .T. ) ;
#29023=ORIENTED_EDGE ( 'NONE', *, *, #698, .T. ) ;
#29040=ADVANCED_FACE ( 'NONE', ( #22384 ), #5843, .T. ) ;
#29041=AXIS2_PLACEMENT_3D ( 'NONE', #33905, #33722, #3671 ) ;
#29056=VERTEX_POINT ( 'NONE', #86 ) ;
#29060=ADVANCED_FACE ( 'NONE', ( #8006 ), #27109, .T. ) ;
#29072=DIRECTION ( 'NONE',  ( -1.000000000000000000, 0.000000000000000000, 0.000000000000000000 ) ) ;
#29074=CARTESIAN_POINT ( 'NONE',  ( 0.000000000000000000, 13.85708833599969303, 45.43276465116672114 ) ) ;
#29092=CARTESIAN_POINT ( 'NONE',  ( 7.999999999999992895, 38.92705108641771261, -27.21837053747755419 ) ) ;
#29098=ORIENTED_EDGE ( 'NONE', *, *, #21194, .T. ) ;
#29099=CIRCLE ( 'NONE', #11278, 52.00000000000000711 ) ;
#29100=ORIENTED_EDGE ( 'NONE', *, *, #17253, .F. ) ;
#29103=ORIENTED_EDGE ( 'NONE', *, *, #3137, .F. ) ;
#29104=EDGE_CURVE ( 'NONE', #28558, #22834, #11352, .T. ) ;
#29106=EDGE_CURVE ( 'NONE', #15493, #9389, #2983, .T. ) ;
#29109=ORIENTED_EDGE ( 'NONE', *, *, #20357, .T. ) ;
#29110=DIRECTION ( 'NONE',  ( -1.000000000000000000, 0.000000000000000000, 0.000000000000000000 ) ) ;
#29111=AXIS2_PLACEMENT_3D ( 'NONE', #32102, #15516, #12668 ) ;
#29114=AXIS2_PLACEMENT_3D ( 'NONE', #32186, #12750, #23912 ) ;
#29118=ORIENTED_EDGE ( 'NONE', *, *, #25532, .T. ) ;
#29121=DIRECTION ( 'NONE',  ( 0.000000000000000000, 0.000000000000000000, 1.000000000000000000 ) ) ;
#29128=CARTESIAN_POINT ( 'NONE',  ( 7.999999999999992895, -46.11014828289849277, 9.022736828080537563 ) ) ;
#29135=CARTESIAN_POINT ( 'NONE',  ( 7.999999999999992895, 11.46872990052381880, 45.56340405422447049 ) ) ;
#29151=CARTESIAN_POINT ( 'NONE',  ( 0.000000000000000000, 34.03046037009304570, -33.13733193845769165 ) ) ;
#29152=ORIENTED_EDGE ( 'NONE', *, *, #29480, .T. ) ;
#29153=EDGE_CURVE ( 'NONE', #2022, #32250, #19950, .T. ) ;
#29159=CARTESIAN_POINT ( 'NONE',  ( 0.000000000000000000, -51.93417535146740960, -2.615612846549736581 ) ) ;
#29160=CARTESIAN_POINT ( 'NONE',  ( 7.999999999999992895, -3.840921266750157326, 47.34345070675169609 ) ) ;
#29173=CIRCLE ( 'NONE', #5575, 47.49900000000003075 ) ;
#29176=AXIS2_PLACEMENT_3D ( 'NONE', #5320, #33031, #8344 ) ;
#29186=EDGE_LOOP ( 'NONE', ( #4687, #12241, #14498, #29540 ) ) ;
#29189=EDGE_CURVE ( 'NONE', #30241, #20113, #14782, .T. ) ;
#29192=ORIENTED_EDGE ( 'NONE', *, *, #14732, .F. ) ;
#29193=LINE ( 'NONE', #17646, #4832 ) ;
#29195=CIRCLE ( 'NONE', #15927, 20.00000000000000711 ) ;
#29198=ORIENTED_EDGE ( 'NONE', *, *, #9242, .T. ) ;
#29201=DIRECTION ( 'NONE',  ( 1.000000000000000000, 0.000000000000000000, 0.000000000000000000 ) ) ;
#29206=AXIS2_PLACEMENT_3D ( 'NONE', #21429, #26686, #4896 ) ;
#29216=CYLINDRICAL_SURFACE ( 'NONE', #19624, 52.00000000000000711 ) ;
#29218=VERTEX_POINT ( 'NONE', #6194 ) ;
#29230=ORIENTED_EDGE ( 'NONE', *, *, #10106, .T. ) ;
#29246=ORIENTED_EDGE ( 'NONE', *, *, #3533, .F. ) ;
#29250=( NAMED_UNIT ( * ) SI_UNIT ( $, .STERADIAN. ) SOLID_ANGLE_UNIT ( ) );
#29252=ORIENTED_EDGE ( 'NONE', *, *, #33464, .F. ) ;
#29259=DIRECTION ( 'NONE',  ( 1.000000000000000000, -0.000000000000000000, 0.000000000000000000 ) ) ;
#29265=EDGE_LOOP ( 'NONE', ( #5535, #2153, #8545, #360 ) ) ;
#29270=DIRECTION ( 'NONE',  ( -1.000000000000000000, -0.000000000000000000, 0.000000000000000000 ) ) ;
#29281=CARTESIAN_POINT ( 'NONE',  ( 0.000000000000000000, 1.347111479062088405E-15, -11.00000000000000000 ) ) ;
#29284=ORIENTED_EDGE ( 'NONE', *, *, #21, .T. ) ;
#29290=ORIENTED_EDGE ( 'NONE', *, *, #16121, .T. ) ;
#29292=DIRECTION ( 'NONE',  ( -1.000000000000000000, 0.000000000000000000, 0.000000000000000000 ) ) ;
#29293=EDGE_CURVE ( 'NONE', #17460, #2675, #19381, .T. ) ;
#29295=ORIENTED_EDGE ( 'NONE', *, *, #2779, .F. ) ;
#29303=VECTOR ( 'NONE', #34205, 1000.000000000000000 ) ;
#29315=DIRECTION ( 'NONE',  ( -1.000000000000000000, -0.000000000000000000, -0.000000000000000000 ) ) ;
#29317=DIRECTION ( 'NONE',  ( -1.000000000000000000, -0.000000000000000000, 0.000000000000000000 ) ) ;
#29319=ORIENTED_EDGE ( 'NONE', *, *, #7618, .T. ) ;
#29324=EDGE_CURVE ( 'NONE', #6382, #35356, #32248, .T. ) ;
#29326=CIRCLE ( 'NONE', #32756, 20.00000000000001066 ) ;
#29328=DIRECTION ( 'NONE',  ( -1.000000000000000000, -0.000000000000000000, -0.000000000000000000 ) ) ;
#29331=MECHANICAL_DESIGN_GEOMETRIC_PRESENTATION_REPRESENTATION('',(#24727),#9181);
#29336=LINE ( 'NONE', #32028, #6770 ) ;
#29339=DIRECTION ( 'NONE',  ( 0.000000000000000000, 0.000000000000000000, 1.000000000000000000 ) ) ;
#29355=CARTESIAN_POINT ( 'NONE',  ( 0.000000000000000000, 0.000000000000000000, 0.000000000000000000 ) ) ;
#29356=VECTOR ( 'NONE', #25465, 1000.000000000000000 ) ;
#29363=ORIENTED_EDGE ( 'NONE', *, *, #28431, .F. ) ;
#29364=DIRECTION ( 'NONE',  ( -1.000000000000000000, 0.000000000000000000, 0.000000000000000000 ) ) ;
#29366=VERTEX_POINT ( 'NONE', #18910 ) ;
#29368=VERTEX_POINT ( 'NONE', #7745 ) ;
#29371=VERTEX_POINT ( 'NONE', #29732 ) ;
#29375=ORIENTED_EDGE ( 'NONE', *, *, #10617, .T. ) ;
#29377=AXIS2_PLACEMENT_3D ( 'NONE', #35082, #21364, #8567 ) ;
#29378=LINE ( 'NONE', #26680, #2161 ) ;
#29381=VERTEX_POINT ( 'NONE', #2377 ) ;
#29383=AXIS2_PLACEMENT_3D ( 'NONE', #31546, #6870, #17843 ) ;
#29393=DIRECTION ( 'NONE',  ( 1.000000000000000000, 0.000000000000000000, 0.000000000000000000 ) ) ;
#29394=ORIENTED_EDGE ( 'NONE', *, *, #1703, .F. ) ;
#29395=VERTEX_POINT ( 'NONE', #35492 ) ;
#29415=ORIENTED_EDGE ( 'NONE', *, *, #31762, .T. ) ;
#29418=CARTESIAN_POINT ( 'NONE',  ( 7.999999999999992895, 36.06787431788677623, 37.45808914225502662 ) ) ;
#29420=ORIENTED_EDGE ( 'NONE', *, *, #8269, .F. ) ;
#29433=CARTESIAN_POINT ( 'NONE',  ( 0.000000000000000000, 14.30000000000000071, 3.000000000000002665 ) ) ;
#29458=ADVANCED_FACE ( 'NONE', ( #22485 ), #21958, .T. ) ;
#29459=ORIENTED_EDGE ( 'NONE', *, *, #19865, .F. ) ;
#29461=DIRECTION ( 'NONE',  ( -1.000000000000000000, 0.000000000000000000, 0.000000000000000000 ) ) ;
#29462=CARTESIAN_POINT ( 'NONE',  ( -9.999999999999994671, 0.000000000000000000, 0.000000000000000000 ) ) ;
#29469=ORIENTED_EDGE ( 'NONE', *, *, #19777, .T. ) ;
#29477=DIRECTION ( 'NONE',  ( -1.000000000000000000, -0.000000000000000000, -0.000000000000000000 ) ) ;
#29480=EDGE_CURVE ( 'NONE', #27160, #4061, #11348, .T. ) ;
#29485=DIRECTION ( 'NONE',  ( -1.000000000000000000, 0.000000000000000000, 0.000000000000000000 ) ) ;
#29492=FACE_OUTER_BOUND ( 'NONE', #5581, .T. ) ;
#29495=CARTESIAN_POINT ( 'NONE',  ( 0.000000000000000000, 0.000000000000000000, 0.000000000000000000 ) ) ;
#29499=ADVANCED_FACE ( 'NONE', ( #13867 ), #8, .T. ) ;
#29505=AXIS2_PLACEMENT_3D ( 'NONE', #33324, #8649, #27586 ) ;
#29509=ORIENTED_EDGE ( 'NONE', *, *, #6432, .T. ) ;
#29510=EDGE_LOOP ( 'NONE', ( #3434, #14909, #7194, #22131 ) ) ;
#29512=CARTESIAN_POINT ( 'NONE',  ( 0.000000000000000000, -41.20225022064654041, 23.63323037071388200 ) ) ;
#29523=DIRECTION ( 'NONE',  ( -1.000000000000000000, -0.000000000000000000, -0.000000000000000000 ) ) ;
#29524=EDGE_CURVE ( 'NONE', #29876, #35108, #11514, .T. ) ;
#29526=ORIENTED_EDGE ( 'NONE', *, *, #21550, .T. ) ;
#29534=DIRECTION ( 'NONE',  ( -1.000000000000000000, 0.000000000000000000, -0.000000000000000000 ) ) ;
#29537=DIRECTION ( 'NONE',  ( -1.000000000000000000, -0.000000000000000000, 0.000000000000000000 ) ) ;
#29540=ORIENTED_EDGE ( 'NONE', *, *, #22769, .F. ) ;
#29543=VERTEX_POINT ( 'NONE', #33307 ) ;
#29549=ORIENTED_EDGE ( 'NONE', *, *, #23614, .T. ) ;
#29550=CIRCLE ( 'NONE', #18030, 20.00000000000000000 ) ;
#29557=LINE ( 'NONE', #35142, #27464 ) ;
#29560=EDGE_LOOP ( 'NONE', ( #17448, #28304, #23769, #1958 ) ) ;
#29568=EDGE_LOOP ( 'NONE', ( #22495, #33078, #27789, #20982 ) ) ;
#29571=DIRECTION ( 'NONE',  ( -1.000000000000000000, 0.000000000000000000, -0.000000000000000000 ) ) ;
#29574=EDGE_CURVE ( 'NONE', #19482, #11865, #3970, .T. ) ;
#29577=DIRECTION ( 'NONE',  ( -1.000000000000000000, 0.000000000000000000, 0.000000000000000000 ) ) ;
#29587=EDGE_CURVE ( 'NONE', #29784, #14247, #33838, .T. ) ;
#29592=CARTESIAN_POINT ( 'NONE',  ( 7.999999999999992895, -6.109652351742118626, 46.58570277113506819 ) ) ;
#29599=VERTEX_POINT ( 'NONE', #9346 ) ;
#29607=AXIS2_PLACEMENT_3D ( 'NONE', #3918, #1201, #33794 ) ;
#29609=CARTESIAN_POINT ( 'NONE',  ( 7.999999999999992895, 0.000000000000000000, 0.000000000000000000 ) ) ;
#29611=CARTESIAN_POINT ( 'NONE',  ( 4.000000000000003553, -30.03615769709763228, 42.44795908868979950 ) ) ;
#29614=CARTESIAN_POINT ( 'NONE',  ( 0.000000000000000000, 34.03046037009256963, 33.13733193845818903 ) ) ;
#29618=CARTESIAN_POINT ( 'NONE',  ( 4.000000000000003553, 36.06787431788733045, -37.45808914225451502 ) ) ;
#29619=VERTEX_POINT ( 'NONE', #3601 ) ;
#29625=ORIENTED_EDGE ( 'NONE', *, *, #107, .T. ) ;
#29626=CARTESIAN_POINT ( 'NONE',  ( -9.999999999999994671, 0.000000000000000000, 0.000000000000000000 ) ) ;
#29636=ORIENTED_EDGE ( 'NONE', *, *, #23894, .F. ) ;
#29639=DIRECTION ( 'NONE',  ( 0.000000000000000000, 0.000000000000000000, 1.000000000000000000 ) ) ;
#29643=EDGE_LOOP ( 'NONE', ( #26635, #16862, #22399, #29904 ) ) ;
#29651=CARTESIAN_POINT ( 'NONE',  ( 7.999999999999992895, -44.61570720899105424, 14.73072383765550164 ) ) ;
#29660=CARTESIAN_POINT ( 'NONE',  ( 7.999999999999992895, -17.50309955389642269, 43.60271849949356948 ) ) ;
#29661=AXIS2_PLACEMENT_3D ( 'NONE', #15594, #2142, #12748 ) ;
#29663=DIRECTION ( 'NONE',  ( 0.000000000000000000, -0.9510565162951565288, 0.3090169943749383474 ) ) ;
#29667=ORIENTED_EDGE ( 'NONE', *, *, #18035, .F. ) ;
#29671=ORIENTED_EDGE ( 'NONE', *, *, #32332, .T. ) ;
#29674=AXIS2_PLACEMENT_3D ( 'NONE', #34811, #21455, #9953 ) ;
#29675=CARTESIAN_POINT ( 'NONE',  ( -9.999999999999994671, 0.000000000000000000, 0.000000000000000000 ) ) ;
#29678=EDGE_LOOP ( 'NONE', ( #14866, #34239, #3858, #13065 ) ) ;
#29685=CYLINDRICAL_SURFACE ( 'NONE', #31703, 47.49900000000001654 ) ;
#29687=VERTEX_POINT ( 'NONE', #20302 ) ;
#29693=CYLINDRICAL_SURFACE ( 'NONE', #14336, 20.00000000000000355 ) ;
#29699=LINE ( 'NONE', #27184, #32116 ) ;
#29701=CARTESIAN_POINT ( 'NONE',  ( 7.999999999999992895, 0.000000000000000000, 0.000000000000000000 ) ) ;
#29708=ORIENTED_EDGE ( 'NONE', *, *, #17657, .T. ) ;
#29711=DIRECTION ( 'NONE',  ( -1.000000000000000000, -0.000000000000000000, -0.000000000000000000 ) ) ;
#29712=EDGE_CURVE ( 'NONE', #7659, #9761, #35554, .T. ) ;
#29713=ORIENTED_EDGE ( 'NONE', *, *, #7688, .T. ) ;
#29721=ORIENTED_EDGE ( 'NONE', *, *, #4921, .F. ) ;
#29725=EDGE_CURVE ( 'NONE', #27299, #5721, #26274, .T. ) ;
#29728=EDGE_CURVE ( 'NONE', #34766, #35237, #20559, .T. ) ;
#29731=AXIS2_PLACEMENT_3D ( 'NONE', #14616, #14439, #22546 ) ;
#29732=CARTESIAN_POINT ( 'NONE',  ( 0.000000000000000000, 9.744342220503382279, 46.48873837489803407 ) ) ;
#29735=DIRECTION ( 'NONE',  ( 0.000000000000000000, 0.000000000000000000, 1.000000000000000000 ) ) ;
#29741=AXIS2_PLACEMENT_3D ( 'NONE', #19204, #13466, #30204 ) ;
#29750=DIRECTION ( 'NONE',  ( -1.000000000000000000, 0.000000000000000000, 0.000000000000000000 ) ) ;
#29755=CARTESIAN_POINT ( 'NONE',  ( 7.999999999999992895, -41.20225022064655462, 23.63323037071389621 ) ) ;
#29757=EDGE_CURVE ( 'NONE', #31746, #17882, #13116, .T. ) ;
#29759=ORIENTED_EDGE ( 'NONE', *, *, #2370, .T. ) ;
#29762=DIRECTION ( 'NONE',  ( 0.000000000000000000, 0.000000000000000000, 1.000000000000000000 ) ) ;
#29763=CYLINDRICAL_SURFACE ( 'NONE', #13987, 20.00000000000000355 ) ;
#29769=DIRECTION ( 'NONE',  ( -1.000000000000000000, 0.000000000000000000, -0.000000000000000000 ) ) ;
#29774=EDGE_CURVE ( 'NONE', #13787, #27224, #21718, .T. ) ;
#29784=VERTEX_POINT ( 'NONE', #2163 ) ;
#29785=VERTEX_POINT ( 'NONE', #15976 ) ;
#29787=DIRECTION ( 'NONE',  ( -1.000000000000000000, 0.000000000000000000, 0.000000000000000000 ) ) ;
#29792=ADVANCED_FACE ( 'NONE', ( #26993 ), #9872, .T. ) ;
#29796=ADVANCED_FACE ( 'NONE', ( #18337 ), #4509, .T. ) ;
#29800=FACE_OUTER_BOUND ( 'NONE', #31382, .T. ) ;
#29802=DIRECTION ( 'NONE',  ( 0.000000000000000000, 0.000000000000000000, 1.000000000000000000 ) ) ;
#29806=DIRECTION ( 'NONE',  ( -1.000000000000000000, -0.000000000000000000, -0.000000000000000000 ) ) ;
#29807=EDGE_CURVE ( 'NONE', #26196, #8972, #21021, .T. ) ;
#29810=ORIENTED_EDGE ( 'NONE', *, *, #14610, .F. ) ;
#29811=CARTESIAN_POINT ( 'NONE',  ( 0.000000000000000000, 49.25004636492388954, 16.68630974939777545 ) ) ;
#29812=CARTESIAN_POINT ( 'NONE',  ( 0.000000000000000000, 6.109652351742432153, -46.58570277113502556 ) ) ;
#29813=DIRECTION ( 'NONE',  ( 0.000000000000000000, 0.000000000000000000, 1.000000000000000000 ) ) ;
#29818=DIRECTION ( 'NONE',  ( 1.000000000000000000, 0.000000000000000000, 0.000000000000000000 ) ) ;
#29821=AXIS2_PLACEMENT_3D ( 'NONE', #9666, #20263, #3926 ) ;
#29822=DIRECTION ( 'NONE',  ( 0.000000000000000000, 0.000000000000000000, 1.000000000000000000 ) ) ;
#29832=EDGE_CURVE ( 'NONE', #14042, #4708, #15386, .T. ) ;
#29834=VERTEX_POINT ( 'NONE', #29512 ) ;
#29836=EDGE_CURVE ( 'NONE', #20467, #8283, #1788, .T. ) ;
#29840=CARTESIAN_POINT ( 'NONE',  ( 0.000000000000000000, 0.000000000000000000, 0.000000000000000000 ) ) ;
#29853=VERTEX_POINT ( 'NONE', #26810 ) ;
#29857=DIRECTION ( 'NONE',  ( -1.000000000000000000, -0.000000000000000000, -0.000000000000000000 ) ) ;
#29861=DIRECTION ( 'NONE',  ( -1.000000000000000000, -0.000000000000000000, -0.000000000000000000 ) ) ;
#29873=EDGE_CURVE ( 'NONE', #17998, #18878, #32092, .T. ) ;
#29876=VERTEX_POINT ( 'NONE', #29159 ) ;
#29877=CARTESIAN_POINT ( 'NONE',  ( 7.999999999999992895, -11.90021268425586953, 45.45261810511210143 ) ) ;
#29882=CARTESIAN_POINT ( 'NONE',  ( 7.999999999999992895, -18.53613841426824393, 48.58406706613897796 ) ) ;
#29886=CARTESIAN_POINT ( 'NONE',  ( 0.000000000000000000, 0.000000000000000000, 0.000000000000000000 ) ) ;
#29887=DIRECTION ( 'NONE',  ( -1.000000000000000000, -0.000000000000000000, 0.000000000000000000 ) ) ;
#29894=VERTEX_POINT ( 'NONE', #15611 ) ;
#29898=CIRCLE ( 'NONE', #16657, 52.00000000000000711 ) ;
#29904=ORIENTED_EDGE ( 'NONE', *, *, #17830, .F. ) ;
#29908=ORIENTED_EDGE ( 'NONE', *, *, #8000, .F. ) ;
#29914=ORIENTED_EDGE ( 'NONE', *, *, #11439, .F. ) ;
#29915=AXIS2_PLACEMENT_3D ( 'NONE', #20986, #31990, #15579 ) ;
#29920=CIRCLE ( 'NONE', #20681, 20.00000000000000355 ) ;
#29922=ORIENTED_EDGE ( 'NONE', *, *, #4443, .T. ) ;
#29926=DIRECTION ( 'NONE',  ( -1.000000000000000000, -0.000000000000000000, 0.000000000000000000 ) ) ;
#29935=CYLINDRICAL_SURFACE ( 'NONE', #5360, 47.49900000000001654 ) ;
#29937=ORIENTED_EDGE ( 'NONE', *, *, #16250, .F. ) ;
#29939=CARTESIAN_POINT ( 'NONE',  ( 7.999999999999992895, 17.50309955389674954, -43.60271849949345579 ) ) ;
#29943=VECTOR ( 'NONE', #12126, 1000.000000000000000 ) ;
#29947=EDGE_CURVE ( 'NONE', #17998, #28739, #13474, .T. ) ;
#29959=DIRECTION ( 'NONE',  ( -1.000000000000000000, -0.000000000000000000, -0.000000000000000000 ) ) ;
#29960=EDGE_CURVE ( 'NONE', #22165, #2676, #10588, .T. ) ;
#29967=DIRECTION ( 'NONE',  ( -1.000000000000000000, 0.000000000000000000, -0.000000000000000000 ) ) ;
#29970=CIRCLE ( 'NONE', #1775, 47.49900000000001654 ) ;
#29976=CARTESIAN_POINT ( 'NONE',  ( 7.999999999999992895, -47.22458491092817212, -5.098390039074724100 ) ) ;
#29977=ORIENTED_EDGE ( 'NONE', *, *, #5135, .T. ) ;
#29979=CARTESIAN_POINT ( 'NONE',  ( 7.999999999999992895, -32.32520163883559405, -34.09746168776067776 ) ) ;
#29983=ORIENTED_EDGE ( 'NONE', *, *, #18957, .F. ) ;
#29989=LINE ( 'NONE', #10537, #31370 ) ;
#29995=CYLINDRICAL_SURFACE ( 'NONE', #30913, 52.00000000000000711 ) ;
#29998=ORIENTED_EDGE ( 'NONE', *, *, #20089, .F. ) ;
#30005=VERTEX_POINT ( 'NONE', #11303 ) ;
#30008=ADVANCED_FACE ( 'NONE', ( #17036 ), #16325, .T. ) ;
#30013=CARTESIAN_POINT ( 'NONE',  ( 0.000000000000000000, 47.49120266317496686, -0.8606222198176971538 ) ) ;
#30016=CARTESIAN_POINT ( 'NONE',  ( 4.000000000000003553, -51.85248208264515313, -3.914090171286743747 ) ) ;
#30018=CARTESIAN_POINT ( 'NONE',  ( 0.000000000000000000, -17.08890430202781374, 43.76671000081938701 ) ) ;
#30027=CARTESIAN_POINT ( 'NONE',  ( 4.000000000000003553, -25.61928775981012762, -45.25098998563503727 ) ) ;
#30028=ORIENTED_EDGE ( 'NONE', *, *, #11492, .T. ) ;
#30034=ORIENTED_EDGE ( 'NONE', *, *, #14848, .T. ) ;
#30037=EDGE_CURVE ( 'NONE', #26487, #13043, #26185, .T. ) ;
#30039=DIRECTION ( 'NONE',  ( -1.000000000000000000, 0.000000000000000000, 0.000000000000000000 ) ) ;
#30056=CARTESIAN_POINT ( 'NONE',  ( 7.999999999999992895, -19.74581912682874929, 48.10512059033388255 ) ) ;
#30063=DIRECTION ( 'NONE',  ( 0.000000000000000000, -0.9822872507286865007, -0.1873813145857356477 ) ) ;
#30064=DIRECTION ( 'NONE',  ( 0.000000000000000000, 0.000000000000000000, 1.000000000000000000 ) ) ;
#30068=DIRECTION ( 'NONE',  ( 0.000000000000000000, 0.000000000000000000, 1.000000000000000000 ) ) ;
#30069=VERTEX_POINT ( 'NONE', #14168 ) ;
#30071=FACE_OUTER_BOUND ( 'NONE', #12824, .T. ) ;
#30077=ORIENTED_EDGE ( 'NONE', *, *, #4761, .T. ) ;
#30080=CARTESIAN_POINT ( 'NONE',  ( 7.999999999999992895, -43.83938735307256707, -18.28286404005846677 ) ) ;
#30081=CARTESIAN_POINT ( 'NONE',  ( -9.999999999999994671, 0.000000000000000000, 0.000000000000000000 ) ) ;
#30108=DIRECTION ( 'NONE',  ( 1.000000000000000000, -0.000000000000000000, 0.000000000000000000 ) ) ;
#30111=ORIENTED_EDGE ( 'NONE', *, *, #1180, .T. ) ;
#30120=LINE ( 'NONE', #30299, #32609 ) ;
#30135=AXIS2_PLACEMENT_3D ( 'NONE', #2157, #35438, #27334 ) ;
#30141=EDGE_CURVE ( 'NONE', #13559, #8148, #20084, .T. ) ;
#30149=FACE_OUTER_BOUND ( 'NONE', #707, .T. ) ;
#30151=CARTESIAN_POINT ( 'NONE',  ( 0.000000000000000000, -26.17370628620627215, -39.63700417846191471 ) ) ;
#30160=EDGE_CURVE ( 'NONE', #6684, #32280, #6610, .T. ) ;
#30173=EDGE_CURVE ( 'NONE', #14501, #28112, #15799, .T. ) ;
#30182=DIRECTION ( 'NONE',  ( 0.000000000000000000, 0.000000000000000000, 1.000000000000000000 ) ) ;
#30191=CARTESIAN_POINT ( 'NONE',  ( 7.999999999999992895, 15.49408907645234734, -44.90087086784577508 ) ) ;
#30200=EDGE_CURVE ( 'NONE', #3813, #25880, #293, .T. ) ;
#30204=DIRECTION ( 'NONE',  ( 0.000000000000000000, 0.2486898871648483555, 0.9685831611286328524 ) ) ;
#30207=ORIENTED_EDGE ( 'NONE', *, *, #1143, .T. ) ;
#30208=DIRECTION ( 'NONE',  ( -1.000000000000000000, 0.000000000000000000, 0.000000000000000000 ) ) ;
#30213=AXIS2_PLACEMENT_3D ( 'NONE', #9281, #30583, #2714 ) ;
#30215=AXIS2_PLACEMENT_3D ( 'NONE', #1364, #23503, #20778 ) ;
#30222=DIRECTION ( 'NONE',  ( -1.000000000000000000, -0.000000000000000000, -0.000000000000000000 ) ) ;
#30223=CARTESIAN_POINT ( 'NONE',  ( 7.999999999999992895, 12.30077720129095731, 50.52416135122086871 ) ) ;
#30225=FACE_OUTER_BOUND ( 'NONE', #9135, .T. ) ;
#30236=CARTESIAN_POINT ( 'NONE',  ( 0.000000000000000000, 0.000000000000000000, 0.000000000000000000 ) ) ;
#30241=VERTEX_POINT ( 'NONE', #13042 ) ;
#30243=ORIENTED_EDGE ( 'NONE', *, *, #264, .F. ) ;
#30244=EDGE_CURVE ( 'NONE', #32535, #12307, #10872, .T. ) ;
#30257=DIRECTION ( 'NONE',  ( -1.000000000000000000, -0.000000000000000000, 0.000000000000000000 ) ) ;
#30268=FACE_OUTER_BOUND ( 'NONE', #2887, .T. ) ;
#30273=ADVANCED_FACE ( 'NONE', ( #18604 ), #2067, .T. ) ;
#30280=CARTESIAN_POINT ( 'NONE',  ( 7.999999999999992895, 44.25018368420744252, 27.31155879685197263 ) ) ;
#30294=EDGE_LOOP ( 'NONE', ( #20889, #31525, #25422, #27391 ) ) ;
#30295=AXIS2_PLACEMENT_3D ( 'NONE', #17825, #28825, #9910 ) ;
#30299=CARTESIAN_POINT ( 'NONE',  ( 4.000000000000003553, -51.19683565102439360, -9.104066087303991139 ) ) ;
#30300=ORIENTED_EDGE ( 'NONE', *, *, #25173, .F. ) ;
#30317=AXIS2_PLACEMENT_3D ( 'NONE', #28595, #3946, #25544 ) ;
#30327=AXIS2_PLACEMENT_3D ( 'NONE', #27906, #33479, #5426 ) ;
#30328=CARTESIAN_POINT ( 'NONE',  ( 7.999999999999992895, 6.109652351741788223, 46.58570277113510372 ) ) ;
#30330=CARTESIAN_POINT ( 'NONE',  ( 7.999999999999992895, 22.82995208772746665, -41.06517797613640397 ) ) ;
#30340=DIRECTION ( 'NONE',  ( -1.000000000000000000, -0.000000000000000000, 0.000000000000000000 ) ) ;
#30349=CIRCLE ( 'NONE', #18820, 20.00000000000000711 ) ;
#30350=DIRECTION ( 'NONE',  ( -1.000000000000000000, -0.000000000000000000, -0.000000000000000000 ) ) ;
#30362=EDGE_CURVE ( 'NONE', #4539, #28558, #8146, .T. ) ;
#30367=AXIS2_PLACEMENT_3D ( 'NONE', #962, #22377, #31022 ) ;
#30368=DIRECTION ( 'NONE',  ( -1.000000000000000000, -0.000000000000000000, -0.000000000000000000 ) ) ;
#30374=AXIS2_PLACEMENT_3D ( 'NONE', #28189, #26021, #22945 ) ;
#30392=ORIENTED_EDGE ( 'NONE', *, *, #15851, .T. ) ;
#30398=VECTOR ( 'NONE', #4074, 1000.000000000000000 ) ;
#30401=EDGE_LOOP ( 'NONE', ( #32921, #21332, #7649, #2518 ) ) ;
#30402=ORIENTED_EDGE ( 'NONE', *, *, #8805, .F. ) ;
#30404=ADVANCED_FACE ( 'NONE', ( #7795 ), #13390, .T. ) ;
#30409=ORIENTED_EDGE ( 'NONE', *, *, #27677, .F. ) ;
#30418=ORIENTED_EDGE ( 'NONE', *, *, #13022, .T. ) ;
#30426=ORIENTED_EDGE ( 'NONE', *, *, #2910, .F. ) ;
#30428=CARTESIAN_POINT ( 'NONE',  ( 0.000000000000000000, 0.000000000000000000, 0.000000000000000000 ) ) ;
#30432=EDGE_LOOP ( 'NONE', ( #34720, #23412, #32726, #29625 ) ) ;
#30437=DIRECTION ( 'NONE',  ( 0.000000000000000000, 0.000000000000000000, 1.000000000000000000 ) ) ;
#30440=EDGE_CURVE ( 'NONE', #20040, #22033, #225, .T. ) ;
#30442=LINE ( 'NONE', #19256, #24012 ) ;
#30443=EDGE_CURVE ( 'NONE', #7406, #20345, #32521, .T. ) ;
#30449=EDGE_CURVE ( 'NONE', #32215, #30567, #22746, .T. ) ;
#30450=VECTOR ( 'NONE', #6219, 1000.000000000000000 ) ;
#30455=CIRCLE ( 'NONE', #33301, 52.00000000000000711 ) ;
#30458=LINE ( 'NONE', #28104, #34071 ) ;
#30465=EDGE_LOOP ( 'NONE', ( #24878, #22391, #7829, #6429 ) ) ;
#30471=ORIENTED_EDGE ( 'NONE', *, *, #20047, .T. ) ;
#30473=FACE_OUTER_BOUND ( 'NONE', #9609, .T. ) ;
#30480=ADVANCED_FACE ( 'NONE', ( #9038 ), #19814, .T. ) ;
#30486=CIRCLE ( 'NONE', #21831, 52.00000000000000711 ) ;
#30487=CARTESIAN_POINT ( 'NONE',  ( 0.000000000000000000, 46.87740477351712798, 3.172455868806031809 ) ) ;
#30488=AXIS2_PLACEMENT_3D ( 'NONE', #21927, #15625, #15986 ) ;
#30489=DIRECTION ( 'NONE',  ( -1.000000000000000000, 0.000000000000000000, 0.000000000000000000 ) ) ;
#30490=ORIENTED_EDGE ( 'NONE', *, *, #27088, .T. ) ;
#30494=CYLINDRICAL_SURFACE ( 'NONE', #8561, 20.00000000000000355 ) ;
#30497=DIRECTION ( 'NONE',  ( -1.000000000000000000, -0.000000000000000000, 0.000000000000000000 ) ) ;
#30502=DIRECTION ( 'NONE',  ( 0.000000000000000000, 0.9510565162951521989, 0.3090169943749515036 ) ) ;
#30504=CIRCLE ( 'NONE', #35121, 20.00000000000000711 ) ;
#30507=CARTESIAN_POINT ( 'NONE',  ( 7.999999999999992895, -46.11014828289837197, -9.022736828081189486 ) ) ;
#30508=CARTESIAN_POINT ( 'NONE',  ( 7.999999999999992895, 0.000000000000000000, 0.000000000000000000 ) ) ;
#30509=ORIENTED_EDGE ( 'NONE', *, *, #10982, .T. ) ;
#30513=CARTESIAN_POINT ( 'NONE',  ( 0.000000000000000000, -25.61928775981074935, 45.25098998563470332 ) ) ;
#30515=LINE ( 'NONE', #14456, #19329 ) ;
#30516=VERTEX_POINT ( 'NONE', #579 ) ;
#30518=CARTESIAN_POINT ( 'NONE',  ( 7.999999999999992895, 35.20873326984128227, -31.88259874183993503 ) ) ;
#30523=ORIENTED_EDGE ( 'NONE', *, *, #25807, .F. ) ;
#30527=EDGE_CURVE ( 'NONE', #14196, #3377, #16983, .T. ) ;
#30535=DIRECTION ( 'NONE',  ( 0.000000000000000000, 0.000000000000000000, 1.000000000000000000 ) ) ;
#30538=FACE_OUTER_BOUND ( 'NONE', #27377, .T. ) ;
#30551=CARTESIAN_POINT ( 'NONE',  ( 7.999999999999992895, 13.85708833600033074, -45.43276465116652219 ) ) ;
#30554=VERTEX_POINT ( 'NONE', #8853 ) ;
#30559=ORIENTED_EDGE ( 'NONE', *, *, #18094, .T. ) ;
#30561=VERTEX_POINT ( 'NONE', #3124 ) ;
#30563=CARTESIAN_POINT ( 'NONE',  ( 0.000000000000000000, 36.34385289850631295, -29.77717097092039111 ) ) ;
#30567=VERTEX_POINT ( 'NONE', #14076 ) ;
#30569=DIRECTION ( 'NONE',  ( 1.000000000000000000, 0.000000000000000000, 0.000000000000000000 ) ) ;
#30572=EDGE_LOOP ( 'NONE', ( #13601, #30646, #17254, #25252, #18402, #25610 ) ) ;
#30583=DIRECTION ( 'NONE',  ( -1.000000000000000000, -0.000000000000000000, 0.000000000000000000 ) ) ;
#30588=CARTESIAN_POINT ( 'NONE',  ( 7.999999999999992895, 15.49408907645171851, 44.90087086784599535 ) ) ;
#30589=EDGE_LOOP ( 'NONE', ( #33090, #28128, #19891, #18342 ) ) ;
#30591=CARTESIAN_POINT ( 'NONE',  ( 7.999999999999992895, 42.41764978026606059, -20.20639853260303198 ) ) ;
#30593=ORIENTED_EDGE ( 'NONE', *, *, #1601, .F. ) ;
#30602=CARTESIAN_POINT ( 'NONE',  ( 0.000000000000000000, 42.60732521687599217, -19.80331771201615609 ) ) ;
#30606=CARTESIAN_POINT ( 'NONE',  ( 7.999999999999992895, 39.55064067543064965, 25.36340625197373910 ) ) ;
#30623=DIRECTION ( 'NONE',  ( 1.000000000000000000, -0.000000000000000000, 0.000000000000000000 ) ) ;
#30640=DIRECTION ( 'NONE',  ( -1.000000000000000000, 0.000000000000000000, -0.000000000000000000 ) ) ;
#30642=EDGE_CURVE ( 'NONE', #1965, #21046, #12674, .T. ) ;
#30646=ORIENTED_EDGE ( 'NONE', *, *, #27324, .F. ) ;
#30649=AXIS2_PLACEMENT_3D ( 'NONE', #1261, #4159, #1441 ) ;
#30650=ORIENTED_EDGE ( 'NONE', *, *, #14607, .F. ) ;
#30653=AXIS2_PLACEMENT_3D ( 'NONE', #19680, #6544, #9076 ) ;
#30655=EDGE_CURVE ( 'NONE', #31131, #27160, #23009, .T. ) ;
#30656=CARTESIAN_POINT ( 'NONE',  ( 4.000000000000003553, 47.32430374665931794, 21.55018039121545215 ) ) ;
#30658=ORIENTED_EDGE ( 'NONE', *, *, #26880, .T. ) ;
#30660=DIRECTION ( 'NONE',  ( -1.000000000000000000, 0.000000000000000000, 0.000000000000000000 ) ) ;
#30670=ADVANCED_FACE ( 'NONE', ( #1845 ), #20888, .T. ) ;
#30676=VECTOR ( 'NONE', #20636, 1000.000000000000000 ) ;
#30677=ADVANCED_FACE ( 'NONE', ( #23441 ), #28482, .T. ) ;
#30678=ORIENTED_EDGE ( 'NONE', *, *, #4724, .F. ) ;
#30680=DIRECTION ( 'NONE',  ( -1.000000000000000000, -0.000000000000000000, -0.000000000000000000 ) ) ;
#30681=DIRECTION ( 'NONE',  ( 0.000000000000000000, 0.000000000000000000, 1.000000000000000000 ) ) ;
#30690=EDGE_CURVE ( 'NONE', #6413, #9689, #2384, .T. ) ;
#30694=VERTEX_POINT ( 'NONE', #31180 ) ;
#30697=DIRECTION ( 'NONE',  ( -1.000000000000000000, 0.000000000000000000, 0.000000000000000000 ) ) ;
#30704=CIRCLE ( 'NONE', #3672, 47.49900000000001654 ) ;
#30706=CYLINDRICAL_SURFACE ( 'NONE', #35021, 47.49900000000001654 ) ;
#30713=EDGE_CURVE ( 'NONE', #7261, #14579, #7221, .T. ) ;
#30714=DIRECTION ( 'NONE',  ( -1.000000000000000000, 0.000000000000000000, 0.000000000000000000 ) ) ;
#30719=CARTESIAN_POINT ( 'NONE',  ( 7.999999999999992895, -8.053585752062238257, 46.81126742072021329 ) ) ;
#30721=AXIS2_PLACEMENT_3D ( 'NONE', #21238, #21762, #24484 ) ;
#30722=CARTESIAN_POINT ( 'NONE',  ( 7.999999999999992895, -26.17370628620627215, -39.63700417846191471 ) ) ;
#30729=ORIENTED_EDGE ( 'NONE', *, *, #15092, .T. ) ;
#30731=FACE_OUTER_BOUND ( 'NONE', #4957, .T. ) ;
#30733=ORIENTED_EDGE ( 'NONE', *, *, #4051, .T. ) ;
#30735=DIRECTION ( 'NONE',  ( 0.000000000000000000, 0.000000000000000000, 1.000000000000000000 ) ) ;
#30742=AXIS2_PLACEMENT_3D ( 'NONE', #24439, #35425, #26978 ) ;
#30744=CARTESIAN_POINT ( 'NONE',  ( 0.000000000000000000, 0.000000000000000000, 0.000000000000000000 ) ) ;
#30747=VECTOR ( 'NONE', #33463, 1000.000000000000000 ) ;
#30750=CARTESIAN_POINT ( 'NONE',  ( -9.999999999999994671, 0.000000000000000000, 0.000000000000000000 ) ) ;
#30751=EDGE_CURVE ( 'NONE', #14247, #29371, #29970, .T. ) ;
#30754=DIRECTION ( 'NONE',  ( 0.000000000000000000, 0.3681245526846786964, -0.9297764858882511252 ) ) ;
#30757=DIRECTION ( 'NONE',  ( -1.000000000000000000, 0.000000000000000000, 0.000000000000000000 ) ) ;
#30759=CARTESIAN_POINT ( 'NONE',  ( 0.000000000000000000, 36.06787431788733045, -37.45808914225451502 ) ) ;
#30762=CARTESIAN_POINT ( 'NONE',  ( 7.999999999999992895, 2.123073309835184830, 47.45152853935336168 ) ) ;
#30766=CYLINDRICAL_SURFACE ( 'NONE', #12349, 20.00000000000000355 ) ;
#30768=VERTEX_POINT ( 'NONE', #18019 ) ;
#30777=ORIENTED_EDGE ( 'NONE', *, *, #7516, .F. ) ;
#30780=EDGE_CURVE ( 'NONE', #35108, #6583, #16136, .T. ) ;
#30790=AXIS2_PLACEMENT_3D ( 'NONE', #1911, #24223, #13074 ) ;
#30792=CYLINDRICAL_SURFACE ( 'NONE', #3986, 20.00000000000000711 ) ;
#30793=DIRECTION ( 'NONE',  ( 0.000000000000000000, -0.1253332335642905471, -0.9921147013144795412 ) ) ;
#30805=DIRECTION ( 'NONE',  ( 0.000000000000000000, 0.9822872507286879440, 0.1873813145857285700 ) ) ;
#30807=VECTOR ( 'NONE', #19424, 1000.000000000000000 ) ;
#30808=ORIENTED_EDGE ( 'NONE', *, *, #6679, .F. ) ;
#30809=DIRECTION ( 'NONE',  ( -1.000000000000000000, 0.000000000000000000, -0.000000000000000000 ) ) ;
#30810=ORIENTED_EDGE ( 'NONE', *, *, #3341, .F. ) ;
#30821=ORIENTED_EDGE ( 'NONE', *, *, #4478, .T. ) ;
#30827=VERTEX_POINT ( 'NONE', #18734 ) ;
#30831=LINE ( 'NONE', #8682, #26369 ) ;
#30833=ORIENTED_EDGE ( 'NONE', *, *, #15417, .T. ) ;
#30834=VECTOR ( 'NONE', #9424, 1000.000000000000000 ) ;
#30836=EDGE_CURVE ( 'NONE', #16982, #22664, #4731, .T. ) ;
#30845=CARTESIAN_POINT ( 'NONE',  ( 7.999999999999992895, 46.21320724403665281, -10.97699764141904488 ) ) ;
#30850=DIRECTION ( 'NONE',  ( -1.000000000000000000, -0.000000000000000000, -0.000000000000000000 ) ) ;
#30858=LINE ( 'NONE', #783, #27637 ) ;
#30864=ORIENTED_EDGE ( 'NONE', *, *, #20768, .F. ) ;
#30867=DIRECTION ( 'NONE',  ( -1.000000000000000000, -0.000000000000000000, 0.000000000000000000 ) ) ;
#30870=ORIENTED_EDGE ( 'NONE', *, *, #7516, .T. ) ;
#30871=EDGE_CURVE ( 'NONE', #5721, #9761, #14985, .T. ) ;
#30873=VERTEX_POINT ( 'NONE', #16374 ) ;
#30874=ORIENTED_EDGE ( 'NONE', *, *, #524, .T. ) ;
#30875=CARTESIAN_POINT ( 'NONE',  ( 4.000000000000003553, 46.77034588191337150, -22.72740077717178053 ) ) ;
#30876=CIRCLE ( 'NONE', #35491, 20.00000000000000711 ) ;
#30879=CIRCLE ( 'NONE', #8436, 20.00000000000000355 ) ;
#30881=LINE ( 'NONE', #12325, #32190 ) ;
#30893=CARTESIAN_POINT ( 'NONE',  ( 0.000000000000000000, 0.000000000000000000, 0.000000000000000000 ) ) ;
#30897=VECTOR ( 'NONE', #22766, 1000.000000000000000 ) ;
#30899=DIRECTION ( 'NONE',  ( 0.000000000000000000, 0.000000000000000000, 1.000000000000000000 ) ) ;
#30900=ORIENTED_EDGE ( 'NONE', *, *, #19126, .F. ) ;
#30909=FACE_OUTER_BOUND ( 'NONE', #32581, .T. ) ;
#30913=AXIS2_PLACEMENT_3D ( 'NONE', #16276, #13599, #24594 ) ;
#30920=ORIENTED_EDGE ( 'NONE', *, *, #6902, .F. ) ;
#30926=DIRECTION ( 'NONE',  ( 0.000000000000000000, 0.5877852522924743583, -0.8090169943749466741 ) ) ;
#30927=AXIS2_PLACEMENT_3D ( 'NONE', #8558, #19530, #6041 ) ;
#30948=LINE ( 'NONE', #6106, #25193 ) ;
#30953=AXIS2_PLACEMENT_3D ( 'NONE', #3362, #8208, #11101 ) ;
#30956=DIRECTION ( 'NONE',  ( -1.000000000000000000, 0.000000000000000000, 0.000000000000000000 ) ) ;
#30983=ORIENTED_EDGE ( 'NONE', *, *, #5211, .F. ) ;
#30986=VERTEX_POINT ( 'NONE', #3607 ) ;
#30997=EDGE_LOOP ( 'NONE', ( #33424, #34250, #20500, #31260 ) ) ;
#31002=CARTESIAN_POINT ( 'NONE',  ( 7.999999999999992895, 17.50309955389611716, 43.60271849949368317 ) ) ;
#31004=ORIENTED_EDGE ( 'NONE', *, *, #13467, .F. ) ;
#31008=EDGE_CURVE ( 'NONE', #32720, #11477, #3082, .T. ) ;
#31014=DIRECTION ( 'NONE',  ( 0.000000000000000000, 0.000000000000000000, 1.000000000000000000 ) ) ;
#31016=CARTESIAN_POINT ( 'NONE',  ( 0.000000000000000000, 0.000000000000000000, -3.000000000000002665 ) ) ;
#31017=CARTESIAN_POINT ( 'NONE',  ( 7.999999999999992895, 42.03146605346819342, -22.12489237027273603 ) ) ;
#31022=DIRECTION ( 'NONE',  ( 0.000000000000000000, 0.000000000000000000, -1.000000000000000000 ) ) ;
#31023=CARTESIAN_POINT ( 'NONE',  ( 0.000000000000000000, 0.000000000000000000, 0.000000000000000000 ) ) ;
#31024=CYLINDRICAL_SURFACE ( 'NONE', #15096, 52.00000000000000711 ) ;
#31026=ORIENTED_EDGE ( 'NONE', *, *, #25553, .T. ) ;
#31035=CIRCLE ( 'NONE', #15501, 52.00000000000000711 ) ;
#31036=CARTESIAN_POINT ( 'NONE',  ( 4.000000000000003553, 50.95304419620825342, 10.38206564895680017 ) ) ;
#31039=DIRECTION ( 'NONE',  ( -1.000000000000000000, 0.000000000000000000, -0.000000000000000000 ) ) ;
#31041=CYLINDRICAL_SURFACE ( 'NONE', #19960, 52.00000000000000711 ) ;
#31042=LINE ( 'NONE', #23103, #23163 ) ;
#31044=ORIENTED_EDGE ( 'NONE', *, *, #33602, .F. ) ;
#31045=ADVANCED_FACE ( 'NONE', ( #17084 ), #17261, .T. ) ;
#31051=CARTESIAN_POINT ( 'NONE',  ( 0.000000000000000000, 39.55064067543064965, 25.36340625197373910 ) ) ;
#31054=FACE_OUTER_BOUND ( 'NONE', #28295, .T. ) ;
#31056=DIRECTION ( 'NONE',  ( -1.000000000000000000, 0.000000000000000000, 0.000000000000000000 ) ) ;
#31062=CARTESIAN_POINT ( 'NONE',  ( 0.000000000000000000, -36.05989434073634925, 30.12041790338604130 ) ) ;
#31066=CARTESIAN_POINT ( 'NONE',  ( 7.999999999999992895, -19.44205635905512608, -43.33776004284631256 ) ) ;
#31076=DIRECTION ( 'NONE',  ( -1.000000000000000000, 0.000000000000000000, 0.000000000000000000 ) ) ;
#31087=DIRECTION ( 'NONE',  ( 0.000000000000000000, 0.000000000000000000, 1.000000000000000000 ) ) ;
#31091=ORIENTED_EDGE ( 'NONE', *, *, #21166, .F. ) ;
#31095=DIRECTION ( 'NONE',  ( 0.000000000000000000, -0.5877852522924803536, 0.8090169943749422332 ) ) ;
#31101=ORIENTED_EDGE ( 'NONE', *, *, #24883, .F. ) ;
#31118=CARTESIAN_POINT ( 'NONE',  ( 7.999999999999992895, -36.05989434073634925, 30.12041790338604130 ) ) ;
#31119=CYLINDRICAL_SURFACE ( 'NONE', #35366, 52.00000000000000711 ) ;
#31129=DIRECTION ( 'NONE',  ( -1.000000000000000000, -0.000000000000000000, -0.000000000000000000 ) ) ;
#31131=VERTEX_POINT ( 'NONE', #14915 ) ;
#31134=EDGE_CURVE ( 'NONE', #6583, #26304, #35172, .T. ) ;
#31137=VERTEX_POINT ( 'NONE', #20306 ) ;
#31139=AXIS2_PLACEMENT_3D ( 'NONE', #32083, #10475, #32434 ) ;
#31141=DIRECTION ( 'NONE',  ( 0.000000000000000000, 0.000000000000000000, 1.000000000000000000 ) ) ;
#31147=DIRECTION ( 'NONE',  ( -1.000000000000000000, -0.000000000000000000, 0.000000000000000000 ) ) ;
#31156=DIRECTION ( 'NONE',  ( 0.000000000000000000, 0.8443279255020161855, -0.5358267949789946583 ) ) ;
#31158=EDGE_CURVE ( 'NONE', #12983, #3192, #26533, .T. ) ;
#31159=ORIENTED_EDGE ( 'NONE', *, *, #31158, .F. ) ;
#31161=ORIENTED_EDGE ( 'NONE', *, *, #2042, .T. ) ;
#31180=CARTESIAN_POINT ( 'NONE',  ( 0.000000000000000000, -51.93417535146743802, 2.615612846549014492 ) ) ;
#31181=ORIENTED_EDGE ( 'NONE', *, *, #35259, .T. ) ;
#31189=CYLINDRICAL_SURFACE ( 'NONE', #17757, 20.00000000000000711 ) ;
#31197=CIRCLE ( 'NONE', #26042, 52.00000000000000711 ) ;
#31199=EDGE_CURVE ( 'NONE', #23286, #7406, #9168, .T. ) ;
#31201=CARTESIAN_POINT ( 'NONE',  ( 7.999999999999992895, 0.000000000000000000, 0.000000000000000000 ) ) ;
#31207=AXIS2_PLACEMENT_3D ( 'NONE', #24129, #32568, #7551 ) ;
#31217=CARTESIAN_POINT ( 'NONE',  ( 7.999999999999992895, -27.79676263918213763, 37.88001506494759241 ) ) ;
#31227=DIRECTION ( 'NONE',  ( -1.000000000000000000, 0.000000000000000000, -0.000000000000000000 ) ) ;
#31228=AXIS2_PLACEMENT_3D ( 'NONE', #31416, #15020, #21137 ) ;
#31234=CIRCLE ( 'NONE', #15697, 20.00000000000000711 ) ;
#31235=DIRECTION ( 'NONE',  ( 0.000000000000000000, -0.9048270524660235736, 0.4257792915650641663 ) ) ;
#31239=CARTESIAN_POINT ( 'NONE',  ( 0.000000000000000000, -13.56094713063606072, 50.20060470671736397 ) ) ;
#31240=ADVANCED_FACE ( 'NONE', ( #14741 ), #28796, .T. ) ;
#31242=LINE ( 'NONE', #8912, #23794 ) ;
#31257=CARTESIAN_POINT ( 'NONE',  ( 0.000000000000000000, 27.79676263918241119, -37.88001506494740056 ) ) ;
#31260=ORIENTED_EDGE ( 'NONE', *, *, #3063, .F. ) ;
#31264=CARTESIAN_POINT ( 'NONE',  ( 7.999999999999992895, 49.25004636492389665, 16.68630974939777545 ) ) ;
#31267=ORIENTED_EDGE ( 'NONE', *, *, #16026, .T. ) ;
#31268=DIRECTION ( 'NONE',  ( 0.000000000000000000, 0.9510565162951521989, 0.3090169943749514481 ) ) ;
#31271=EDGE_CURVE ( 'NONE', #4101, #17645, #69, .T. ) ;
#31283=CIRCLE ( 'NONE', #11164, 47.49900000000003075 ) ;
#31285=EDGE_CURVE ( 'NONE', #11684, #8621, #32381, .T. ) ;
#31288=CARTESIAN_POINT ( 'NONE',  ( 0.000000000000000000, -35.11945359308084846, -38.34871548466050939 ) ) ;
#31289=CARTESIAN_POINT ( 'NONE',  ( 0.000000000000000000, -11.46872990052349550, -45.56340405422456996 ) ) ;
#31294=DIRECTION ( 'NONE',  ( -1.000000000000000000, 0.000000000000000000, -0.000000000000000000 ) ) ;
#31296=DIRECTION ( 'NONE',  ( 0.000000000000000000, 0.1253332335643046747, -0.9921147013144777649 ) ) ;
#31322=FACE_OUTER_BOUND ( 'NONE', #24368, .T. ) ;
#31327=EDGE_CURVE ( 'NONE', #18878, #22481, #14441, .T. ) ;
#31331=DIRECTION ( 'NONE',  ( -1.000000000000000000, -0.000000000000000000, 0.000000000000000000 ) ) ;
#31337=CARTESIAN_POINT ( 'NONE',  ( 7.999999999999992895, 19.74581912682909390, -48.10512059033372623 ) ) ;
#31343=AXIS2_PLACEMENT_3D ( 'NONE', #16137, #21728, #27155 ) ;
#31358=EDGE_CURVE ( 'NONE', #4138, #21338, #1971, .T. ) ;
#31359=DIRECTION ( 'NONE',  ( 0.000000000000000000, 0.000000000000000000, 1.000000000000000000 ) ) ;
#31360=VERTEX_POINT ( 'NONE', #34737 ) ;
#31369=LINE ( 'NONE', #35508, #2863 ) ;
#31370=VECTOR ( 'NONE', #13422, 1000.000000000000000 ) ;
#31379=CARTESIAN_POINT ( 'NONE',  ( 0.000000000000000000, 47.22458491092820765, 5.098390039074404356 ) ) ;
#31382=EDGE_LOOP ( 'NONE', ( #21471, #16811, #7574, #30392 ) ) ;
#31383=DIRECTION ( 'NONE',  ( -1.000000000000000000, -0.000000000000000000, 0.000000000000000000 ) ) ;
#31401=AXIS2_PLACEMENT_3D ( 'NONE', #5234, #14016, #25009 ) ;
#31402=ORIENTED_EDGE ( 'NONE', *, *, #23135, .T. ) ;
#31411=ADVANCED_FACE ( 'NONE', ( #13311 ), #29685, .T. ) ;
#31412=DIRECTION ( 'NONE',  ( -1.000000000000000000, -0.000000000000000000, -0.000000000000000000 ) ) ;
#31416=CARTESIAN_POINT ( 'NONE',  ( 0.000000000000000000, -27.79676263918213763, 37.88001506494759241 ) ) ;
#31417=AXIS2_PLACEMENT_3D ( 'NONE', #25467, #786, #22744 ) ;
#31418=AXIS2_PLACEMENT_3D ( 'NONE', #30893, #31426, #25680 ) ;
#31426=DIRECTION ( 'NONE',  ( -1.000000000000000000, -0.000000000000000000, 0.000000000000000000 ) ) ;
#31427=AXIS2_PLACEMENT_3D ( 'NONE', #22593, #28024, #3372 ) ;
#31435=LINE ( 'NONE', #9464, #10661 ) ;
#31438=AXIS2_PLACEMENT_3D ( 'NONE', #19744, #17233, #33819 ) ;
#31441=CYLINDRICAL_SURFACE ( 'NONE', #19217, 20.00000000000000355 ) ;
#31446=CIRCLE ( 'NONE', #26862, 20.00000000000000355 ) ;
#31447=DIRECTION ( 'NONE',  ( 1.000000000000000000, 0.000000000000000000, 0.000000000000000000 ) ) ;
#31450=EDGE_CURVE ( 'NONE', #933, #11196, #19053, .T. ) ;
#31453=CIRCLE ( 'NONE', #23007, 47.49900000000001654 ) ;
#31456=VERTEX_POINT ( 'NONE', #2511 ) ;
#31457=ORIENTED_EDGE ( 'NONE', *, *, #4084, .T. ) ;
#31462=CYLINDRICAL_SURFACE ( 'NONE', #416, 52.00000000000000711 ) ;
#31468=CIRCLE ( 'NONE', #34326, 20.00000000000000711 ) ;
#31470=CARTESIAN_POINT ( 'NONE',  ( 7.999999999999992895, 18.53613841426789932, 48.58406706613910586 ) ) ;
#31479=VECTOR ( 'NONE', #31966, 1000.000000000000000 ) ;
#31483=AXIS2_PLACEMENT_3D ( 'NONE', #13341, #2727, #22128 ) ;
#31484=FACE_OUTER_BOUND ( 'NONE', #5834, .T. ) ;
#31490=DIRECTION ( 'NONE',  ( -1.000000000000000000, 0.000000000000000000, -0.000000000000000000 ) ) ;
#31492=ORIENTED_EDGE ( 'NONE', *, *, #9630, .F. ) ;
#31495=VECTOR ( 'NONE', #23533, 1000.000000000000000 ) ;
#31501=DIRECTION ( 'NONE',  ( 0.000000000000000000, 0.9980267284282717810, -0.06279051952930997382 ) ) ;
#31505=CIRCLE ( 'NONE', #15960, 52.00000000000000711 ) ;
#31514=DIRECTION ( 'NONE',  ( 0.000000000000000000, 0.000000000000000000, 1.000000000000000000 ) ) ;
#31525=ORIENTED_EDGE ( 'NONE', *, *, #24958, .F. ) ;
#31528=VECTOR ( 'NONE', #6958, 1000.000000000000000 ) ;
#31530=VERTEX_POINT ( 'NONE', #33607 ) ;
#31537=AXIS2_PLACEMENT_3D ( 'NONE', #2156, #13130, #26987 ) ;
#31544=DIRECTION ( 'NONE',  ( -1.000000000000000000, 0.000000000000000000, 0.000000000000000000 ) ) ;
#31546=CARTESIAN_POINT ( 'NONE',  ( 0.000000000000000000, 0.000000000000000000, 0.000000000000000000 ) ) ;
#31553=EDGE_LOOP ( 'NONE', ( #4732, #28447, #1032, #6164 ) ) ;
#31555=EDGE_CURVE ( 'NONE', #5428, #21923, #2690, .T. ) ;
#31558=CARTESIAN_POINT ( 'NONE',  ( 0.000000000000000000, 45.78515115856061612, -12.64416602183615623 ) ) ;
#31561=DIRECTION ( 'NONE',  ( -1.000000000000000000, -0.000000000000000000, 0.000000000000000000 ) ) ;
#31580=ORIENTED_EDGE ( 'NONE', *, *, #12787, .T. ) ;
#31583=EDGE_LOOP ( 'NONE', ( #25223, #2438, #21210, #32197 ) ) ;
#31587=DIRECTION ( 'NONE',  ( 0.000000000000000000, 0.000000000000000000, -1.000000000000000000 ) ) ;
#31591=DIRECTION ( 'NONE',  ( -1.000000000000000000, -0.000000000000000000, 0.000000000000000000 ) ) ;
#31599=DIRECTION ( 'NONE',  ( -1.000000000000000000, 0.000000000000000000, 0.000000000000000000 ) ) ;
#31602=DIRECTION ( 'NONE',  ( 1.000000000000000000, -0.000000000000000000, -0.000000000000000000 ) ) ;
#31607=VERTEX_POINT ( 'NONE', #4282 ) ;
#31610=CARTESIAN_POINT ( 'NONE',  ( 0.000000000000000000, 8.053585752061906078, 46.81126742072027014 ) ) ;
#31611=VERTEX_POINT ( 'NONE', #25887 ) ;
#31615=ORIENTED_EDGE ( 'NONE', *, *, #8238, .T. ) ;
#31618=AXIS2_PLACEMENT_3D ( 'NONE', #2883, #19578, #27362 ) ;
#31619=CARTESIAN_POINT ( 'NONE',  ( 7.999999999999992895, -24.72041153920761758, 40.55929306992680949 ) ) ;
#31620=DIRECTION ( 'NONE',  ( -1.000000000000000000, -0.000000000000000000, -0.000000000000000000 ) ) ;
#31624=DIRECTION ( 'NONE',  ( 0.000000000000000000, 0.3681245526846786964, -0.9297764858882511252 ) ) ;
#31634=DIRECTION ( 'NONE',  ( 0.000000000000000000, -0.2486898871648622611, 0.9685831611286292997 ) ) ;
#31638=DIRECTION ( 'NONE',  ( -1.000000000000000000, 0.000000000000000000, 0.000000000000000000 ) ) ;
#31642=EDGE_CURVE ( 'NONE', #35403, #2939, #9875, .T. ) ;
#31644=FACE_OUTER_BOUND ( 'NONE', #27742, .T. ) ;
#31645=DIRECTION ( 'NONE',  ( 1.000000000000000000, -0.000000000000000000, -0.000000000000000000 ) ) ;
#31646=ORIENTED_EDGE ( 'NONE', *, *, #27301, .F. ) ;
#31647=AXIS2_PLACEMENT_3D ( 'NONE', #34095, #3681, #22921 ) ;
#31650=DIRECTION ( 'NONE',  ( -1.000000000000000000, 0.000000000000000000, -0.000000000000000000 ) ) ;
#31652=VERTEX_POINT ( 'NONE', #9481 ) ;
#31658=ORIENTED_EDGE ( 'NONE', *, *, #16337, .F. ) ;
#31660=DIRECTION ( 'NONE',  ( -1.000000000000000000, 0.000000000000000000, 0.000000000000000000 ) ) ;
#31662=AXIS2_PLACEMENT_3D ( 'NONE', #16870, #12203, #28589 ) ;
#31664=ORIENTED_EDGE ( 'NONE', *, *, #9301, .F. ) ;
#31680=CARTESIAN_POINT ( 'NONE',  ( 0.000000000000000000, 20.99948489194422763, 42.60488980472790388 ) ) ;
#31684=FACE_OUTER_BOUND ( 'NONE', #15227, .T. ) ;
#31692=DIRECTION ( 'NONE',  ( 1.000000000000000000, -0.000000000000000000, -0.000000000000000000 ) ) ;
#31694=DIRECTION ( 'NONE',  ( -1.000000000000000000, 0.000000000000000000, 0.000000000000000000 ) ) ;
#31703=AXIS2_PLACEMENT_3D ( 'NONE', #7368, #15980, #29339 ) ;
#31705=EDGE_CURVE ( 'NONE', #10010, #33387, #4144, .T. ) ;
#31708=VERTEX_POINT ( 'NONE', #25523 ) ;
#31711=DIRECTION ( 'NONE',  ( 0.000000000000000000, 0.8443279255020124108, 0.5358267949790006535 ) ) ;
#31713=VERTEX_POINT ( 'NONE', #838 ) ;
#31723=CIRCLE ( 'NONE', #32889, 52.00000000000000711 ) ;
#31724=EDGE_CURVE ( 'NONE', #35356, #12864, #23082, .T. ) ;
#31732=VERTEX_POINT ( 'NONE', #34339 ) ;
#31733=EDGE_CURVE ( 'NONE', #19728, #966, #26557, .T. ) ;
#31734=FACE_OUTER_BOUND ( 'NONE', #31843, .T. ) ;
#31735=CYLINDRICAL_SURFACE ( 'NONE', #7621, 52.00000000000000711 ) ;
#31746=VERTEX_POINT ( 'NONE', #7137 ) ;
#31755=ORIENTED_EDGE ( 'NONE', *, *, #13888, .T. ) ;
#31759=EDGE_CURVE ( 'NONE', #5115, #29876, #22514, .T. ) ;
#31761=AXIS2_PLACEMENT_3D ( 'NONE', #17323, #33546, #19664 ) ;
#31762=EDGE_CURVE ( 'NONE', #27203, #29543, #23690, .T. ) ;
#31776=DIRECTION ( 'NONE',  ( -1.000000000000000000, -0.000000000000000000, 0.000000000000000000 ) ) ;
#31781=CARTESIAN_POINT ( 'NONE',  ( 0.000000000000000000, 0.000000000000000000, 0.000000000000000000 ) ) ;
#31785=FACE_OUTER_BOUND ( 'NONE', #15134, .T. ) ;
#31789=ORIENTED_EDGE ( 'NONE', *, *, #27121, .T. ) ;
#31795=ORIENTED_EDGE ( 'NONE', *, *, #13536, .F. ) ;
#31796=CARTESIAN_POINT ( 'NONE',  ( 0.000000000000000000, 17.50309955389674954, -43.60271849949345579 ) ) ;
#31801=DIRECTION ( 'NONE',  ( -1.000000000000000000, -0.000000000000000000, 0.000000000000000000 ) ) ;
#31809=DIRECTION ( 'NONE',  ( -1.000000000000000000, -0.000000000000000000, -0.000000000000000000 ) ) ;
#31819=DIRECTION ( 'NONE',  ( 0.000000000000000000, 0.000000000000000000, 1.000000000000000000 ) ) ;
#31833=CARTESIAN_POINT ( 'NONE',  ( 0.000000000000000000, 0.000000000000000000, 0.000000000000000000 ) ) ;
#31843=EDGE_LOOP ( 'NONE', ( #33504, #19563, #11778, #14549 ) ) ;
#31850=CARTESIAN_POINT ( 'NONE',  ( 0.000000000000000000, -22.43957647427188817, 41.27978878573619426 ) ) ;
#31858=ADVANCED_FACE ( 'NONE', ( #4644 ), #21345, .T. ) ;
#31860=FACE_OUTER_BOUND ( 'NONE', #1560, .T. ) ;
#31862=CARTESIAN_POINT ( 'NONE',  ( 7.999999999999992895, -34.03046037009232094, -33.13733193845841640 ) ) ;
#31871=EDGE_LOOP ( 'NONE', ( #28143, #3786, #30870, #12974 ) ) ;
#31877=CARTESIAN_POINT ( 'NONE',  ( 0.000000000000000000, -24.72041153920761758, 40.55929306992680949 ) ) ;
#31892=EDGE_CURVE ( 'NONE', #12629, #29368, #15055, .T. ) ;
#31893=DIRECTION ( 'NONE',  ( -1.000000000000000000, -0.000000000000000000, -0.000000000000000000 ) ) ;
#31894=ORIENTED_EDGE ( 'NONE', *, *, #35235, .F. ) ;
#31897=VECTOR ( 'NONE', #11811, 1000.000000000000000 ) ;
#31915=DIRECTION ( 'NONE',  ( 0.000000000000000000, 0.4817536741017164337, -0.8763066800438629178 ) ) ;
#31921=CYLINDRICAL_SURFACE ( 'NONE', #18748, 47.49900000000001654 ) ;
#31934=VECTOR ( 'NONE', #7268, 1000.000000000000000 ) ;
#31940=CIRCLE ( 'NONE', #34236, 20.00000000000000711 ) ;
#31941=APPLICATION_CONTEXT ( 'automotive_design' ) ;
#31955=DIRECTION ( 'NONE',  ( 0.000000000000000000, -0.9822872507286865007, -0.1873813145857356477 ) ) ;
#31957=ORIENTED_EDGE ( 'NONE', *, *, #24224, .T. ) ;
#31960=CARTESIAN_POINT ( 'NONE',  ( 0.000000000000000000, -13.85708833599938217, -45.43276465116679930 ) ) ;
#31962=VERTEX_POINT ( 'NONE', #5345 ) ;
#31966=DIRECTION ( 'NONE',  ( -1.000000000000000000, 0.000000000000000000, 0.000000000000000000 ) ) ;
#31969=AXIS2_PLACEMENT_3D ( 'NONE', #27365, #5749, #30064 ) ;
#31976=ORIENTED_EDGE ( 'NONE', *, *, #21115, .T. ) ;
#31980=DIRECTION ( 'NONE',  ( -1.000000000000000000, 0.000000000000000000, 0.000000000000000000 ) ) ;
#31981=CIRCLE ( 'NONE', #2679, 20.00000000000000711 ) ;
#31990=DIRECTION ( 'NONE',  ( -1.000000000000000000, -0.000000000000000000, -0.000000000000000000 ) ) ;
#31993=CARTESIAN_POINT ( 'NONE',  ( 7.999999999999992895, -42.03146605346803000, 22.12489237027305577 ) ) ;
#31995=CIRCLE ( 'NONE', #2132, 47.49900000000001654 ) ;
#31996=CARTESIAN_POINT ( 'NONE',  ( 0.000000000000000000, -49.25004636492376875, -16.68630974939810940 ) ) ;
#32003=DIRECTION ( 'NONE',  ( -1.000000000000000000, 0.000000000000000000, 0.000000000000000000 ) ) ;
#32004=AXIS2_PLACEMENT_3D ( 'NONE', #21041, #29537, #35299 ) ;
#32005=DIRECTION ( 'NONE',  ( 0.000000000000000000, 0.000000000000000000, 1.000000000000000000 ) ) ;
#32009=CARTESIAN_POINT ( 'NONE',  ( 7.999999999999992895, -43.83938735307282997, 18.28286404005782728 ) ) ;
#32013=VECTOR ( 'NONE', #35576, 1000.000000000000000 ) ;
#32028=CARTESIAN_POINT ( 'NONE',  ( 4.000000000000003553, 51.19683565102457834, -9.104066087302935983 ) ) ;
#32032=ORIENTED_EDGE ( 'NONE', *, *, #29960, .F. ) ;
#32036=LINE ( 'NONE', #9533, #12834 ) ;
#32037=DIRECTION ( 'NONE',  ( -1.000000000000000000, 0.000000000000000000, -0.000000000000000000 ) ) ;
#32044=VECTOR ( 'NONE', #29270, 1000.000000000000000 ) ;
#32053=CYLINDRICAL_SURFACE ( 'NONE', #21001, 47.49900000000001654 ) ;
#32055=EDGE_LOOP ( 'NONE', ( #30678, #16863, #9159, #34865 ) ) ;
#32066=DIRECTION ( 'NONE',  ( -1.000000000000000000, 0.000000000000000000, 0.000000000000000000 ) ) ;
#32070=AXIS2_PLACEMENT_3D ( 'NONE', #30606, #13870, #33310 ) ;
#32071=CYLINDRICAL_SURFACE ( 'NONE', #26873, 20.00000000000000355 ) ;
#32080=ORIENTED_EDGE ( 'NONE', *, *, #3765, .F. ) ;
#32083=CARTESIAN_POINT ( 'NONE',  ( 7.999999999999992895, 0.000000000000000000, 0.000000000000000000 ) ) ;
#32086=CARTESIAN_POINT ( 'NONE',  ( 7.999999999999992895, 47.22458491092821475, 5.098390039074404356 ) ) ;
#32090=DIRECTION ( 'NONE',  ( 0.000000000000000000, 0.000000000000000000, 1.000000000000000000 ) ) ;
#32092=CIRCLE ( 'NONE', #5655, 47.49900000000003075 ) ;
#32102=CARTESIAN_POINT ( 'NONE',  ( 7.999999999999992895, -44.75336757549789013, 14.30704879393590545 ) ) ;
#32106=EDGE_CURVE ( 'NONE', #6382, #33849, #12199, .T. ) ;
#32116=VECTOR ( 'NONE', #32566, 1000.000000000000000 ) ;
#32123=CARTESIAN_POINT ( 'NONE',  ( 7.999999999999992895, -41.20225022064621356, -23.63323037071446464 ) ) ;
#32124=LINE ( 'NONE', #7093, #20833 ) ;
#32130=CARTESIAN_POINT ( 'NONE',  ( 7.999999999999992895, 37.91532898920963390, -28.61088654061597225 ) ) ;
#32145=DIRECTION ( 'NONE',  ( -1.000000000000000000, 0.000000000000000000, 0.000000000000000000 ) ) ;
#32147=EDGE_CURVE ( 'NONE', #15756, #7835, #8732, .T. ) ;
#32162=ORIENTED_EDGE ( 'NONE', *, *, #26640, .T. ) ;
#32167=ORIENTED_EDGE ( 'NONE', *, *, #32537, .T. ) ;
#32168=CIRCLE ( 'NONE', #12643, 20.00000000000000355 ) ;
#32170=CARTESIAN_POINT ( 'NONE',  ( 0.000000000000000000, 2.123073309835863842, -47.45152853935333326 ) ) ;
#32180=EDGE_CURVE ( 'NONE', #26214, #26454, #6430, .T. ) ;
#32183=DIRECTION ( 'NONE',  ( 0.000000000000000000, 0.000000000000000000, 1.000000000000000000 ) ) ;
#32186=CARTESIAN_POINT ( 'NONE',  ( 7.999999999999992895, 44.75336757549799671, -14.30704879393557327 ) ) ;
#32187=DIRECTION ( 'NONE',  ( 0.000000000000000000, 0.9510565162951545304, -0.3090169943749447867 ) ) ;
#32189=EDGE_CURVE ( 'NONE', #1301, #7659, #20591, .T. ) ;
#32190=VECTOR ( 'NONE', #33941, 1000.000000000000000 ) ;
#32191=ADVANCED_FACE ( 'NONE', ( #6217, #17351 ), #15181, .F. ) ;
#32196=AXIS2_PLACEMENT_3D ( 'NONE', #33615, #8946, #30926 ) ;
#32197=ORIENTED_EDGE ( 'NONE', *, *, #31759, .T. ) ;
#32205=DIRECTION ( 'NONE',  ( 0.000000000000000000, 0.7705132427757861446, 0.6374239897486934092 ) ) ;
#32206=FACE_OUTER_BOUND ( 'NONE', #34541, .T. ) ;
#32208=CARTESIAN_POINT ( 'NONE',  ( 7.999999999999992895, 13.85708833599969303, 45.43276465116672114 ) ) ;
#32215=VERTEX_POINT ( 'NONE', #6919 ) ;
#32222=CYLINDRICAL_SURFACE ( 'NONE', #35578, 20.00000000000000711 ) ;
#32247=FACE_OUTER_BOUND ( 'NONE', #562, .T. ) ;
#32248=LINE ( 'NONE', #23974, #33788 ) ;
#32250=VERTEX_POINT ( 'NONE', #23486 ) ;
#32263=VERTEX_POINT ( 'NONE', #4417 ) ;
#32267=CARTESIAN_POINT ( 'NONE',  ( 0.000000000000000000, 46.87740477351717061, -3.172455868805379442 ) ) ;
#32268=CARTESIAN_POINT ( 'NONE',  ( 7.999999999999992895, 0.000000000000000000, 0.000000000000000000 ) ) ;
#32274=CIRCLE ( 'NONE', #24799, 20.00000000000000355 ) ;
#32275=( GEOMETRIC_REPRESENTATION_CONTEXT ( 3 ) GLOBAL_UNCERTAINTY_ASSIGNED_CONTEXT ( ( #3849 ) ) GLOBAL_UNIT_ASSIGNED_CONTEXT ( ( #12860, #23113, #29250 ) ) REPRESENTATION_CONTEXT ( 'NONE', 'WORKASPACE' ) );
#32277=FACE_OUTER_BOUND ( 'NONE', #32055, .T. ) ;
#32278=AXIS2_PLACEMENT_3D ( 'NONE', #12594, #12233, #33843 ) ;
#32280=VERTEX_POINT ( 'NONE', #15360 ) ;
#32290=EDGE_LOOP ( 'NONE', ( #557, #5776, #3155, #18390 ) ) ;
#32292=CARTESIAN_POINT ( 'NONE',  ( 7.999999999999992895, 22.43957647427161461, 41.27978878573636479 ) ) ;
#32296=AXIS2_PLACEMENT_3D ( 'NONE', #16028, #17, #32612 ) ;
#32299=CARTESIAN_POINT ( 'NONE',  ( 7.999999999999992895, 0.000000000000000000, 0.000000000000000000 ) ) ;
#32303=DIRECTION ( 'NONE',  ( 0.000000000000000000, 0.000000000000000000, 1.000000000000000000 ) ) ;
#32304=CARTESIAN_POINT ( 'NONE',  ( 7.999999999999992895, -15.49408907645140943, -44.90087086784610904 ) ) ;
#32307=CARTESIAN_POINT ( 'NONE',  ( 7.999999999999992895, -46.87740477351715640, 16.82754413119429415 ) ) ;
#32309=EDGE_CURVE ( 'NONE', #19478, #23898, #32124, .T. ) ;
#32311=FACE_OUTER_BOUND ( 'NONE', #11915, .T. ) ;
#32313=CARTESIAN_POINT ( 'NONE',  ( 7.999999999999992895, 30.93515269692114344, 36.04401931830264516 ) ) ;
#32314=CARTESIAN_POINT ( 'NONE',  ( 7.999999999999992895, 38.92705108641771261, -27.21837053747755419 ) ) ;
#32319=CARTESIAN_POINT ( 'NONE',  ( 0.000000000000000000, 37.91532898920923600, 28.61088654061652647 ) ) ;
#32322=CARTESIAN_POINT ( 'NONE',  ( 50.00005079999998969, 0.000000000000000000, 3.000000000000002665 ) ) ;
#32324=VERTEX_POINT ( 'NONE', #34479 ) ;
#32325=ORIENTED_EDGE ( 'NONE', *, *, #32180, .T. ) ;
#32329=ORIENTED_EDGE ( 'NONE', *, *, #10871, .T. ) ;
#32332=EDGE_CURVE ( 'NONE', #169, #31131, #4775, .T. ) ;
#32340=ORIENTED_EDGE ( 'NONE', *, *, #15171, .F. ) ;
#32343=AXIS2_PLACEMENT_3D ( 'NONE', #32268, #29926, #7588 ) ;
#32345=EDGE_CURVE ( 'NONE', #11865, #13559, #11078, .T. ) ;
#32351=DIRECTION ( 'NONE',  ( 0.000000000000000000, 0.000000000000000000, 1.000000000000000000 ) ) ;
#32361=VECTOR ( 'NONE', #19668, 1000.000000000000000 ) ;
#32365=DIRECTION ( 'NONE',  ( -1.000000000000000000, 0.000000000000000000, 0.000000000000000000 ) ) ;
#32370=CARTESIAN_POINT ( 'NONE',  ( 0.000000000000000000, -5.667686777401384823, -46.64153600743608763 ) ) ;
#32371=CIRCLE ( 'NONE', #15673, 52.00000000000000711 ) ;
#32373=ORIENTED_EDGE ( 'NONE', *, *, #30244, .F. ) ;
#32379=DIRECTION ( 'NONE',  ( -1.000000000000000000, 0.000000000000000000, -0.000000000000000000 ) ) ;
#32381=LINE ( 'NONE', #7536, #22492 ) ;
#32382=VERTEX_POINT ( 'NONE', #20762 ) ;
#32383=VERTEX_POINT ( 'NONE', #10512 ) ;
#32386=VECTOR ( 'NONE', #13062, 1000.000000000000000 ) ;
#32391=EDGE_CURVE ( 'NONE', #13336, #34584, #6462, .T. ) ;
#32392=DIRECTION ( 'NONE',  ( 0.000000000000000000, 0.000000000000000000, -1.000000000000000000 ) ) ;
#32393=ORIENTED_EDGE ( 'NONE', *, *, #13055, .T. ) ;
#32394=DIRECTION ( 'NONE',  ( -1.000000000000000000, 0.000000000000000000, -0.000000000000000000 ) ) ;
#32401=AXIS2_PLACEMENT_3D ( 'NONE', #9788, #17164, #28171 ) ;
#32415=AXIS2_PLACEMENT_3D ( 'NONE', #30328, #3141, #30502 ) ;
#32417=CARTESIAN_POINT ( 'NONE',  ( 7.999999999999992895, 46.87740477351717061, 16.82754413119462455 ) ) ;
#32421=CARTESIAN_POINT ( 'NONE',  ( 0.000000000000000000, 0.000000000000000000, 0.000000000000000000 ) ) ;
#32434=DIRECTION ( 'NONE',  ( 0.000000000000000000, 0.000000000000000000, 1.000000000000000000 ) ) ;
#32439=DIRECTION ( 'NONE',  ( -1.000000000000000000, 0.000000000000000000, -0.000000000000000000 ) ) ;
#32440=DIRECTION ( 'NONE',  ( 0.000000000000000000, 0.000000000000000000, -1.000000000000000000 ) ) ;
#32451=VERTEX_POINT ( 'NONE', #2605 ) ;
#32452=CARTESIAN_POINT ( 'NONE',  ( 0.000000000000000000, 0.000000000000000000, 0.000000000000000000 ) ) ;
#32463=ORIENTED_EDGE ( 'NONE', *, *, #33014, .T. ) ;
#32470=DIRECTION ( 'NONE',  ( 0.000000000000000000, -0.3681245526846653737, -0.9297764858882564543 ) ) ;
#32480=DIRECTION ( 'NONE',  ( -1.000000000000000000, -0.000000000000000000, 0.000000000000000000 ) ) ;
#32489=DIRECTION ( 'NONE',  ( -1.000000000000000000, -0.000000000000000000, 0.000000000000000000 ) ) ;
#32492=CARTESIAN_POINT ( 'NONE',  ( 0.000000000000000000, 0.000000000000000000, 0.000000000000000000 ) ) ;
#32494=ORIENTED_EDGE ( 'NONE', *, *, #19823, .T. ) ;
#32495=ORIENTED_EDGE ( 'NONE', *, *, #26955, .F. ) ;
#32499=FACE_OUTER_BOUND ( 'NONE', #29510, .T. ) ;
#32505=AXIS2_PLACEMENT_3D ( 'NONE', #12253, #12430, #9007 ) ;
#32516=DIRECTION ( 'NONE',  ( -1.000000000000000000, 0.000000000000000000, 0.000000000000000000 ) ) ;
#32521=CIRCLE ( 'NONE', #25648, 20.00000000000000711 ) ;
#32528=CYLINDRICAL_SURFACE ( 'NONE', #33611, 20.00000000000000355 ) ;
#32535=VERTEX_POINT ( 'NONE', #3614 ) ;
#32537=EDGE_CURVE ( 'NONE', #7261, #4978, #35241, .T. ) ;
#32542=ORIENTED_EDGE ( 'NONE', *, *, #8000, .T. ) ;
#32543=EDGE_CURVE ( 'NONE', #18045, #1374, #19136, .T. ) ;
#32546=AXIS2_PLACEMENT_3D ( 'NONE', #25200, #19427, #2888 ) ;
#32548=CARTESIAN_POINT ( 'NONE',  ( 7.999999999999992895, 0.000000000000000000, 0.000000000000000000 ) ) ;
#32550=EDGE_CURVE ( 'NONE', #17170, #27299, #23131, .T. ) ;
#32553=DIRECTION ( 'NONE',  ( 0.000000000000000000, 0.000000000000000000, 1.000000000000000000 ) ) ;
#32559=CARTESIAN_POINT ( 'NONE',  ( 7.999999999999992895, -41.20225022064621356, -23.63323037071446464 ) ) ;
#32562=CIRCLE ( 'NONE', #18843, 20.00000000000000711 ) ;
#32566=DIRECTION ( 'NONE',  ( 0.000000000000000000, 1.000000000000000000, 0.000000000000000000 ) ) ;
#32568=DIRECTION ( 'NONE',  ( -1.000000000000000000, -0.000000000000000000, -0.000000000000000000 ) ) ;
#32581=EDGE_LOOP ( 'NONE', ( #34760, #17780, #8589, #33314 ) ) ;
#32597=CIRCLE ( 'NONE', #2172, 20.00000000000000711 ) ;
#32602=ADVANCED_FACE ( 'NONE', ( #712 ), #6124, .T. ) ;
#32609=VECTOR ( 'NONE', #19804, 1000.000000000000000 ) ;
#32612=DIRECTION ( 'NONE',  ( 0.000000000000000000, 0.000000000000000000, 1.000000000000000000 ) ) ;
#32622=CARTESIAN_POINT ( 'NONE',  ( 7.999999999999992895, 0.000000000000000000, 0.000000000000000000 ) ) ;
#32623=CYLINDRICAL_SURFACE ( 'NONE', #19806, 47.49900000000001654 ) ;
#32624=AXIS2_PLACEMENT_3D ( 'NONE', #11103, #24961, #18656 ) ;
#32628=CARTESIAN_POINT ( 'NONE',  ( 0.000000000000000000, 45.78515115856044559, 12.64416602183680816 ) ) ;
#32639=EDGE_CURVE ( 'NONE', #9389, #29599, #20631, .T. ) ;
#32652=CIRCLE ( 'NONE', #30367, 20.00000000000000711 ) ;
#32658=VECTOR ( 'NONE', #25765, 1000.000000000000000 ) ;
#32663=CARTESIAN_POINT ( 'NONE',  ( 7.999999999999992895, -46.11014828289837197, -9.022736828081189486 ) ) ;
#32668=VECTOR ( 'NONE', #9157, 1000.000000000000000 ) ;
#32670=EDGE_CURVE ( 'NONE', #14164, #6382, #25864, .T. ) ;
#32673=ADVANCED_FACE ( 'NONE', ( #31322 ), #17624, .T. ) ;
#32682=CARTESIAN_POINT ( 'NONE',  ( 0.000000000000000000, 0.000000000000000000, 0.000000000000000000 ) ) ;
#32683=CARTESIAN_POINT ( 'NONE',  ( 7.999999999999992895, -37.91532898920942074, 28.61088654061626357 ) ) ;
#32685=ADVANCED_FACE ( 'NONE', ( #23029 ), #9882, .T. ) ;
#32695=ORIENTED_EDGE ( 'NONE', *, *, #11943, .F. ) ;
#32704=VERTEX_POINT ( 'NONE', #28632 ) ;
#32706=FACE_OUTER_BOUND ( 'NONE', #16554, .T. ) ;
#32714=DIRECTION ( 'NONE',  ( 1.000000000000000000, -0.000000000000000000, -0.000000000000000000 ) ) ;
#32720=VERTEX_POINT ( 'NONE', #28980 ) ;
#32722=CARTESIAN_POINT ( 'NONE',  ( 7.999999999999992895, 20.99948489194422763, 42.60488980472790388 ) ) ;
#32726=ORIENTED_EDGE ( 'NONE', *, *, #2731, .F. ) ;
#32727=CARTESIAN_POINT ( 'NONE',  ( 7.999999999999992895, 0.2227391519123156360, -46.98410307550729215 ) ) ;
#32729=AXIS2_PLACEMENT_3D ( 'NONE', #3361, #630, #5865 ) ;
#32733=CARTESIAN_POINT ( 'NONE',  ( 7.999999999999992895, -18.53613841426757602, -48.58406706613921244 ) ) ;
#32734=CIRCLE ( 'NONE', #10903, 20.00000000000000355 ) ;
#32737=DIRECTION ( 'NONE',  ( -1.000000000000000000, 0.000000000000000000, 0.000000000000000000 ) ) ;
#32741=DIRECTION ( 'NONE',  ( -1.000000000000000000, -0.000000000000000000, 0.000000000000000000 ) ) ;
#32743=CARTESIAN_POINT ( 'NONE',  ( -9.999999999999994671, 0.000000000000000000, 0.000000000000000000 ) ) ;
#32747=EDGE_CURVE ( 'NONE', #33531, #1331, #25929, .T. ) ;
#32752=DIRECTION ( 'NONE',  ( 0.000000000000000000, 0.000000000000000000, 1.000000000000000000 ) ) ;
#32756=AXIS2_PLACEMENT_3D ( 'NONE', #29877, #32394, #2349 ) ;
#32760=FACE_OUTER_BOUND ( 'NONE', #20521, .T. ) ;
#32763=CIRCLE ( 'NONE', #2890, 20.00000000000001066 ) ;
#32766=CARTESIAN_POINT ( 'NONE',  ( 4.000000000000003553, -25.61928775981074935, 45.25098998563470332 ) ) ;
#32771=DIRECTION ( 'NONE',  ( 0.000000000000000000, -0.9822872507286903865, 0.1873813145857150808 ) ) ;
#32774=LINE ( 'NONE', #30080, #19555 ) ;
#32776=ORIENTED_EDGE ( 'NONE', *, *, #18568, .F. ) ;
#32787=DIRECTION ( 'NONE',  ( -1.000000000000000000, 0.000000000000000000, 0.000000000000000000 ) ) ;
#32789=CIRCLE ( 'NONE', #17243, 20.00000000000000355 ) ;
#32791=AXIS2_PLACEMENT_3D ( 'NONE', #23249, #20348, #31359 ) ;
#32795=EDGE_CURVE ( 'NONE', #29599, #31713, #25311, .T. ) ;
#32796=LINE ( 'NONE', #8289, #21770 ) ;
#32804=VERTEX_POINT ( 'NONE', #27001 ) ;
#32805=ADVANCED_FACE ( 'NONE', ( #21394 ), #24122, .T. ) ;
#32810=ORIENTED_EDGE ( 'NONE', *, *, #20733, .F. ) ;
#32812=CARTESIAN_POINT ( 'NONE',  ( 0.000000000000000000, 38.92705108641771261, -27.21837053747755419 ) ) ;
#32813=ORIENTED_EDGE ( 'NONE', *, *, #8238, .F. ) ;
#32834=CARTESIAN_POINT ( 'NONE',  ( 4.000000000000003553, 40.47821179127763003, -32.64221760512714354 ) ) ;
#32838=EDGE_CURVE ( 'NONE', #29619, #13072, #20683, .T. ) ;
#32839=CARTESIAN_POINT ( 'NONE',  ( 7.999999999999992895, 38.92705108641732892, 27.21837053747812263 ) ) ;
#32846=CARTESIAN_POINT ( 'NONE',  ( 7.999999999999992895, 46.11014828289842882, -9.022736828080857308 ) ) ;
#32848=DIRECTION ( 'NONE',  ( 0.000000000000000000, 0.2486898871648553222, -0.9685831611286309650 ) ) ;
#32851=DIRECTION ( 'NONE',  ( -1.000000000000000000, 0.000000000000000000, 0.000000000000000000 ) ) ;
#32854=EDGE_CURVE ( 'NONE', #16713, #29785, #27349, .T. ) ;
#32864=ORIENTED_EDGE ( 'NONE', *, *, #12876, .T. ) ;
#32865=DIRECTION ( 'NONE',  ( -1.000000000000000000, 0.000000000000000000, 0.000000000000000000 ) ) ;
#32866=FACE_OUTER_BOUND ( 'NONE', #12252, .T. ) ;
#32870=ORIENTED_EDGE ( 'NONE', *, *, #14047, .F. ) ;
#32878=EDGE_CURVE ( 'NONE', #33836, #27200, #27619, .T. ) ;
#32880=ORIENTED_EDGE ( 'NONE', *, *, #2972, .F. ) ;
#32883=EDGE_CURVE ( 'NONE', #15669, #7480, #9762, .T. ) ;
#32889=AXIS2_PLACEMENT_3D ( 'NONE', #26331, #24514, #13531 ) ;
#32893=CARTESIAN_POINT ( 'NONE',  ( 0.000000000000000000, -15.49408907645140943, -44.90087086784610904 ) ) ;
#32899=ORIENTED_EDGE ( 'NONE', *, *, #13905, .F. ) ;
#32901=DIRECTION ( 'NONE',  ( -1.000000000000000000, 0.000000000000000000, 0.000000000000000000 ) ) ;
#32909=ORIENTED_EDGE ( 'NONE', *, *, #22938, .T. ) ;
#32910=ORIENTED_EDGE ( 'NONE', *, *, #8151, .F. ) ;
#32911=EDGE_CURVE ( 'NONE', #33000, #3384, #24163, .T. ) ;
#32912=EDGE_CURVE ( 'NONE', #13354, #30986, #29898, .T. ) ;
#32914=AXIS2_PLACEMENT_3D ( 'NONE', #26524, #9229, #4029 ) ;
#32917=AXIS2_PLACEMENT_3D ( 'NONE', #15718, #34834, #35026 ) ;
#32921=ORIENTED_EDGE ( 'NONE', *, *, #8226, .T. ) ;
#32923=DIRECTION ( 'NONE',  ( 0.000000000000000000, 0.000000000000000000, 1.000000000000000000 ) ) ;
#32935=DIRECTION ( 'NONE',  ( -1.000000000000000000, 0.000000000000000000, -0.000000000000000000 ) ) ;
#32936=DIRECTION ( 'NONE',  ( 0.000000000000000000, 0.000000000000000000, -1.000000000000000000 ) ) ;
#32945=VERTEX_POINT ( 'NONE', #18523 ) ;
#32947=DIRECTION ( 'NONE',  ( 0.000000000000000000, 0.000000000000000000, -1.000000000000000000 ) ) ;
#32952=CIRCLE ( 'NONE', #31228, 20.00000000000000711 ) ;
#32958=ORIENTED_EDGE ( 'NONE', *, *, #1423, .T. ) ;
#32960=LINE ( 'NONE', #21961, #6742 ) ;
#32967=AXIS2_PLACEMENT_3D ( 'NONE', #30018, #30714, #10749 ) ;
#32970=CIRCLE ( 'NONE', #17420, 20.00000000000000355 ) ;
#32974=DIRECTION ( 'NONE',  ( -1.000000000000000000, 0.000000000000000000, 0.000000000000000000 ) ) ;
#32980=VECTOR ( 'NONE', #27000, 1000.000000000000000 ) ;
#32984=DIRECTION ( 'NONE',  ( 1.000000000000000000, 0.000000000000000000, 0.000000000000000000 ) ) ;
#32988=ORIENTED_EDGE ( 'NONE', *, *, #29757, .F. ) ;
#32989=AXIS2_PLACEMENT_3D ( 'NONE', #20522, #12258, #28464 ) ;
#32992=CARTESIAN_POINT ( 'NONE',  ( 0.000000000000000000, 24.47917365150010127, -45.87777302070911389 ) ) ;
#32998=ADVANCED_FACE ( 'NONE', ( #27704 ), #8764, .T. ) ;
#33000=VERTEX_POINT ( 'NONE', #30223 ) ;
#33010=EDGE_CURVE ( 'NONE', #7529, #2044, #34492, .T. ) ;
#33012=EDGE_CURVE ( 'NONE', #20345, #9, #3040, .T. ) ;
#33014=EDGE_CURVE ( 'NONE', #34614, #19983, #18392, .T. ) ;
#33019=CARTESIAN_POINT ( 'NONE',  ( 7.999999999999992895, 0.000000000000000000, 0.000000000000000000 ) ) ;
#33030=EDGE_CURVE ( 'NONE', #6171, #19728, #8036, .T. ) ;
#33031=DIRECTION ( 'NONE',  ( -1.000000000000000000, -0.000000000000000000, -0.000000000000000000 ) ) ;
#33035=CARTESIAN_POINT ( 'NONE',  ( 7.999999999999992895, 0.000000000000000000, 0.000000000000000000 ) ) ;
#33039=DIRECTION ( 'NONE',  ( -1.000000000000000000, 0.000000000000000000, 0.000000000000000000 ) ) ;
#33046=ORIENTED_EDGE ( 'NONE', *, *, #33902, .T. ) ;
#33051=VECTOR ( 'NONE', #4880, 1000.000000000000000 ) ;
#33056=EDGE_CURVE ( 'NONE', #10826, #33486, #27049, .T. ) ;
#33057=EDGE_CURVE ( 'NONE', #25880, #25236, #11312, .T. ) ;
#33058=DIRECTION ( 'NONE',  ( 0.000000000000000000, 0.3681245526846786964, -0.9297764858882511252 ) ) ;
#33060=CARTESIAN_POINT ( 'NONE',  ( 7.999999999999992895, -44.47301969247433817, -16.68249143361957820 ) ) ;
#33062=DIRECTION ( 'NONE',  ( 0.000000000000000000, 0.000000000000000000, 1.000000000000000000 ) ) ;
#33077=DIRECTION ( 'NONE',  ( 1.000000000000000000, 0.000000000000000000, -0.000000000000000000 ) ) ;
#33078=ORIENTED_EDGE ( 'NONE', *, *, #34139, .F. ) ;
#33082=DIRECTION ( 'NONE',  ( -1.000000000000000000, 0.000000000000000000, 0.000000000000000000 ) ) ;
#33083=ORIENTED_EDGE ( 'NONE', *, *, #34467, .T. ) ;
#33090=ORIENTED_EDGE ( 'NONE', *, *, #21, .F. ) ;
#33092=CARTESIAN_POINT ( 'NONE',  ( 7.999999999999992895, -22.43957647427129842, -41.27978878573651400 ) ) ;
#33103=DIRECTION ( 'NONE',  ( 0.000000000000000000, 0.000000000000000000, 1.000000000000000000 ) ) ;
#33110=CARTESIAN_POINT ( 'NONE',  ( 7.999999999999992895, -9.744342220503080298, -46.48873837489808380 ) ) ;
#33116=DIRECTION ( 'NONE',  ( -1.000000000000000000, 0.000000000000000000, 0.000000000000000000 ) ) ;
#33117=EDGE_CURVE ( 'NONE', #1430, #22165, #31035, .T. ) ;
#33123=DIRECTION ( 'NONE',  ( -1.000000000000000000, 0.000000000000000000, -0.000000000000000000 ) ) ;
#33127=AXIS2_PLACEMENT_3D ( 'NONE', #13984, #5883, #25507 ) ;
#33136=DIRECTION ( 'NONE',  ( -1.000000000000000000, 0.000000000000000000, -0.000000000000000000 ) ) ;
#33138=ORIENTED_EDGE ( 'NONE', *, *, #35283, .F. ) ;
#33139=ORIENTED_EDGE ( 'NONE', *, *, #12517, .T. ) ;
#33144=ORIENTED_EDGE ( 'NONE', *, *, #30200, .T. ) ;
#33151=CARTESIAN_POINT ( 'NONE',  ( 7.999999999999992895, -0.6505223195686569149, 51.99593080916758936 ) ) ;
#33156=CARTESIAN_POINT ( 'NONE',  ( 7.999999999999992895, -51.19683565102439360, -9.104066087303991139 ) ) ;
#33159=ORIENTED_EDGE ( 'NONE', *, *, #12975, .F. ) ;
#33166=VERTEX_POINT ( 'NONE', #27292 ) ;
#33171=EDGE_CURVE ( 'NONE', #21169, #30069, #33352, .T. ) ;
#33172=DIRECTION ( 'NONE',  ( 0.000000000000000000, 0.7705132427757904745, -0.6374239897486881912 ) ) ;
#33173=AXIS2_PLACEMENT_3D ( 'NONE', #14320, #31076, #22595 ) ;
#33183=CARTESIAN_POINT ( 'NONE',  ( 7.999999999999992895, -44.61570720899084819, -14.73072383765613935 ) ) ;
#33187=CARTESIAN_POINT ( 'NONE',  ( 7.999999999999992895, -20.99948489194452250, 42.60488980472776177 ) ) ;
#33190=CIRCLE ( 'NONE', #24562, 47.49900000000000944 ) ;
#33193=CYLINDRICAL_SURFACE ( 'NONE', #13662, 52.00000000000000711 ) ;
#33199=CIRCLE ( 'NONE', #23431, 52.00000000000000711 ) ;
#33206=CARTESIAN_POINT ( 'NONE',  ( 0.000000000000000000, -49.25004636492401033, 16.68630974939741662 ) ) ;
#33211=CARTESIAN_POINT ( 'NONE',  ( 0.000000000000000000, 0.000000000000000000, 0.000000000000000000 ) ) ;
#33214=EDGE_CURVE ( 'NONE', #11602, #26795, #21704, .T. ) ;
#33217=CIRCLE ( 'NONE', #2199, 52.00000000000000711 ) ;
#33222=CARTESIAN_POINT ( 'NONE',  ( 7.999999999999992895, 29.60891106212840285, -37.14118181634734839 ) ) ;
#33226=AXIS2_PLACEMENT_3D ( 'NONE', #2837, #22241, #3006 ) ;
#33227=AXIS2_PLACEMENT_3D ( 'NONE', #8979, #8801, #13699 ) ;
#33230=DIRECTION ( 'NONE',  ( 1.000000000000000000, -0.000000000000000000, 0.000000000000000000 ) ) ;
#33240=ADVANCED_FACE ( 'NONE', ( #32866 ), #2824, .T. ) ;
#33241=ADVANCED_FACE ( 'NONE', ( #32499 ), #5504, .T. ) ;
#33242=DIRECTION ( 'NONE',  ( 0.000000000000000000, -0.8443279255020201823, 0.5358267949789886631 ) ) ;
#33248=CIRCLE ( 'NONE', #19440, 52.00000000000000711 ) ;
#33251=CARTESIAN_POINT ( 'NONE',  ( 0.000000000000000000, 32.00046193115196758, -34.40241257139653186 ) ) ;
#33254=ADVANCED_FACE ( 'NONE', ( #2458 ), #29995, .T. ) ;
#33278=EDGE_CURVE ( 'NONE', #14164, #29056, #28170, .T. ) ;
#33289=DIRECTION ( 'NONE',  ( -1.000000000000000000, 0.000000000000000000, 0.000000000000000000 ) ) ;
#33291=DIRECTION ( 'NONE',  ( -1.000000000000000000, -0.000000000000000000, 0.000000000000000000 ) ) ;
#33293=ORIENTED_EDGE ( 'NONE', *, *, #23294, .F. ) ;
#33295=ORIENTED_EDGE ( 'NONE', *, *, #32838, .F. ) ;
#33301=AXIS2_PLACEMENT_3D ( 'NONE', #29609, #15895, #20006 ) ;
#33302=ORIENTED_EDGE ( 'NONE', *, *, #32883, .T. ) ;
#33303=CYLINDRICAL_SURFACE ( 'NONE', #20566, 52.00000000000000711 ) ;
#33306=CARTESIAN_POINT ( 'NONE',  ( 4.000000000000003553, -19.74581912682808493, -48.10512059033414545 ) ) ;
#33307=CARTESIAN_POINT ( 'NONE',  ( 0.000000000000000000, -31.08872492059928305, -41.68322423723133596 ) ) ;
#33310=DIRECTION ( 'NONE',  ( 0.000000000000000000, 0.1253332335643046469, -0.9921147013144777649 ) ) ;
#33314=ORIENTED_EDGE ( 'NONE', *, *, #16239, .T. ) ;
#33324=CARTESIAN_POINT ( 'NONE',  ( 0.000000000000000000, -44.75336757549767697, -14.30704879393654494 ) ) ;
#33330=DIRECTION ( 'NONE',  ( 1.000000000000000000, -0.000000000000000000, 0.000000000000000000 ) ) ;
#33333=ORIENTED_EDGE ( 'NONE', *, *, #6815, .F. ) ;
#33335=CYLINDRICAL_SURFACE ( 'NONE', #19146, 52.00000000000000711 ) ;
#33340=LINE ( 'NONE', #8664, #9266 ) ;
#33346=CARTESIAN_POINT ( 'NONE',  ( 4.000000000000003553, -7.162210897275381072, -51.50439529848838305 ) ) ;
#33352=CIRCLE ( 'NONE', #11505, 52.00000000000000711 ) ;
#33358=ADVANCED_FACE ( 'NONE', ( #17337 ), #33744, .T. ) ;
#33360=CARTESIAN_POINT ( 'NONE',  ( 7.999999999999992895, 24.72041153920734047, 40.55929306992698002 ) ) ;
#33370=DIRECTION ( 'NONE',  ( 0.000000000000000000, 0.000000000000000000, 1.000000000000000000 ) ) ;
#33375=DIRECTION ( 'NONE',  ( 0.000000000000000000, 0.000000000000000000, 1.000000000000000000 ) ) ;
#33380=LINE ( 'NONE', #8705, #25343 ) ;
#33383=VERTEX_POINT ( 'NONE', #30518 ) ;
#33385=CARTESIAN_POINT ( 'NONE',  ( -9.999999999999994671, 0.000000000000000000, 0.000000000000000000 ) ) ;
#33386=LINE ( 'NONE', #11430, #166 ) ;
#33387=VERTEX_POINT ( 'NONE', #9075 ) ;
#33394=DIRECTION ( 'NONE',  ( 0.000000000000000000, 0.000000000000000000, -1.000000000000000000 ) ) ;
#33402=CARTESIAN_POINT ( 'NONE',  ( -9.999999999999994671, 0.000000000000000000, 0.000000000000000000 ) ) ;
#33403=ADVANCED_FACE ( 'NONE', ( #33924 ), #31041, .T. ) ;
#33408=CARTESIAN_POINT ( 'NONE',  ( 7.999999999999992895, -25.61928775981012762, -45.25098998563503727 ) ) ;
#33415=DIRECTION ( 'NONE',  ( -1.000000000000000000, -0.000000000000000000, -0.000000000000000000 ) ) ;
#33419=AXIS2_PLACEMENT_3D ( 'NONE', #2341, #35278, #32553 ) ;
#33421=CARTESIAN_POINT ( 'NONE',  ( 0.000000000000000000, 42.41764978026606769, 20.20639853260304619 ) ) ;
#33424=ORIENTED_EDGE ( 'NONE', *, *, #1887, .F. ) ;
#33428=VERTEX_POINT ( 'NONE', #11429 ) ;
#33434=CIRCLE ( 'NONE', #3588, 47.49900000000001654 ) ;
#33437=EDGE_LOOP ( 'NONE', ( #14387, #31658, #18474, #6465 ) ) ;
#33446=EDGE_CURVE ( 'NONE', #6691, #19596, #18255, .T. ) ;
#33455=LINE ( 'NONE', #8779, #595 ) ;
#33459=ORIENTED_EDGE ( 'NONE', *, *, #26516, .T. ) ;
#33463=DIRECTION ( 'NONE',  ( -1.000000000000000000, 0.000000000000000000, 0.000000000000000000 ) ) ;
#33464=EDGE_CURVE ( 'NONE', #20157, #27614, #34948, .T. ) ;
#33472=AXIS2_PLACEMENT_3D ( 'NONE', #3883, #11607, #17530 ) ;
#33479=DIRECTION ( 'NONE',  ( -1.000000000000000000, 0.000000000000000000, -0.000000000000000000 ) ) ;
#33482=ORIENTED_EDGE ( 'NONE', *, *, #2697, .F. ) ;
#33486=VERTEX_POINT ( 'NONE', #5591 ) ;
#33498=DIRECTION ( 'NONE',  ( -1.000000000000000000, 0.000000000000000000, 0.000000000000000000 ) ) ;
#33501=CYLINDRICAL_SURFACE ( 'NONE', #2308, 20.00000000000000355 ) ;
#33502=CARTESIAN_POINT ( 'NONE',  ( 0.000000000000000000, 13.56094713063571078, 50.20060470671747055 ) ) ;
#33504=ORIENTED_EDGE ( 'NONE', *, *, #25807, .T. ) ;
#33511=EDGE_CURVE ( 'NONE', #27872, #12895, #27028, .T. ) ;
#33520=ORIENTED_EDGE ( 'NONE', *, *, #10550, .T. ) ;
#33521=EDGE_LOOP ( 'NONE', ( #3737, #16231, #35042, #9530 ) ) ;
#33522=EDGE_CURVE ( 'NONE', #10666, #19094, #26900, .T. ) ;
#33526=DIRECTION ( 'NONE',  ( 0.000000000000000000, 0.9980267284282712259, 0.06279051952931682945 ) ) ;
#33530=DIRECTION ( 'NONE',  ( -1.000000000000000000, -0.000000000000000000, -0.000000000000000000 ) ) ;
#33531=VERTEX_POINT ( 'NONE', #21590 ) ;
#33545=CARTESIAN_POINT ( 'NONE',  ( 7.999999999999992895, 0.000000000000000000, 0.000000000000000000 ) ) ;
#33546=DIRECTION ( 'NONE',  ( -1.000000000000000000, -0.000000000000000000, -0.000000000000000000 ) ) ;
#33551=DIRECTION ( 'NONE',  ( 0.000000000000000000, -0.2486898871648415832, -0.9685831611286344067 ) ) ;
#33553=DIRECTION ( 'NONE',  ( -1.000000000000000000, 0.000000000000000000, 0.000000000000000000 ) ) ;
#33562=ORIENTED_EDGE ( 'NONE', *, *, #8110, .F. ) ;
#33566=ORIENTED_EDGE ( 'NONE', *, *, #29, .T. ) ;
#33568=CIRCLE ( 'NONE', #6527, 47.49900000000001654 ) ;
#33570=ADVANCED_FACE ( 'NONE', ( #9958 ), #8270, .T. ) ;
#33583=DIRECTION ( 'NONE',  ( -1.000000000000000000, -0.000000000000000000, -0.000000000000000000 ) ) ;
#33589=DIRECTION ( 'NONE',  ( -1.000000000000000000, 0.000000000000000000, 0.000000000000000000 ) ) ;
#33592=DIRECTION ( 'NONE',  ( 0.000000000000000000, 0.000000000000000000, 1.000000000000000000 ) ) ;
#33594=CARTESIAN_POINT ( 'NONE',  ( 0.000000000000000000, -46.90537658765327933, -2.727856614654800005 ) ) ;
#33599=CARTESIAN_POINT ( 'NONE',  ( 0.000000000000000000, 3.840921266750509488, -47.34345070675166767 ) ) ;
#33602=EDGE_CURVE ( 'NONE', #14042, #28842, #11678, .T. ) ;
#33603=VERTEX_POINT ( 'NONE', #20123 ) ;
#33607=CARTESIAN_POINT ( 'NONE',  ( 7.999999999999992895, 34.03046037009256963, 33.13733193845818903 ) ) ;
#33609=ORIENTED_EDGE ( 'NONE', *, *, #20653, .F. ) ;
#33611=AXIS2_PLACEMENT_3D ( 'NONE', #2319, #18666, #13289 ) ;
#33612=DIRECTION ( 'NONE',  ( 0.000000000000000000, 0.000000000000000000, -1.000000000000000000 ) ) ;
#33613=CARTESIAN_POINT ( 'NONE',  ( 7.999999999999992895, -15.49408907645203470, 44.90087086784588877 ) ) ;
#33614=ORIENTED_EDGE ( 'NONE', *, *, #29807, .F. ) ;
#33615=CARTESIAN_POINT ( 'NONE',  ( 7.999999999999992895, 0.000000000000000000, 0.000000000000000000 ) ) ;
#33618=CARTESIAN_POINT ( 'NONE',  ( 0.000000000000000000, 43.55304910509448035, -28.41006711799937179 ) ) ;
#33622=CARTESIAN_POINT ( 'NONE',  ( 7.999999999999992895, 51.93417535146742381, -2.615612846549375536 ) ) ;
#33627=CARTESIAN_POINT ( 'NONE',  ( 7.999999999999992895, 0.000000000000000000, 0.000000000000000000 ) ) ;
#33635=CARTESIAN_POINT ( 'NONE',  ( 4.000000000000003553, 35.11945359308164427, -38.34871548465979174 ) ) ;
#33639=CLOSED_SHELL ( 'NONE', ( #21082, #25614, #29792, #27150, #28475, #26923, #32191, #34406, #25318, #33403, #6283, #18369, #29040, #12403, #12133, #34505, #9543, #5966, #11895, #1051, #23618, #15833, #30404, #27062, #17668, #33358, #9741, #25518, #506, #5455, #22933, #21977, #1995, #23848, #3135, #10285, #14594, #19787, #20446, #20498, #26256, #33254, #8527, #17670, #17442, #10398, #28685, #17773, #12678, #32602, #13748, #29458, #33659, #7759, #2420, #5171, #15614, #15416, #26716, #4689, #16538, #27444, #31240, #5541, #13853, #4705, #28250, #19588, #20867, #19830, #35294, #3205, #26687, #888, #21536, #18749, #22405, #4887, #29060, #32685, #1853, #22327, #27216, #9260, #11447, #15655, #18638, #2218, #5569, #28050, #10295, #25235, #12510, #11933, #17391, #31858, #22813, #35446, #5061, #31045, #3613, #2043, #24543, #9330, #417, #10121, #27104, #16223, #48, #30008, #7823, #25846, #24684, #21117, #17162, #13266, #21780, #34554, #28670, #2009, #21327, #8424, #479, #21646, #7781, #9706, #32998, #9309, #16959, #34659, #28083, #18938, #3206, #4237, #33570, #3249, #15575, #34635, #18367, #32673, #19645, #25027, #4394, #21586, #31411, #25149, #22605, #9291, #26541, #6602, #8868, #13214, #29796, #27720, #16035, #24302, #12129, #14727, #27760, #6120, #25130, #23818, #29499, #25347, #22871, #4662, #10074, #33241, #17033, #24300, #30670, #32805, #28888, #30273, #24911, #8751, #25569, #21936, #20241, #2327, #17004, #15709, #5922, #30480, #6221, #17077, #22466, #21834, #3345, #23153, #33240, #12145, #30677, #18705, #2567, #18161, #27313, #14887, #11713, #25399, #15192, #14243, #4899, #13187, #21807, #9345, #34109, #4495, #19366, #8334, #27535 ) ) ;
#33642=CIRCLE ( 'NONE', #22713, 52.00000000000000711 ) ;
#33646=CARTESIAN_POINT ( 'NONE',  ( 7.999999999999992895, -26.17370628620682638, 39.63700417846155233 ) ) ;
#33647=ORIENTED_EDGE ( 'NONE', *, *, #18035, .T. ) ;
#33652=CIRCLE ( 'NONE', #32505, 52.00000000000000711 ) ;
#33656=DIRECTION ( 'NONE',  ( -1.000000000000000000, -0.000000000000000000, -0.000000000000000000 ) ) ;
#33659=ADVANCED_FACE ( 'NONE', ( #28255 ), #33303, .T. ) ;
#33667=VECTOR ( 'NONE', #6097, 1000.000000000000000 ) ;
#33678=DIRECTION ( 'NONE',  ( -1.000000000000000000, 0.000000000000000000, -0.000000000000000000 ) ) ;
#33681=ORIENTED_EDGE ( 'NONE', *, *, #8226, .F. ) ;
#33683=ORIENTED_EDGE ( 'NONE', *, *, #2120, .F. ) ;
#33685=CARTESIAN_POINT ( 'NONE',  ( 7.999999999999992895, 0.000000000000000000, 0.000000000000000000 ) ) ;
#33700=DIRECTION ( 'NONE',  ( 0.000000000000000000, -0.9822872507286865007, -0.1873813145857354812 ) ) ;
#33711=AXIS2_PLACEMENT_3D ( 'NONE', #29135, #4488, #5005 ) ;
#33719=AXIS2_PLACEMENT_3D ( 'NONE', #8254, #18889, #13498 ) ;
#33722=DIRECTION ( 'NONE',  ( -1.000000000000000000, 0.000000000000000000, 0.000000000000000000 ) ) ;
#33723=EDGE_CURVE ( 'NONE', #34390, #34778, #30948, .T. ) ;
#33725=CARTESIAN_POINT ( 'NONE',  ( 0.000000000000000000, -24.47917365149914559, -45.87777302070961127 ) ) ;
#33735=AXIS2_PLACEMENT_3D ( 'NONE', #118, #7858, #11108 ) ;
#33737=CYLINDRICAL_SURFACE ( 'NONE', #2631, 20.00000000000000711 ) ;
#33743=CARTESIAN_POINT ( 'NONE',  ( -9.999999999999994671, 0.000000000000000000, 0.000000000000000000 ) ) ;
#33744=CYLINDRICAL_SURFACE ( 'NONE', #8474, 52.00000000000000711 ) ;
#33751=AXIS2_PLACEMENT_3D ( 'NONE', #26074, #6268, #15064 ) ;
#33753=ORIENTED_EDGE ( 'NONE', *, *, #20078, .T. ) ;
#33770=EDGE_CURVE ( 'NONE', #20492, #17645, #14817, .T. ) ;
#33771=CYLINDRICAL_SURFACE ( 'NONE', #22628, 47.49900000000001654 ) ;
#33780=CARTESIAN_POINT ( 'NONE',  ( 7.999999999999992895, 27.43636312076321104, 38.14186064215159888 ) ) ;
#33783=DIRECTION ( 'NONE',  ( -1.000000000000000000, -0.000000000000000000, -0.000000000000000000 ) ) ;
#33784=VERTEX_POINT ( 'NONE', #1418 ) ;
#33788=VECTOR ( 'NONE', #2209, 1000.000000000000000 ) ;
#33792=CIRCLE ( 'NONE', #19955, 47.49900000000000944 ) ;
#33794=DIRECTION ( 'NONE',  ( 0.000000000000000000, 0.7705132427757904745, -0.6374239897486881912 ) ) ;
#33795=VERTEX_POINT ( 'NONE', #28963 ) ;
#33798=VECTOR ( 'NONE', #2991, 1000.000000000000000 ) ;
#33819=DIRECTION ( 'NONE',  ( 0.000000000000000000, -0.9048270524660146918, -0.4257792915650830956 ) ) ;
#33822=FACE_OUTER_BOUND ( 'NONE', #30997, .T. ) ;
#33828=CARTESIAN_POINT ( 'NONE',  ( 7.999999999999992895, 20.99948489194422763, 42.60488980472790388 ) ) ;
#33830=ORIENTED_EDGE ( 'NONE', *, *, #1423, .F. ) ;
#33834=ORIENTED_EDGE ( 'NONE', *, *, #21648, .F. ) ;
#33836=VERTEX_POINT ( 'NONE', #15254 ) ;
#33838=LINE ( 'NONE', #20127, #6208 ) ;
#33840=VERTEX_POINT ( 'NONE', #15075 ) ;
#33843=DIRECTION ( 'NONE',  ( 0.000000000000000000, -6.982962677686266711E-15, 1.000000000000000000 ) ) ;
#33849=VERTEX_POINT ( 'NONE', #20828 ) ;
#33853=CIRCLE ( 'NONE', #13186, 20.00000000000000711 ) ;
#33861=VERTEX_POINT ( 'NONE', #26447 ) ;
#33863=DIRECTION ( 'NONE',  ( 0.000000000000000000, 0.000000000000000000, 1.000000000000000000 ) ) ;
#33865=ORIENTED_EDGE ( 'NONE', *, *, #3578, .T. ) ;
#33876=ORIENTED_EDGE ( 'NONE', *, *, #29, .F. ) ;
#33878=EDGE_CURVE ( 'NONE', #2676, #25030, #15605, .T. ) ;
#33881=ORIENTED_EDGE ( 'NONE', *, *, #5135, .F. ) ;
#33893=VECTOR ( 'NONE', #21005, 1000.000000000000000 ) ;
#33896=FACE_OUTER_BOUND ( 'NONE', #23569, .T. ) ;
#33902=EDGE_CURVE ( 'NONE', #3119, #18391, #24625, .T. ) ;
#33904=FACE_OUTER_BOUND ( 'NONE', #19857, .T. ) ;
#33905=CARTESIAN_POINT ( 'NONE',  ( 7.999999999999992895, -46.87740477351715640, -3.172455868805712509 ) ) ;
#33912=CARTESIAN_POINT ( 'NONE',  ( 7.999999999999992895, 51.85248208264518865, 3.914090171286368935 ) ) ;
#33913=DIRECTION ( 'NONE',  ( -1.000000000000000000, -0.000000000000000000, 0.000000000000000000 ) ) ;
#33916=VECTOR ( 'NONE', #33077, 1000.000000000000000 ) ;
#33918=VECTOR ( 'NONE', #145, 1000.000000000000000 ) ;
#33920=DIRECTION ( 'NONE',  ( 0.000000000000000000, 0.9822872507286893873, -0.1873813145857213258 ) ) ;
#33924=FACE_OUTER_BOUND ( 'NONE', #29678, .T. ) ;
#33927=ORIENTED_EDGE ( 'NONE', *, *, #16250, .T. ) ;
#33928=EDGE_LOOP ( 'NONE', ( #14828, #32810, #4226, #31976 ) ) ;
#33934=FACE_OUTER_BOUND ( 'NONE', #4765, .T. ) ;
#33941=DIRECTION ( 'NONE',  ( -1.000000000000000000, -0.000000000000000000, 0.000000000000000000 ) ) ;
#33942=CIRCLE ( 'NONE', #31647, 20.00000000000000711 ) ;
#33947=CARTESIAN_POINT ( 'NONE',  ( 7.999999999999992895, -17.08890430202718491, -43.76671000081963570 ) ) ;
#33955=DIRECTION ( 'NONE',  ( -1.000000000000000000, 0.000000000000000000, 0.000000000000000000 ) ) ;
#33962=CIRCLE ( 'NONE', #18427, 52.00000000000000711 ) ;
#33968=AXIS2_PLACEMENT_3D ( 'NONE', #29660, #32003, #32183 ) ;
#33970=EDGE_CURVE ( 'NONE', #35265, #17430, #34997, .T. ) ;
#33977=CIRCLE ( 'NONE', #12723, 47.49900000000001654 ) ;
#33983=EDGE_CURVE ( 'NONE', #32383, #18097, #6799, .T. ) ;
#33987=VERTEX_POINT ( 'NONE', #16145 ) ;
#33998=CIRCLE ( 'NONE', #18465, 52.00000000000000711 ) ;
#34004=CARTESIAN_POINT ( 'NONE',  ( 0.000000000000000000, -15.49408907645203470, 44.90087086784588877 ) ) ;
#34017=CYLINDRICAL_SURFACE ( 'NONE', #16896, 20.00000000000000711 ) ;
#34024=AXIS2_PLACEMENT_3D ( 'NONE', #14509, #23339, #17932 ) ;
#34035=DIRECTION ( 'NONE',  ( 0.000000000000000000, -0.9980267284282708928, -0.06279051952932446223 ) ) ;
#34037=CARTESIAN_POINT ( 'NONE',  ( 4.000000000000003553, -47.32430374665947426, 21.55018039121510398 ) ) ;
#34040=ORIENTED_EDGE ( 'NONE', *, *, #2370, .F. ) ;
#34045=EDGE_LOOP ( 'NONE', ( #8419, #10944, #5648, #8497 ) ) ;
#34049=DIRECTION ( 'NONE',  ( 0.000000000000000000, 0.000000000000000000, -1.000000000000000000 ) ) ;
#34054=DIRECTION ( 'NONE',  ( 0.000000000000000000, 0.4817536741017164337, -0.8763066800438629178 ) ) ;
#34056=EDGE_LOOP ( 'NONE', ( #31004, #1242, #22473, #35482 ) ) ;
#34062=ORIENTED_EDGE ( 'NONE', *, *, #5609, .T. ) ;
#34063=DIRECTION ( 'NONE',  ( -1.000000000000000000, -0.000000000000000000, 0.000000000000000000 ) ) ;
#34066=CARTESIAN_POINT ( 'NONE',  ( 7.999999999999992895, 0.000000000000000000, 0.000000000000000000 ) ) ;
#34071=VECTOR ( 'NONE', #19270, 1000.000000000000000 ) ;
#34075=CARTESIAN_POINT ( 'NONE',  ( 7.999999999999992895, 0.000000000000000000, 0.000000000000000000 ) ) ;
#34078=LINE ( 'NONE', #12468, #27198 ) ;
#34082=CYLINDRICAL_SURFACE ( 'NONE', #20437, 20.00000000000000711 ) ;
#34083=CIRCLE ( 'NONE', #22573, 52.00000000000000711 ) ;
#34084=AXIS2_PLACEMENT_3D ( 'NONE', #33947, #11613, #3706 ) ;
#34092=CIRCLE ( 'NONE', #2500, 20.00000000000000711 ) ;
#34095=CARTESIAN_POINT ( 'NONE',  ( 7.999999999999992895, -17.08890430202718491, -43.76671000081963570 ) ) ;
#34103=DIRECTION ( 'NONE',  ( -1.000000000000000000, 0.000000000000000000, 0.000000000000000000 ) ) ;
#34108=EDGE_LOOP ( 'NONE', ( #16414, #3967, #26724, #29922 ) ) ;
#34109=ADVANCED_FACE ( 'NONE', ( #30731 ), #6414, .T. ) ;
#34112=VERTEX_POINT ( 'NONE', #14159 ) ;
#34118=CIRCLE ( 'NONE', #4244, 20.00000000000000711 ) ;
#34125=CARTESIAN_POINT ( 'NONE',  ( 7.999999999999992895, 46.21320724403665281, -10.97699764141904488 ) ) ;
#34134=DIRECTION ( 'NONE',  ( -1.000000000000000000, 0.000000000000000000, 0.000000000000000000 ) ) ;
#34138=ORIENTED_EDGE ( 'NONE', *, *, #16107, .F. ) ;
#34139=EDGE_CURVE ( 'NONE', #19094, #12307, #34425, .T. ) ;
#34148=AXIS2_PLACEMENT_3D ( 'NONE', #26195, #9807, #26564 ) ;
#34156=DIRECTION ( 'NONE',  ( 0.000000000000000000, 0.000000000000000000, -1.000000000000000000 ) ) ;
#34161=ORIENTED_EDGE ( 'NONE', *, *, #23614, .F. ) ;
#34163=CARTESIAN_POINT ( 'NONE',  ( 0.000000000000000000, 43.55304910509406824, 28.41006711800001128 ) ) ;
#34170=CARTESIAN_POINT ( 'NONE',  ( 0.000000000000000000, 22.43957647427220081, -41.27978878573601662 ) ) ;
#34175=CARTESIAN_POINT ( 'NONE',  ( 0.000000000000000000, -2.123073309835510791, 47.45152853935334747 ) ) ;
#34178=CYLINDRICAL_SURFACE ( 'NONE', #15898, 20.00000000000000355 ) ;
#34180=CARTESIAN_POINT ( 'NONE',  ( 4.000000000000003553, -18.53613841426757958, -48.58406706613921244 ) ) ;
#34186=EDGE_CURVE ( 'NONE', #26304, #12651, #828, .T. ) ;
#34191=DIRECTION ( 'NONE',  ( -1.000000000000000000, 0.000000000000000000, 0.000000000000000000 ) ) ;
#34205=DIRECTION ( 'NONE',  ( 1.000000000000000000, -0.000000000000000000, -0.000000000000000000 ) ) ;
#34218=DIRECTION ( 'NONE',  ( -1.000000000000000000, 0.000000000000000000, -0.000000000000000000 ) ) ;
#34220=DIRECTION ( 'NONE',  ( 0.000000000000000000, 0.000000000000000000, -1.000000000000000000 ) ) ;
#34222=ORIENTED_EDGE ( 'NONE', *, *, #3903, .T. ) ;
#34224=ORIENTED_EDGE ( 'NONE', *, *, #8563, .T. ) ;
#34228=CARTESIAN_POINT ( 'NONE',  ( 7.999999999999992895, 37.91532898920963390, -28.61088654061597225 ) ) ;
#34230=AXIS2_PLACEMENT_3D ( 'NONE', #18781, #21652, #13564 ) ;
#34236=AXIS2_PLACEMENT_3D ( 'NONE', #7195, #18362, #5056 ) ;
#34239=ORIENTED_EDGE ( 'NONE', *, *, #24788, .F. ) ;
#34249=AXIS2_PLACEMENT_3D ( 'NONE', #24583, #14280, #27469 ) ;
#34250=ORIENTED_EDGE ( 'NONE', *, *, #34440, .T. ) ;
#34259=AXIS2_PLACEMENT_3D ( 'NONE', #26616, #7344, #12571 ) ;
#34260=DIRECTION ( 'NONE',  ( 0.000000000000000000, 0.000000000000000000, 1.000000000000000000 ) ) ;
#34264=DIRECTION ( 'NONE',  ( -1.000000000000000000, -0.000000000000000000, 0.000000000000000000 ) ) ;
#34269=AXIS2_PLACEMENT_3D ( 'NONE', #18046, #34632, #20916 ) ;
#34274=CARTESIAN_POINT ( 'NONE',  ( 7.999999999999992895, -44.25018368420724357, -27.31155879685229237 ) ) ;
#34275=CIRCLE ( 'NONE', #18149, 20.00000000000000711 ) ;
#34279=LINE ( 'NONE', #9610, #30834 ) ;
#34290=ORIENTED_EDGE ( 'NONE', *, *, #14120, .T. ) ;
#34292=DIRECTION ( 'NONE',  ( 0.000000000000000000, 0.2486898871648552389, -0.9685831611286310761 ) ) ;
#34293=DIRECTION ( 'NONE',  ( 0.000000000000000000, 0.000000000000000000, 1.000000000000000000 ) ) ;
#34298=CARTESIAN_POINT ( 'NONE',  ( 4.000000000000003553, -31.08872492059985859, 41.68322423723089543 ) ) ;
#34299=EDGE_CURVE ( 'NONE', #34977, #6171, #6948, .T. ) ;
#34301=VECTOR ( 'NONE', #33330, 1000.000000000000000 ) ;
#34302=CIRCLE ( 'NONE', #19900, 20.00000000000000711 ) ;
#34304=DIRECTION ( 'NONE',  ( 0.000000000000000000, 0.1253332335642974305, 0.9921147013144787641 ) ) ;
#34306=FACE_OUTER_BOUND ( 'NONE', #10104, .T. ) ;
#34317=DIRECTION ( 'NONE',  ( 0.000000000000000000, 0.000000000000000000, 1.000000000000000000 ) ) ;
#34326=AXIS2_PLACEMENT_3D ( 'NONE', #33421, #8742, #3024 ) ;
#34336=VECTOR ( 'NONE', #18265, 1000.000000000000000 ) ;
#34337=LINE ( 'NONE', #14338, #6793 ) ;
#34339=CARTESIAN_POINT ( 'NONE',  ( 7.999999999999992895, -47.22458491092817212, -5.098390039074724100 ) ) ;
#34349=CARTESIAN_POINT ( 'NONE',  ( 7.999999999999992895, -22.43957647427129842, -41.27978878573651400 ) ) ;
#34350=DIRECTION ( 'NONE',  ( 0.000000000000000000, -0.5877852522924624790, -0.8090169943749551118 ) ) ;
#34357=CARTESIAN_POINT ( 'NONE',  ( 0.000000000000000000, 26.17370628620655282, 39.63700417846173707 ) ) ;
#34374=CARTESIAN_POINT ( 'NONE',  ( 7.999999999999992895, 30.93515269692163372, -36.04401931830219752 ) ) ;
#34376=ORIENTED_EDGE ( 'NONE', *, *, #10515, .F. ) ;
#34378=ORIENTED_EDGE ( 'NONE', *, *, #28206, .F. ) ;
#34386=AXIS2_PLACEMENT_3D ( 'NONE', #23563, #17610, #28620 ) ;
#34389=ORIENTED_EDGE ( 'NONE', *, *, #35524, .T. ) ;
#34390=VERTEX_POINT ( 'NONE', #21333 ) ;
#34401=FACE_OUTER_BOUND ( 'NONE', #16040, .T. ) ;
#34403=DIRECTION ( 'NONE',  ( -1.000000000000000000, -0.000000000000000000, 0.000000000000000000 ) ) ;
#34406=ADVANCED_FACE ( 'NONE', ( #26763 ), #5503, .F. ) ;
#34412=ORIENTED_EDGE ( 'NONE', *, *, #18348, .T. ) ;
#34422=DIRECTION ( 'NONE',  ( -1.000000000000000000, -0.000000000000000000, 0.000000000000000000 ) ) ;
#34423=CARTESIAN_POINT ( 'NONE',  ( 7.999999999999992895, -46.77034588191320807, 22.72740077717213936 ) ) ;
#34425=CIRCLE ( 'NONE', #20508, 20.00000000000000711 ) ;
#34435=DIRECTION ( 'NONE',  ( 0.000000000000000000, 0.9822872507286892763, -0.1873813145857214646 ) ) ;
#34437=VERTEX_POINT ( 'NONE', #2635 ) ;
#34440=EDGE_CURVE ( 'NONE', #6697, #21923, #4969, .T. ) ;
#34444=EDGE_LOOP ( 'NONE', ( #34689, #7313, #14, #11593 ) ) ;
#34454=ORIENTED_EDGE ( 'NONE', *, *, #4761, .F. ) ;
#34458=ORIENTED_EDGE ( 'NONE', *, *, #33970, .F. ) ;
#34464=CARTESIAN_POINT ( 'NONE',  ( 0.000000000000000000, -29.60891106212813995, 37.14118181634756866 ) ) ;
#34467=EDGE_CURVE ( 'NONE', #1935, #20040, #15859, .T. ) ;
#34468=CARTESIAN_POINT ( 'NONE',  ( 0.000000000000000000, -3.840921266749480534, -47.34345070675175293 ) ) ;
#34471=ORIENTED_EDGE ( 'NONE', *, *, #30160, .F. ) ;
#34476=EDGE_LOOP ( 'NONE', ( #33566, #29810, #23493, #28694 ) ) ;
#34479=CARTESIAN_POINT ( 'NONE',  ( 0.000000000000000000, -47.22458491092817212, -5.098390039074724100 ) ) ;
#34483=VECTOR ( 'NONE', #10742, 1000.000000000000000 ) ;
#34492=CIRCLE ( 'NONE', #23560, 20.00000000000000711 ) ;
#34493=DIRECTION ( 'NONE',  ( -1.000000000000000000, -0.000000000000000000, 0.000000000000000000 ) ) ;
#34495=DIRECTION ( 'NONE',  ( -1.000000000000000000, -0.000000000000000000, -0.000000000000000000 ) ) ;
#34499=ORIENTED_EDGE ( 'NONE', *, *, #17210, .F. ) ;
#34501=DIRECTION ( 'NONE',  ( -1.000000000000000000, 0.000000000000000000, -0.000000000000000000 ) ) ;
#34505=ADVANCED_FACE ( 'NONE', ( #25469 ), #14113, .T. ) ;
#34515=CYLINDRICAL_SURFACE ( 'NONE', #13143, 20.00000000000000711 ) ;
#34520=ORIENTED_EDGE ( 'NONE', *, *, #16068, .T. ) ;
#34525=CYLINDRICAL_SURFACE ( 'NONE', #4041, 52.00000000000000711 ) ;
#34527=CARTESIAN_POINT ( 'NONE',  ( 7.999999999999992895, 44.47301969247469344, -16.68249143361863318 ) ) ;
#34531=DIRECTION ( 'NONE',  ( -1.000000000000000000, 0.000000000000000000, 0.000000000000000000 ) ) ;
#34537=CYLINDRICAL_SURFACE ( 'NONE', #29661, 52.00000000000000711 ) ;
#34540=DIRECTION ( 'NONE',  ( -1.000000000000000000, -0.000000000000000000, -0.000000000000000000 ) ) ;
#34541=EDGE_LOOP ( 'NONE', ( #30874, #10103, #26708, #9819 ) ) ;
#34545=DIRECTION ( 'NONE',  ( -1.000000000000000000, 0.000000000000000000, -0.000000000000000000 ) ) ;
#34554=ADVANCED_FACE ( 'NONE', ( #27822 ), #11594, .T. ) ;
#34559=EDGE_CURVE ( 'NONE', #453, #35403, #26812, .T. ) ;
#34562=DIRECTION ( 'NONE',  ( -1.000000000000000000, 0.000000000000000000, -0.000000000000000000 ) ) ;
#34563=EDGE_LOOP ( 'NONE', ( #23417, #14780, #1575, #29118 ) ) ;
#34575=DIRECTION ( 'NONE',  ( -1.000000000000000000, -0.000000000000000000, -0.000000000000000000 ) ) ;
#34583=DIRECTION ( 'NONE',  ( -1.000000000000000000, -0.000000000000000000, -0.000000000000000000 ) ) ;
#34584=VERTEX_POINT ( 'NONE', #16984 ) ;
#34596=EDGE_CURVE ( 'NONE', #28129, #4109, #8386, .T. ) ;
#34600=AXIS2_PLACEMENT_3D ( 'NONE', #6998, #34562, #31501 ) ;
#34604=ORIENTED_EDGE ( 'NONE', *, *, #25112, .T. ) ;
#34610=EDGE_LOOP ( 'NONE', ( #33683, #23233, #2598, #10140 ) ) ;
#34614=VERTEX_POINT ( 'NONE', #12308 ) ;
#34624=CARTESIAN_POINT ( 'NONE',  ( 7.999999999999992895, 0.000000000000000000, 0.000000000000000000 ) ) ;
#34627=DIRECTION ( 'NONE',  ( 0.000000000000000000, 0.000000000000000000, 1.000000000000000000 ) ) ;
#34628=CARTESIAN_POINT ( 'NONE',  ( 7.999999999999992895, -42.03146605346771025, -22.12489237027362421 ) ) ;
#34630=ORIENTED_EDGE ( 'NONE', *, *, #30642, .F. ) ;
#34632=DIRECTION ( 'NONE',  ( -1.000000000000000000, -0.000000000000000000, -0.000000000000000000 ) ) ;
#34635=ADVANCED_FACE ( 'NONE', ( #26359 ), #17878, .T. ) ;
#34637=EDGE_CURVE ( 'NONE', #15571, #32324, #1515, .T. ) ;
#34648=AXIS2_PLACEMENT_3D ( 'NONE', #29651, #13614, #10392 ) ;
#34658=DIRECTION ( 'NONE',  ( -1.000000000000000000, 0.000000000000000000, 0.000000000000000000 ) ) ;
#34659=ADVANCED_FACE ( 'NONE', ( #1693 ), #31921, .T. ) ;
#34665=FACE_OUTER_BOUND ( 'NONE', #28581, .T. ) ;
#34673=ORIENTED_EDGE ( 'NONE', *, *, #11910, .T. ) ;
#34676=DIRECTION ( 'NONE',  ( -1.000000000000000000, 0.000000000000000000, 0.000000000000000000 ) ) ;
#34686=CARTESIAN_POINT ( 'NONE',  ( 7.999999999999992895, 37.91532898920923600, 28.61088654061652647 ) ) ;
#34689=ORIENTED_EDGE ( 'NONE', *, *, #9303, .T. ) ;
#34702=ORIENTED_EDGE ( 'NONE', *, *, #1333, .F. ) ;
#34720=ORIENTED_EDGE ( 'NONE', *, *, #26022, .T. ) ;
#34726=ORIENTED_EDGE ( 'NONE', *, *, #3781, .T. ) ;
#34728=CARTESIAN_POINT ( 'NONE',  ( 7.999999999999992895, 39.78933988720149273, -24.98727647984960853 ) ) ;
#34731=ORIENTED_EDGE ( 'NONE', *, *, #10850, .F. ) ;
#34734=CARTESIAN_POINT ( 'NONE',  ( 0.000000000000000000, 11.46872990052381880, 45.56340405422447049 ) ) ;
#34737=CARTESIAN_POINT ( 'NONE',  ( 7.999999999999992895, -9.744342220503712682, 46.48873837489796301 ) ) ;
#34738=ORIENTED_EDGE ( 'NONE', *, *, #32543, .T. ) ;
#34741=CIRCLE ( 'NONE', #12320, 47.49900000000000944 ) ;
#34746=CYLINDRICAL_SURFACE ( 'NONE', #17285, 52.00000000000000711 ) ;
#34749=EDGE_CURVE ( 'NONE', #13787, #14743, #34279, .T. ) ;
#34756=DIRECTION ( 'NONE',  ( -1.000000000000000000, 0.000000000000000000, 0.000000000000000000 ) ) ;
#34758=CARTESIAN_POINT ( 'NONE',  ( 7.999999999999992895, -5.871425383721172508, -51.66745943012291065 ) ) ;
#34760=ORIENTED_EDGE ( 'NONE', *, *, #29153, .F. ) ;
#34765=DIRECTION ( 'NONE',  ( 0.000000000000000000, 0.000000000000000000, 1.000000000000000000 ) ) ;
#34766=VERTEX_POINT ( 'NONE', #1509 ) ;
#34767=VERTEX_POINT ( 'NONE', #12491 ) ;
#34778=VERTEX_POINT ( 'NONE', #34468 ) ;
#34783=EDGE_LOOP ( 'NONE', ( #12012, #21960, #9352, #24462 ) ) ;
#34787=FACE_OUTER_BOUND ( 'NONE', #34108, .T. ) ;
#34795=FACE_OUTER_BOUND ( 'NONE', #14536, .T. ) ;
#34798=VECTOR ( 'NONE', #20824, 1000.000000000000000 ) ;
#34800=DIRECTION ( 'NONE',  ( 0.000000000000000000, -0.9048270524660235736, 0.4257792915650641663 ) ) ;
#34811=CARTESIAN_POINT ( 'NONE',  ( 7.999999999999992895, 0.000000000000000000, 0.000000000000000000 ) ) ;
#34813=CARTESIAN_POINT ( 'NONE',  ( 0.000000000000000000, 0.000000000000000000, 0.000000000000000000 ) ) ;
#34816=ORIENTED_EDGE ( 'NONE', *, *, #6815, .T. ) ;
#34822=ORIENTED_EDGE ( 'NONE', *, *, #31134, .T. ) ;
#34829=ORIENTED_EDGE ( 'NONE', *, *, #14610, .T. ) ;
#34833=LINE ( 'NONE', #1893, #24092 ) ;
#34834=DIRECTION ( 'NONE',  ( 1.000000000000000000, 0.000000000000000000, 0.000000000000000000 ) ) ;
#34842=DIRECTION ( 'NONE',  ( 0.000000000000000000, 0.000000000000000000, 1.000000000000000000 ) ) ;
#34846=ORIENTED_EDGE ( 'NONE', *, *, #4728, .T. ) ;
#34851=AXIS2_PLACEMENT_3D ( 'NONE', #15068, #17240, #17592 ) ;
#34855=CARTESIAN_POINT ( 'NONE',  ( 7.999999999999992895, 0.000000000000000000, 0.000000000000000000 ) ) ;
#34858=CARTESIAN_POINT ( 'NONE',  ( 0.000000000000000000, 27.43636312076375461, -38.14186064215119387 ) ) ;
#34862=AXIS2_PLACEMENT_3D ( 'NONE', #15929, #32865, #29822 ) ;
#34865=ORIENTED_EDGE ( 'NONE', *, *, #14158, .T. ) ;
#34866=CIRCLE ( 'NONE', #31401, 20.00000000000000711 ) ;
#34880=AXIS2_PLACEMENT_3D ( 'NONE', #2761, #10312, #35338 ) ;
#34886=FACE_OUTER_BOUND ( 'NONE', #4170, .T. ) ;
#34904=CARTESIAN_POINT ( 'NONE',  ( 7.999999999999992895, 6.109652351742432153, -46.58570277113502556 ) ) ;
#34907=DIRECTION ( 'NONE',  ( 0.000000000000000000, 0.000000000000000000, 1.000000000000000000 ) ) ;
#34908=ORIENTED_EDGE ( 'NONE', *, *, #12730, .T. ) ;
#34916=CARTESIAN_POINT ( 'NONE',  ( 0.000000000000000000, 36.06787431788677623, 37.45808914225502662 ) ) ;
#34917=VERTEX_POINT ( 'NONE', #15524 ) ;
#34923=DIRECTION ( 'NONE',  ( 1.000000000000000000, 0.000000000000000000, 0.000000000000000000 ) ) ;
#34934=DIRECTION ( 'NONE',  ( 0.000000000000000000, 0.000000000000000000, 1.000000000000000000 ) ) ;
#34935=ORIENTED_EDGE ( 'NONE', *, *, #1867, .F. ) ;
#34936=DIRECTION ( 'NONE',  ( 0.000000000000000000, 0.000000000000000000, 1.000000000000000000 ) ) ;
#34948=CIRCLE ( 'NONE', #27490, 20.00000000000000711 ) ;
#34950=FACE_OUTER_BOUND ( 'NONE', #5689, .T. ) ;
#34961=ORIENTED_EDGE ( 'NONE', *, *, #31271, .T. ) ;
#34968=CARTESIAN_POINT ( 'NONE',  ( 7.999999999999992895, -30.93515269692089120, -36.04401931830286543 ) ) ;
#34973=DIRECTION ( 'NONE',  ( 0.000000000000000000, 0.000000000000000000, 1.000000000000000000 ) ) ;
#34974=AXIS2_PLACEMENT_3D ( 'NONE', #21013, #12581, #12396 ) ;
#34976=ORIENTED_EDGE ( 'NONE', *, *, #19406, .T. ) ;
#34977=VERTEX_POINT ( 'NONE', #19479 ) ;
#34979=EDGE_CURVE ( 'NONE', #30005, #10010, #50, .T. ) ;
#34981=ORIENTED_EDGE ( 'NONE', *, *, #1824, .T. ) ;
#34987=CARTESIAN_POINT ( 'NONE',  ( 7.999999999999992895, 0.000000000000000000, 0.000000000000000000 ) ) ;
#34992=CIRCLE ( 'NONE', #3940, 20.00000000000000711 ) ;
#34995=CARTESIAN_POINT ( 'NONE',  ( 0.000000000000000000, 46.19362259308845609, -8.585149169757999132 ) ) ;
#34997=CIRCLE ( 'NONE', #17142, 20.00000000000000355 ) ;
#35016=CIRCLE ( 'NONE', #12586, 20.00000000000000711 ) ;
#35021=AXIS2_PLACEMENT_3D ( 'NONE', #16997, #22757, #16824 ) ;
#35026=DIRECTION ( 'NONE',  ( 0.000000000000000000, 0.000000000000000000, -1.000000000000000000 ) ) ;
#35028=DIRECTION ( 'NONE',  ( -1.000000000000000000, 0.000000000000000000, 0.000000000000000000 ) ) ;
#35031=LINE ( 'NONE', #8292, #10785 ) ;
#35034=ORIENTED_EDGE ( 'NONE', *, *, #28165, .T. ) ;
#35040=EDGE_CURVE ( 'NONE', #34390, #25018, #10147, .T. ) ;
#35041=CARTESIAN_POINT ( 'NONE',  ( 0.000000000000000000, -0.2227391519119825691, 46.98410307550729215 ) ) ;
#35042=ORIENTED_EDGE ( 'NONE', *, *, #7263, .F. ) ;
#35045=DIRECTION ( 'NONE',  ( 1.000000000000000000, 0.000000000000000000, 0.000000000000000000 ) ) ;
#35051=EDGE_LOOP ( 'NONE', ( #33753, #20387, #32329, #13690 ) ) ;
#35057=ORIENTED_EDGE ( 'NONE', *, *, #20973, .F. ) ;
#35063=ORIENTED_EDGE ( 'NONE', *, *, #20733, .T. ) ;
#35067=CARTESIAN_POINT ( 'NONE',  ( 0.000000000000000000, -42.41764978026593269, -20.20639853260333751 ) ) ;
#35082=CARTESIAN_POINT ( 'NONE',  ( 7.999999999999992895, -5.667686777402029641, 46.64153600743602368 ) ) ;
#35083=CARTESIAN_POINT ( 'NONE',  ( 7.999999999999992895, -19.74581912682808493, -48.10512059033414545 ) ) ;
#35087=CARTESIAN_POINT ( 'NONE',  ( -9.999999999999994671, 0.000000000000000000, 0.000000000000000000 ) ) ;
#35090=CARTESIAN_POINT ( 'NONE',  ( 7.999999999999992895, -27.43636312076294814, -38.14186064215180494 ) ) ;
#35108=VERTEX_POINT ( 'NONE', #20343 ) ;
#35113=ORIENTED_EDGE ( 'NONE', *, *, #16026, .F. ) ;
#35115=AXIS2_PLACEMENT_3D ( 'NONE', #30236, #5576, #27883 ) ;
#35118=DIRECTION ( 'NONE',  ( 0.000000000000000000, 0.9822872507286879440, 0.1873813145857285423 ) ) ;
#35121=AXIS2_PLACEMENT_3D ( 'NONE', #17914, #18631, #26207 ) ;
#35126=DIRECTION ( 'NONE',  ( 0.000000000000000000, 0.000000000000000000, 1.000000000000000000 ) ) ;
#35142=CARTESIAN_POINT ( 'NONE',  ( 4.000000000000003553, 51.93417535146742381, 2.615612846549361770 ) ) ;
#35145=ORIENTED_EDGE ( 'NONE', *, *, #3395, .T. ) ;
#35156=CARTESIAN_POINT ( 'NONE',  ( 7.999999999999992895, 37.91532898920923600, 28.61088654061652647 ) ) ;
#35171=CARTESIAN_POINT ( 'NONE',  ( 7.999999999999992895, 0.000000000000000000, 0.000000000000000000 ) ) ;
#35172=CIRCLE ( 'NONE', #32278, 47.49900000000001654 ) ;
#35178=DIRECTION ( 'NONE',  ( -1.000000000000000000, 0.000000000000000000, -0.000000000000000000 ) ) ;
#35181=DIRECTION ( 'NONE',  ( 1.000000000000000000, 0.000000000000000000, -0.000000000000000000 ) ) ;
#35182=ORIENTED_EDGE ( 'NONE', *, *, #30751, .F. ) ;
#35186=VERTEX_POINT ( 'NONE', #1466 ) ;
#35189=DIRECTION ( 'NONE',  ( -1.000000000000000000, 0.000000000000000000, 0.000000000000000000 ) ) ;
#35193=CIRCLE ( 'NONE', #3567, 20.00000000000000355 ) ;
#35217=EDGE_CURVE ( 'NONE', #10666, #30768, #1568, .T. ) ;
#35235=EDGE_CURVE ( 'NONE', #33428, #33166, #6162, .T. ) ;
#35236=CARTESIAN_POINT ( 'NONE',  ( 7.999999999999992895, 46.11014828289831513, 9.022736828081523441 ) ) ;
#35237=VERTEX_POINT ( 'NONE', #20706 ) ;
#35238=EDGE_LOOP ( 'NONE', ( #26840, #22651, #10287, #8971 ) ) ;
#35241=CIRCLE ( 'NONE', #18544, 20.00000000000000711 ) ;
#35244=DIRECTION ( 'NONE',  ( 0.000000000000000000, 0.9822872507286893873, -0.1873813145857213258 ) ) ;
#35245=EDGE_CURVE ( 'NONE', #23477, #1839, #23972, .T. ) ;
#35252=CIRCLE ( 'NONE', #4211, 47.49900000000000944 ) ;
#35255=FACE_OUTER_BOUND ( 'NONE', #29560, .T. ) ;
#35256=FACE_OUTER_BOUND ( 'NONE', #25804, .T. ) ;
#35257=DIRECTION ( 'NONE',  ( 0.000000000000000000, 0.000000000000000000, 1.000000000000000000 ) ) ;
#35259=EDGE_CURVE ( 'NONE', #34917, #35594, #29557, .T. ) ;
#35265=VERTEX_POINT ( 'NONE', #34968 ) ;
#35269=DIRECTION ( 'NONE',  ( 0.000000000000000000, 0.000000000000000000, -1.000000000000000000 ) ) ;
#35270=AXIS2_PLACEMENT_3D ( 'NONE', #20680, #34403, #6655 ) ;
#35277=EDGE_CURVE ( 'NONE', #7529, #12629, #17637, .T. ) ;
#35278=DIRECTION ( 'NONE',  ( -1.000000000000000000, -0.000000000000000000, -0.000000000000000000 ) ) ;
#35283=EDGE_CURVE ( 'NONE', #7270, #13488, #29378, .T. ) ;
#35293=DIRECTION ( 'NONE',  ( 0.000000000000000000, 0.000000000000000000, 1.000000000000000000 ) ) ;
#35294=ADVANCED_FACE ( 'NONE', ( #32247 ), #32071, .T. ) ;
#35299=DIRECTION ( 'NONE',  ( 0.000000000000000000, 0.000000000000000000, 1.000000000000000000 ) ) ;
#35301=CYLINDRICAL_SURFACE ( 'NONE', #1341, 20.00000000000000355 ) ;
#35303=CARTESIAN_POINT ( 'NONE',  ( 7.999999999999992895, 0.000000000000000000, 0.000000000000000000 ) ) ;
#35304=DIRECTION ( 'NONE',  ( 0.000000000000000000, 0.000000000000000000, 1.000000000000000000 ) ) ;
#35310=EDGE_CURVE ( 'NONE', #26957, #8310, #31453, .T. ) ;
#35320=CIRCLE ( 'NONE', #25540, 47.49900000000001654 ) ;
#35323=DIRECTION ( 'NONE',  ( -1.000000000000000000, -0.000000000000000000, -0.000000000000000000 ) ) ;
#35338=DIRECTION ( 'NONE',  ( 0.000000000000000000, 0.000000000000000000, 1.000000000000000000 ) ) ;
#35340=AXIS2_PLACEMENT_3D ( 'NONE', #29675, #29861, #7876 ) ;
#35341=CIRCLE ( 'NONE', #18066, 52.00000000000000711 ) ;
#35345=DIRECTION ( 'NONE',  ( -1.000000000000000000, -0.000000000000000000, 0.000000000000000000 ) ) ;
#35352=ORIENTED_EDGE ( 'NONE', *, *, #16067, .T. ) ;
#35356=VERTEX_POINT ( 'NONE', #2376 ) ;
#35361=ORIENTED_EDGE ( 'NONE', *, *, #26258, .T. ) ;
#35366=AXIS2_PLACEMENT_3D ( 'NONE', #1593, #25906, #28951 ) ;
#35368=AXIS2_PLACEMENT_3D ( 'NONE', #14326, #14863, #14674 ) ;
#35369=DIRECTION ( 'NONE',  ( 0.000000000000000000, 0.2486898871648482723, 0.9685831611286328524 ) ) ;
#35372=DIRECTION ( 'NONE',  ( 0.000000000000000000, 0.7705132427757861446, 0.6374239897486934092 ) ) ;
#35377=ORIENTED_EDGE ( 'NONE', *, *, #15007, .T. ) ;
#35380=DIRECTION ( 'NONE',  ( 1.000000000000000000, 0.000000000000000000, 0.000000000000000000 ) ) ;
#35381=DIRECTION ( 'NONE',  ( -1.000000000000000000, -0.000000000000000000, 0.000000000000000000 ) ) ;
#35384=LINE ( 'NONE', #7821, #21651 ) ;
#35390=DIRECTION ( 'NONE',  ( 0.000000000000000000, -0.2486898871648622611, 0.9685831611286292997 ) ) ;
#35392=AXIS2_PLACEMENT_3D ( 'NONE', #3721, #822, #33592 ) ;
#35393=ORIENTED_EDGE ( 'NONE', *, *, #29960, .T. ) ;
#35397=DIRECTION ( 'NONE',  ( -1.000000000000000000, -0.000000000000000000, -0.000000000000000000 ) ) ;
#35403=VERTEX_POINT ( 'NONE', #7930 ) ;
#35407=EDGE_CURVE ( 'NONE', #10004, #6879, #8643, .T. ) ;
#35410=ORIENTED_EDGE ( 'NONE', *, *, #7425, .F. ) ;
#35413=CARTESIAN_POINT ( 'NONE',  ( 7.999999999999992895, -31.08872492059928305, -41.68322423723133596 ) ) ;
#35425=DIRECTION ( 'NONE',  ( -1.000000000000000000, 0.000000000000000000, 0.000000000000000000 ) ) ;
#35430=CARTESIAN_POINT ( 'NONE',  ( 50.00005079999998969, 0.000000000000000000, 0.000000000000000000 ) ) ;
#35437=CIRCLE ( 'NONE', #6095, 20.00000000000000711 ) ;
#35438=DIRECTION ( 'NONE',  ( -1.000000000000000000, -0.000000000000000000, 0.000000000000000000 ) ) ;
#35440=ORIENTED_EDGE ( 'NONE', *, *, #4246, .F. ) ;
#35445=DIRECTION ( 'NONE',  ( 0.000000000000000000, -0.7705132427757815927, -0.6374239897486989603 ) ) ;
#35446=ADVANCED_FACE ( 'NONE', ( #8098 ), #25212, .T. ) ;
#35451=DIRECTION ( 'NONE',  ( -1.000000000000000000, 0.000000000000000000, 0.000000000000000000 ) ) ;
#35458=CARTESIAN_POINT ( 'NONE',  ( 7.999999999999992895, 24.47917365150010482, -45.87777302070911389 ) ) ;
#35469=DIRECTION ( 'NONE',  ( 0.000000000000000000, 0.000000000000000000, 1.000000000000000000 ) ) ;
#35470=EDGE_LOOP ( 'NONE', ( #927, #27569, #19591, #13821 ) ) ;
#35472=CARTESIAN_POINT ( 'NONE',  ( 0.000000000000000000, 0.000000000000000000, 0.000000000000000000 ) ) ;
#35482=ORIENTED_EDGE ( 'NONE', *, *, #10850, .T. ) ;
#35484=DIRECTION ( 'NONE',  ( 0.000000000000000000, -1.000000000000000000, 0.000000000000000000 ) ) ;
#35491=AXIS2_PLACEMENT_3D ( 'NONE', #6349, #30497, #11225 ) ;
#35492=CARTESIAN_POINT ( 'NONE',  ( 7.999999999999992895, 5.871425383722286284, -51.66745943012276854 ) ) ;
#35496=CARTESIAN_POINT ( 'NONE',  ( 0.000000000000000000, 0.000000000000000000, 0.000000000000000000 ) ) ;
#35497=EDGE_CURVE ( 'NONE', #7838, #12939, #32774, .T. ) ;
#35498=CIRCLE ( 'NONE', #25701, 47.49900000000001654 ) ;
#35506=CYLINDRICAL_SURFACE ( 'NONE', #6407, 47.49900000000001654 ) ;
#35508=CARTESIAN_POINT ( 'NONE',  ( 4.000000000000003553, 39.64889472655731595, 33.64468972902522381 ) ) ;
#35515=DIRECTION ( 'NONE',  ( 0.000000000000000000, 0.000000000000000000, 1.000000000000000000 ) ) ;
#35517=AXIS2_PLACEMENT_3D ( 'NONE', #15230, #15762, #10028 ) ;
#35518=ORIENTED_EDGE ( 'NONE', *, *, #5691, .T. ) ;
#35521=DIRECTION ( 'NONE',  ( -1.000000000000000000, 0.000000000000000000, -0.000000000000000000 ) ) ;
#35524=EDGE_CURVE ( 'NONE', #352, #25438, #22313, .T. ) ;
#35529=EDGE_CURVE ( 'NONE', #25030, #13426, #32789, .T. ) ;
#35537=ORIENTED_EDGE ( 'NONE', *, *, #25380, .T. ) ;
#35541=ORIENTED_EDGE ( 'NONE', *, *, #3533, .T. ) ;
#35554=CIRCLE ( 'NONE', #34386, 52.00000000000000711 ) ;
#35556=AXIS2_PLACEMENT_3D ( 'NONE', #20621, #25704, #17038 ) ;
#35558=DIRECTION ( 'NONE',  ( 0.000000000000000000, -0.9048270524660146918, -0.4257792915650830956 ) ) ;
#35563=DIRECTION ( 'NONE',  ( -1.000000000000000000, 0.000000000000000000, -0.000000000000000000 ) ) ;
#35567=CARTESIAN_POINT ( 'NONE',  ( 7.999999999999992895, -46.11014828289849277, 9.022736828080537563 ) ) ;
#35569=CARTESIAN_POINT ( 'NONE',  ( 0.000000000000000000, 46.77034588191337150, -22.72740077717178053 ) ) ;
#35570=DIRECTION ( 'NONE',  ( 0.000000000000000000, -0.3681245526846853022, 0.9297764858882484607 ) ) ;
#35576=DIRECTION ( 'NONE',  ( -1.000000000000000000, 0.000000000000000000, 0.000000000000000000 ) ) ;
#35578=AXIS2_PLACEMENT_3D ( 'NONE', #24475, #26828, #35293 ) ;
#35584=DIRECTION ( 'NONE',  ( 0.000000000000000000, 0.000000000000000000, 1.000000000000000000 ) ) ;
#35585=DIRECTION ( 'NONE',  ( -1.000000000000000000, 0.000000000000000000, -0.000000000000000000 ) ) ;
#35590=VERTEX_POINT ( 'NONE', #15398 ) ;
#35594=VERTEX_POINT ( 'NONE', #3924 ) ;
#35595=CARTESIAN_POINT ( 'NONE',  ( 4.000000000000003553, 31.08872492060014991, -41.68322423723069647 ) ) ;
#35597=CARTESIAN_POINT ( 'NONE',  ( 7.999999999999992895, 0.000000000000000000, 0.000000000000000000 ) ) ;
#35600=AXIS2_PLACEMENT_3D ( 'NONE', #32299, #16424, #2428 ) ;
#35605=DIRECTION ( 'NONE',  ( 0.000000000000000000, -6.982962677686266711E-15, 1.000000000000000000 ) ) ;
#35608=CARTESIAN_POINT ( 'NONE',  ( 50.00005079999998969, 0.000000000000000000, 0.000000000000000000 ) ) ;
#35609=PRESENTATION_STYLE_ASSIGNMENT (( #25151 ) ) ;
#35615=ORIENTED_EDGE ( 'NONE', *, *, #25116, .F. ) ;
ENDSEC;
END-ISO-10303-21;
